ISO-10303-21;
HEADER;
/* Generated by software containing ST-Developer
 * from STEP Tools, Inc. (www.steptools.com) 
 */

FILE_DESCRIPTION(
/* description */ (''),
/* implementation_level */ '2;1');

FILE_NAME(
/* name */ 'ISO 4762 - M2.5 x 6 - 12.9 (Rack Screw).step',
/* time_stamp */ '2026-10-05T09:57:53+05:00',
/* author */ (''),
/* organization */ (''),
/* preprocessor_version */ 'ST-DEVELOPER v20.2',
/* originating_system */ 'Autodesk Translation Framework v15.15.0.0',
/* authorisation */ '');

FILE_SCHEMA (('AUTOMOTIVE_DESIGN { 1 0 10303 214 3 1 1 }'));
ENDSEC;

DATA;
#10=MECHANICAL_DESIGN_GEOMETRIC_PRESENTATION_REPRESENTATION('',(#567),#113984);
#108=TOROIDAL_SURFACE('',#63498,1.315,0.1);
#109=TOROIDAL_SURFACE('',#63692,2.05,0.2);
#431=(
BOUNDED_CURVE()
B_SPLINE_CURVE(2,(#112949,#112950,#112951),.UNSPECIFIED.,.F.,.F.)
B_SPLINE_CURVE_WITH_KNOTS((3,3),(0.0227595441420062,0.0437553375522101),
 .UNSPECIFIED.)
CURVE()
GEOMETRIC_REPRESENTATION_ITEM()
RATIONAL_B_SPLINE_CURVE((1.00144169675558,1.00138583461502,1.))
REPRESENTATION_ITEM('')
);
#432=(
BOUNDED_CURVE()
B_SPLINE_CURVE(2,(#112963,#112964,#112965),.UNSPECIFIED.,.F.,.F.)
B_SPLINE_CURVE_WITH_KNOTS((3,3),(0.,0.0209957934101858),.UNSPECIFIED.)
CURVE()
GEOMETRIC_REPRESENTATION_ITEM()
RATIONAL_B_SPLINE_CURVE((1.,1.00138583461543,1.001441696756))
REPRESENTATION_ITEM('')
);
#433=(
BOUNDED_CURVE()
B_SPLINE_CURVE(2,(#113258,#113259,#113260),.UNSPECIFIED.,.F.,.F.)
B_SPLINE_CURVE_WITH_KNOTS((3,3),(0.0227595441420239,0.0437553375522102),
 .UNSPECIFIED.)
CURVE()
GEOMETRIC_REPRESENTATION_ITEM()
RATIONAL_B_SPLINE_CURVE((1.00144169675773,1.00138583461709,1.))
REPRESENTATION_ITEM('')
);
#434=(
BOUNDED_CURVE()
B_SPLINE_CURVE(2,(#113267,#113268,#113269),.UNSPECIFIED.,.F.,.F.)
B_SPLINE_CURVE_WITH_KNOTS((3,3),(0.,0.0209957934101477),.UNSPECIFIED.)
CURVE()
GEOMETRIC_REPRESENTATION_ITEM()
RATIONAL_B_SPLINE_CURVE((1.,1.00138583461455,1.00144169675509))
REPRESENTATION_ITEM('')
);
#435=(
BOUNDED_CURVE()
B_SPLINE_CURVE(2,(#113272,#113273,#113274),.UNSPECIFIED.,.F.,.F.)
B_SPLINE_CURVE_WITH_KNOTS((3,3),(0.0227595441420216,0.04375533755221),
 .UNSPECIFIED.)
CURVE()
GEOMETRIC_REPRESENTATION_ITEM()
RATIONAL_B_SPLINE_CURVE((1.00144169675475,1.00138583461423,1.))
REPRESENTATION_ITEM('')
);
#436=(
BOUNDED_CURVE()
B_SPLINE_CURVE(2,(#113281,#113282,#113283),.UNSPECIFIED.,.F.,.F.)
B_SPLINE_CURVE_WITH_KNOTS((3,3),(0.,0.020995793410179),.UNSPECIFIED.)
CURVE()
GEOMETRIC_REPRESENTATION_ITEM()
RATIONAL_B_SPLINE_CURVE((1.,1.00138583461437,1.0014416967549))
REPRESENTATION_ITEM('')
);
#437=(
BOUNDED_CURVE()
B_SPLINE_CURVE(2,(#113286,#113287,#113288),.UNSPECIFIED.,.F.,.F.)
B_SPLINE_CURVE_WITH_KNOTS((3,3),(0.0227595441420233,0.0437553375522096),
 .UNSPECIFIED.)
CURVE()
GEOMETRIC_REPRESENTATION_ITEM()
RATIONAL_B_SPLINE_CURVE((1.0014416967577,1.00138583461706,1.))
REPRESENTATION_ITEM('')
);
#438=(
BOUNDED_CURVE()
B_SPLINE_CURVE(2,(#113295,#113296,#113297),.UNSPECIFIED.,.F.,.F.)
B_SPLINE_CURVE_WITH_KNOTS((3,3),(0.,0.0209957934101891),.UNSPECIFIED.)
CURVE()
GEOMETRIC_REPRESENTATION_ITEM()
RATIONAL_B_SPLINE_CURVE((1.,1.00138583461396,1.00144169675448))
REPRESENTATION_ITEM('')
);
#439=(
BOUNDED_CURVE()
B_SPLINE_CURVE(2,(#113300,#113301,#113302),.UNSPECIFIED.,.F.,.F.)
B_SPLINE_CURVE_WITH_KNOTS((3,3),(0.0227595441420034,0.04375533755221),
 .UNSPECIFIED.)
CURVE()
GEOMETRIC_REPRESENTATION_ITEM()
RATIONAL_B_SPLINE_CURVE((1.00144169675772,1.00138583461708,1.))
REPRESENTATION_ITEM('')
);
#440=(
BOUNDED_CURVE()
B_SPLINE_CURVE(2,(#113309,#113310,#113311),.UNSPECIFIED.,.F.,.F.)
B_SPLINE_CURVE_WITH_KNOTS((3,3),(0.,0.0209957934101803),.UNSPECIFIED.)
CURVE()
GEOMETRIC_REPRESENTATION_ITEM()
RATIONAL_B_SPLINE_CURVE((1.,1.00138583461545,1.00144169675603))
REPRESENTATION_ITEM('')
);
#441=(
BOUNDED_CURVE()
B_SPLINE_CURVE(2,(#113314,#113315,#113316),.UNSPECIFIED.,.F.,.F.)
B_SPLINE_CURVE_WITH_KNOTS((3,3),(0.0227595441420504,0.0437553375522096),
 .UNSPECIFIED.)
CURVE()
GEOMETRIC_REPRESENTATION_ITEM()
RATIONAL_B_SPLINE_CURVE((1.00144169675773,1.00138583461708,1.))
REPRESENTATION_ITEM('')
);
#442=(
BOUNDED_CURVE()
B_SPLINE_CURVE(2,(#113323,#113324,#113325),.UNSPECIFIED.,.F.,.F.)
B_SPLINE_CURVE_WITH_KNOTS((3,3),(0.,0.0209957934102014),.UNSPECIFIED.)
CURVE()
GEOMETRIC_REPRESENTATION_ITEM()
RATIONAL_B_SPLINE_CURVE((1.,1.00138583461972,1.00144169676047))
REPRESENTATION_ITEM('')
);
#443=(
BOUNDED_CURVE()
B_SPLINE_CURVE(2,(#113328,#113329,#113330),.UNSPECIFIED.,.F.,.F.)
B_SPLINE_CURVE_WITH_KNOTS((3,3),(0.0227595441420253,0.04375533755221),
 .UNSPECIFIED.)
CURVE()
GEOMETRIC_REPRESENTATION_ITEM()
RATIONAL_B_SPLINE_CURVE((1.00144169676086,1.0013858346201,1.))
REPRESENTATION_ITEM('')
);
#444=(
BOUNDED_CURVE()
B_SPLINE_CURVE(2,(#113337,#113338,#113339),.UNSPECIFIED.,.F.,.F.)
B_SPLINE_CURVE_WITH_KNOTS((3,3),(0.,0.0209957934102032),.UNSPECIFIED.)
CURVE()
GEOMETRIC_REPRESENTATION_ITEM()
RATIONAL_B_SPLINE_CURVE((1.,1.00138583461651,1.00144169675713))
REPRESENTATION_ITEM('')
);
#445=(
BOUNDED_CURVE()
B_SPLINE_CURVE(2,(#113342,#113343,#113344),.UNSPECIFIED.,.F.,.F.)
B_SPLINE_CURVE_WITH_KNOTS((3,3),(0.0227595441420214,0.0437553375522101),
 .UNSPECIFIED.)
CURVE()
GEOMETRIC_REPRESENTATION_ITEM()
RATIONAL_B_SPLINE_CURVE((1.00144169675793,1.00138583461728,1.))
REPRESENTATION_ITEM('')
);
#446=(
BOUNDED_CURVE()
B_SPLINE_CURVE(2,(#113351,#113352,#113353),.UNSPECIFIED.,.F.,.F.)
B_SPLINE_CURVE_WITH_KNOTS((3,3),(0.,0.0209957934101777),.UNSPECIFIED.)
CURVE()
GEOMETRIC_REPRESENTATION_ITEM()
RATIONAL_B_SPLINE_CURVE((1.,1.00138583461269,1.00144169675315))
REPRESENTATION_ITEM('')
);
#447=(
BOUNDED_CURVE()
B_SPLINE_CURVE(2,(#113356,#113357,#113358),.UNSPECIFIED.,.F.,.F.)
B_SPLINE_CURVE_WITH_KNOTS((3,3),(0.0227595441419899,0.0437553375522099),
 .UNSPECIFIED.)
CURVE()
GEOMETRIC_REPRESENTATION_ITEM()
RATIONAL_B_SPLINE_CURVE((1.00144169675096,1.00138583461059,1.))
REPRESENTATION_ITEM('')
);
#448=(
BOUNDED_CURVE()
B_SPLINE_CURVE(2,(#113365,#113366,#113367),.UNSPECIFIED.,.F.,.F.)
B_SPLINE_CURVE_WITH_KNOTS((3,3),(0.,0.0209957934101782),.UNSPECIFIED.)
CURVE()
GEOMETRIC_REPRESENTATION_ITEM()
RATIONAL_B_SPLINE_CURVE((1.,1.00138583461646,1.00144169675708))
REPRESENTATION_ITEM('')
);
#449=(
BOUNDED_CURVE()
B_SPLINE_CURVE(2,(#113370,#113371,#113372),.UNSPECIFIED.,.F.,.F.)
B_SPLINE_CURVE_WITH_KNOTS((3,3),(0.0227595441420376,0.0437553375522098),
 .UNSPECIFIED.)
CURVE()
GEOMETRIC_REPRESENTATION_ITEM()
RATIONAL_B_SPLINE_CURVE((1.0014416967547,1.00138583461417,1.))
REPRESENTATION_ITEM('')
);
#450=(
BOUNDED_CURVE()
B_SPLINE_CURVE(2,(#113379,#113380,#113381),.UNSPECIFIED.,.F.,.F.)
B_SPLINE_CURVE_WITH_KNOTS((3,3),(0.,0.020995793410168),.UNSPECIFIED.)
CURVE()
GEOMETRIC_REPRESENTATION_ITEM()
RATIONAL_B_SPLINE_CURVE((1.,1.00138583461699,1.00144169675762))
REPRESENTATION_ITEM('')
);
#451=(
BOUNDED_CURVE()
B_SPLINE_CURVE(2,(#113384,#113385,#113386),.UNSPECIFIED.,.F.,.F.)
B_SPLINE_CURVE_WITH_KNOTS((3,3),(0.0227595441420211,0.0437553375522103),
 .UNSPECIFIED.)
CURVE()
GEOMETRIC_REPRESENTATION_ITEM()
RATIONAL_B_SPLINE_CURVE((1.00144169675723,1.00138583461661,1.))
REPRESENTATION_ITEM('')
);
#452=(
BOUNDED_CURVE()
B_SPLINE_CURVE(2,(#113393,#113394,#113395),.UNSPECIFIED.,.F.,.F.)
B_SPLINE_CURVE_WITH_KNOTS((3,3),(0.,0.0209957934101646),.UNSPECIFIED.)
CURVE()
GEOMETRIC_REPRESENTATION_ITEM()
RATIONAL_B_SPLINE_CURVE((1.,1.00138583461121,1.00144169675162))
REPRESENTATION_ITEM('')
);
#453=(
BOUNDED_CURVE()
B_SPLINE_CURVE(2,(#113398,#113399,#113400),.UNSPECIFIED.,.F.,.F.)
B_SPLINE_CURVE_WITH_KNOTS((3,3),(0.0227595441420204,0.0437553375522103),
 .UNSPECIFIED.)
CURVE()
GEOMETRIC_REPRESENTATION_ITEM()
RATIONAL_B_SPLINE_CURVE((1.0014416967587,1.00138583461803,1.))
REPRESENTATION_ITEM('')
);
#454=(
BOUNDED_CURVE()
B_SPLINE_CURVE(2,(#113407,#113408,#113409),.UNSPECIFIED.,.F.,.F.)
B_SPLINE_CURVE_WITH_KNOTS((3,3),(0.,0.0209957934102059),.UNSPECIFIED.)
CURVE()
GEOMETRIC_REPRESENTATION_ITEM()
RATIONAL_B_SPLINE_CURVE((1.,1.00138583461321,1.00144169675369))
REPRESENTATION_ITEM('')
);
#455=(
BOUNDED_CURVE()
B_SPLINE_CURVE(2,(#113412,#113413,#113414),.UNSPECIFIED.,.F.,.F.)
B_SPLINE_CURVE_WITH_KNOTS((3,3),(0.0227595441420123,0.0437553375522097),
 .UNSPECIFIED.)
CURVE()
GEOMETRIC_REPRESENTATION_ITEM()
RATIONAL_B_SPLINE_CURVE((1.00144169675907,1.00138583461838,1.))
REPRESENTATION_ITEM('')
);
#456=(
BOUNDED_CURVE()
B_SPLINE_CURVE(2,(#113421,#113422,#113423),.UNSPECIFIED.,.F.,.F.)
B_SPLINE_CURVE_WITH_KNOTS((3,3),(0.,0.020995793410209),.UNSPECIFIED.)
CURVE()
GEOMETRIC_REPRESENTATION_ITEM()
RATIONAL_B_SPLINE_CURVE((1.,1.00138583461559,1.00144169675616))
REPRESENTATION_ITEM('')
);
#457=(
BOUNDED_CURVE()
B_SPLINE_CURVE(2,(#113426,#113427,#113428),.UNSPECIFIED.,.F.,.F.)
B_SPLINE_CURVE_WITH_KNOTS((3,3),(0.0227595441420273,0.04375533755221),
 .UNSPECIFIED.)
CURVE()
GEOMETRIC_REPRESENTATION_ITEM()
RATIONAL_B_SPLINE_CURVE((1.00144169675712,1.0013858346165,1.))
REPRESENTATION_ITEM('')
);
#458=(
BOUNDED_CURVE()
B_SPLINE_CURVE(2,(#113435,#113436,#113437),.UNSPECIFIED.,.F.,.F.)
B_SPLINE_CURVE_WITH_KNOTS((3,3),(0.,0.0209957934101636),.UNSPECIFIED.)
CURVE()
GEOMETRIC_REPRESENTATION_ITEM()
RATIONAL_B_SPLINE_CURVE((1.,1.00138583461551,1.00144169675609))
REPRESENTATION_ITEM('')
);
#459=(
BOUNDED_CURVE()
B_SPLINE_CURVE(2,(#113440,#113441,#113442),.UNSPECIFIED.,.F.,.F.)
B_SPLINE_CURVE_WITH_KNOTS((3,3),(0.0227595441420356,0.0437553375522098),
 .UNSPECIFIED.)
CURVE()
GEOMETRIC_REPRESENTATION_ITEM()
RATIONAL_B_SPLINE_CURVE((1.00144169675546,1.00138583461491,1.))
REPRESENTATION_ITEM('')
);
#460=(
BOUNDED_CURVE()
B_SPLINE_CURVE(2,(#113449,#113450,#113451),.UNSPECIFIED.,.F.,.F.)
B_SPLINE_CURVE_WITH_KNOTS((3,3),(0.,0.0209957934102153),.UNSPECIFIED.)
CURVE()
GEOMETRIC_REPRESENTATION_ITEM()
RATIONAL_B_SPLINE_CURVE((1.,1.00138583461812,1.0014416967588))
REPRESENTATION_ITEM('')
);
#461=(
BOUNDED_CURVE()
B_SPLINE_CURVE(2,(#113454,#113455,#113456),.UNSPECIFIED.,.F.,.F.)
B_SPLINE_CURVE_WITH_KNOTS((3,3),(0.0227595441420236,0.0437553375522102),
 .UNSPECIFIED.)
CURVE()
GEOMETRIC_REPRESENTATION_ITEM()
RATIONAL_B_SPLINE_CURVE((1.00144169675374,1.00138583461325,1.))
REPRESENTATION_ITEM('')
);
#462=(
BOUNDED_CURVE()
B_SPLINE_CURVE(2,(#113463,#113464,#113465),.UNSPECIFIED.,.F.,.F.)
B_SPLINE_CURVE_WITH_KNOTS((3,3),(0.,0.0209957934101627),.UNSPECIFIED.)
CURVE()
GEOMETRIC_REPRESENTATION_ITEM()
RATIONAL_B_SPLINE_CURVE((1.,1.00138583461917,1.0014416967599))
REPRESENTATION_ITEM('')
);
#463=(
BOUNDED_CURVE()
B_SPLINE_CURVE(2,(#113468,#113469,#113470),.UNSPECIFIED.,.F.,.F.)
B_SPLINE_CURVE_WITH_KNOTS((3,3),(0.0227595441420239,0.0437553375522098),
 .UNSPECIFIED.)
CURVE()
GEOMETRIC_REPRESENTATION_ITEM()
RATIONAL_B_SPLINE_CURVE((1.00144169675673,1.00138583461613,1.))
REPRESENTATION_ITEM('')
);
#464=(
BOUNDED_CURVE()
B_SPLINE_CURVE(2,(#113477,#113478,#113479),.UNSPECIFIED.,.F.,.F.)
B_SPLINE_CURVE_WITH_KNOTS((3,3),(0.,0.0209957934102122),.UNSPECIFIED.)
CURVE()
GEOMETRIC_REPRESENTATION_ITEM()
RATIONAL_B_SPLINE_CURVE((1.,1.00138583461449,1.00144169675502))
REPRESENTATION_ITEM('')
);
#465=(
BOUNDED_CURVE()
B_SPLINE_CURVE(2,(#113482,#113483,#113484),.UNSPECIFIED.,.F.,.F.)
B_SPLINE_CURVE_WITH_KNOTS((3,3),(0.0227595441420244,0.0437553375522098),
 .UNSPECIFIED.)
CURVE()
GEOMETRIC_REPRESENTATION_ITEM()
RATIONAL_B_SPLINE_CURVE((1.00144169675843,1.00138583461776,1.))
REPRESENTATION_ITEM('')
);
#466=(
BOUNDED_CURVE()
B_SPLINE_CURVE(2,(#113491,#113492,#113493),.UNSPECIFIED.,.F.,.F.)
B_SPLINE_CURVE_WITH_KNOTS((3,3),(0.,0.0209957934102044),.UNSPECIFIED.)
CURVE()
GEOMETRIC_REPRESENTATION_ITEM()
RATIONAL_B_SPLINE_CURVE((1.,1.00138583461816,1.00144169675884))
REPRESENTATION_ITEM('')
);
#467=(
BOUNDED_CURVE()
B_SPLINE_CURVE(2,(#113496,#113497,#113498),.UNSPECIFIED.,.F.,.F.)
B_SPLINE_CURVE_WITH_KNOTS((3,3),(0.0227595441420142,0.0437553375522099),
 .UNSPECIFIED.)
CURVE()
GEOMETRIC_REPRESENTATION_ITEM()
RATIONAL_B_SPLINE_CURVE((1.00144169675525,1.00138583461471,1.))
REPRESENTATION_ITEM('')
);
#468=(
BOUNDED_CURVE()
B_SPLINE_CURVE(2,(#113505,#113506,#113507),.UNSPECIFIED.,.F.,.F.)
B_SPLINE_CURVE_WITH_KNOTS((3,3),(0.,0.0209957934101661),.UNSPECIFIED.)
CURVE()
GEOMETRIC_REPRESENTATION_ITEM()
RATIONAL_B_SPLINE_CURVE((1.,1.00138583461737,1.00144169675803))
REPRESENTATION_ITEM('')
);
#469=(
BOUNDED_CURVE()
B_SPLINE_CURVE(2,(#113510,#113511,#113512),.UNSPECIFIED.,.F.,.F.)
B_SPLINE_CURVE_WITH_KNOTS((3,3),(0.0227595441419954,0.0437553375522101),
 .UNSPECIFIED.)
CURVE()
GEOMETRIC_REPRESENTATION_ITEM()
RATIONAL_B_SPLINE_CURVE((1.00144169675597,1.0013858346154,1.))
REPRESENTATION_ITEM('')
);
#470=(
BOUNDED_CURVE()
B_SPLINE_CURVE(2,(#113519,#113520,#113521),.UNSPECIFIED.,.F.,.F.)
B_SPLINE_CURVE_WITH_KNOTS((3,3),(0.,0.0209957934101572),.UNSPECIFIED.)
CURVE()
GEOMETRIC_REPRESENTATION_ITEM()
RATIONAL_B_SPLINE_CURVE((1.,1.00138583461617,1.00144169675677))
REPRESENTATION_ITEM('')
);
#471=(
BOUNDED_CURVE()
B_SPLINE_CURVE(2,(#113524,#113525,#113526),.UNSPECIFIED.,.F.,.F.)
B_SPLINE_CURVE_WITH_KNOTS((3,3),(0.0227595441420733,0.0437553375522098),
 .UNSPECIFIED.)
CURVE()
GEOMETRIC_REPRESENTATION_ITEM()
RATIONAL_B_SPLINE_CURVE((1.00144169676135,1.00138583462057,1.))
REPRESENTATION_ITEM('')
);
#472=(
BOUNDED_CURVE()
B_SPLINE_CURVE(2,(#113533,#113534,#113535),.UNSPECIFIED.,.F.,.F.)
B_SPLINE_CURVE_WITH_KNOTS((3,3),(0.,0.0209957934101981),.UNSPECIFIED.)
CURVE()
GEOMETRIC_REPRESENTATION_ITEM()
RATIONAL_B_SPLINE_CURVE((1.,1.00138583461495,1.0014416967555))
REPRESENTATION_ITEM('')
);
#473=(
BOUNDED_CURVE()
B_SPLINE_CURVE(2,(#113538,#113539,#113540),.UNSPECIFIED.,.F.,.F.)
B_SPLINE_CURVE_WITH_KNOTS((3,3),(0.022759544142027,0.0437553375522101),
 .UNSPECIFIED.)
CURVE()
GEOMETRIC_REPRESENTATION_ITEM()
RATIONAL_B_SPLINE_CURVE((1.00144169675767,1.00138583461703,1.))
REPRESENTATION_ITEM('')
);
#474=(
BOUNDED_CURVE()
B_SPLINE_CURVE(2,(#113547,#113548,#113549),.UNSPECIFIED.,.F.,.F.)
B_SPLINE_CURVE_WITH_KNOTS((3,3),(0.,0.0209957934102148),.UNSPECIFIED.)
CURVE()
GEOMETRIC_REPRESENTATION_ITEM()
RATIONAL_B_SPLINE_CURVE((1.,1.00138583461343,1.00144169675392))
REPRESENTATION_ITEM('')
);
#475=(
BOUNDED_CURVE()
B_SPLINE_CURVE(2,(#113552,#113553,#113554),.UNSPECIFIED.,.F.,.F.)
B_SPLINE_CURVE_WITH_KNOTS((3,3),(0.0227595441420587,0.04375533755221),
 .UNSPECIFIED.)
CURVE()
GEOMETRIC_REPRESENTATION_ITEM()
RATIONAL_B_SPLINE_CURVE((1.00144169675587,1.0013858346153,1.))
REPRESENTATION_ITEM('')
);
#476=(
BOUNDED_CURVE()
B_SPLINE_CURVE(2,(#113561,#113562,#113563),.UNSPECIFIED.,.F.,.F.)
B_SPLINE_CURVE_WITH_KNOTS((3,3),(0.,0.0209957934101868),.UNSPECIFIED.)
CURVE()
GEOMETRIC_REPRESENTATION_ITEM()
RATIONAL_B_SPLINE_CURVE((1.,1.00138583461518,1.00144169675574))
REPRESENTATION_ITEM('')
);
#477=(
BOUNDED_CURVE()
B_SPLINE_CURVE(2,(#113566,#113567,#113568),.UNSPECIFIED.,.F.,.F.)
B_SPLINE_CURVE_WITH_KNOTS((3,3),(0.0227595441420354,0.0437553375522099),
 .UNSPECIFIED.)
CURVE()
GEOMETRIC_REPRESENTATION_ITEM()
RATIONAL_B_SPLINE_CURVE((1.0014416967583,1.00138583461764,1.))
REPRESENTATION_ITEM('')
);
#478=(
BOUNDED_CURVE()
B_SPLINE_CURVE(2,(#113575,#113576,#113577),.UNSPECIFIED.,.F.,.F.)
B_SPLINE_CURVE_WITH_KNOTS((3,3),(0.,0.0209957934101755),.UNSPECIFIED.)
CURVE()
GEOMETRIC_REPRESENTATION_ITEM()
RATIONAL_B_SPLINE_CURVE((1.,1.00138583461728,1.00144169675792))
REPRESENTATION_ITEM('')
);
#479=(
BOUNDED_CURVE()
B_SPLINE_CURVE(2,(#113580,#113581,#113582),.UNSPECIFIED.,.F.,.F.)
B_SPLINE_CURVE_WITH_KNOTS((3,3),(0.0227595441420414,0.0437553375522097),
 .UNSPECIFIED.)
CURVE()
GEOMETRIC_REPRESENTATION_ITEM()
RATIONAL_B_SPLINE_CURVE((1.00144169676129,1.00138583462051,1.))
REPRESENTATION_ITEM('')
);
#480=(
BOUNDED_CURVE()
B_SPLINE_CURVE(2,(#113589,#113590,#113591),.UNSPECIFIED.,.F.,.F.)
B_SPLINE_CURVE_WITH_KNOTS((3,3),(0.,0.0209957934101856),.UNSPECIFIED.)
CURVE()
GEOMETRIC_REPRESENTATION_ITEM()
RATIONAL_B_SPLINE_CURVE((1.,1.00138583461831,1.001441696759))
REPRESENTATION_ITEM('')
);
#481=(
BOUNDED_CURVE()
B_SPLINE_CURVE(2,(#113594,#113595,#113596),.UNSPECIFIED.,.F.,.F.)
B_SPLINE_CURVE_WITH_KNOTS((3,3),(0.0227595441420472,0.0437553375522097),
 .UNSPECIFIED.)
CURVE()
GEOMETRIC_REPRESENTATION_ITEM()
RATIONAL_B_SPLINE_CURVE((1.00144169675876,1.00138583461808,1.))
REPRESENTATION_ITEM('')
);
#482=(
BOUNDED_CURVE()
B_SPLINE_CURVE(2,(#113603,#113604,#113605),.UNSPECIFIED.,.F.,.F.)
B_SPLINE_CURVE_WITH_KNOTS((3,3),(0.,0.0209957934101722),.UNSPECIFIED.)
CURVE()
GEOMETRIC_REPRESENTATION_ITEM()
RATIONAL_B_SPLINE_CURVE((1.,1.00138583461417,1.0014416967547))
REPRESENTATION_ITEM('')
);
#483=(
BOUNDED_CURVE()
B_SPLINE_CURVE(2,(#113608,#113609,#113610),.UNSPECIFIED.,.F.,.F.)
B_SPLINE_CURVE_WITH_KNOTS((3,3),(0.0227595441420099,0.0437553375522099),
 .UNSPECIFIED.)
CURVE()
GEOMETRIC_REPRESENTATION_ITEM()
RATIONAL_B_SPLINE_CURVE((1.00144169675708,1.00138583461646,1.))
REPRESENTATION_ITEM('')
);
#484=(
BOUNDED_CURVE()
B_SPLINE_CURVE(2,(#113617,#113618,#113619),.UNSPECIFIED.,.F.,.F.)
B_SPLINE_CURVE_WITH_KNOTS((3,3),(0.,0.0209957934101837),.UNSPECIFIED.)
CURVE()
GEOMETRIC_REPRESENTATION_ITEM()
RATIONAL_B_SPLINE_CURVE((1.,1.00138583461363,1.00144169675414))
REPRESENTATION_ITEM('')
);
#485=(
BOUNDED_CURVE()
B_SPLINE_CURVE(2,(#113622,#113623,#113624),.UNSPECIFIED.,.F.,.F.)
B_SPLINE_CURVE_WITH_KNOTS((3,3),(0.0227595441420264,0.0437553375522102),
 .UNSPECIFIED.)
CURVE()
GEOMETRIC_REPRESENTATION_ITEM()
RATIONAL_B_SPLINE_CURVE((1.00144169675219,1.00138583461176,1.))
REPRESENTATION_ITEM('')
);
#486=(
BOUNDED_CURVE()
B_SPLINE_CURVE(2,(#113631,#113632,#113633),.UNSPECIFIED.,.F.,.F.)
B_SPLINE_CURVE_WITH_KNOTS((3,3),(0.,0.0209957934101768),.UNSPECIFIED.)
CURVE()
GEOMETRIC_REPRESENTATION_ITEM()
RATIONAL_B_SPLINE_CURVE((1.,1.00138583461562,1.0014416967562))
REPRESENTATION_ITEM('')
);
#487=(
BOUNDED_CURVE()
B_SPLINE_CURVE(2,(#113636,#113637,#113638),.UNSPECIFIED.,.F.,.F.)
B_SPLINE_CURVE_WITH_KNOTS((3,3),(0.0227595441419788,0.0437553375522102),
 .UNSPECIFIED.)
CURVE()
GEOMETRIC_REPRESENTATION_ITEM()
RATIONAL_B_SPLINE_CURVE((1.00144169675083,1.00138583461046,1.))
REPRESENTATION_ITEM('')
);
#488=(
BOUNDED_CURVE()
B_SPLINE_CURVE(2,(#113645,#113646,#113647),.UNSPECIFIED.,.F.,.F.)
B_SPLINE_CURVE_WITH_KNOTS((3,3),(0.,0.0209957934101946),.UNSPECIFIED.)
CURVE()
GEOMETRIC_REPRESENTATION_ITEM()
RATIONAL_B_SPLINE_CURVE((1.,1.00138583461436,1.00144169675489))
REPRESENTATION_ITEM('')
);
#489=(
BOUNDED_CURVE()
B_SPLINE_CURVE(2,(#113650,#113651,#113652),.UNSPECIFIED.,.F.,.F.)
B_SPLINE_CURVE_WITH_KNOTS((3,3),(0.0227595441420032,0.04375533755221),
 .UNSPECIFIED.)
CURVE()
GEOMETRIC_REPRESENTATION_ITEM()
RATIONAL_B_SPLINE_CURVE((1.00144169675912,1.00138583461843,1.))
REPRESENTATION_ITEM('')
);
#490=(
BOUNDED_CURVE()
B_SPLINE_CURVE(2,(#113659,#113660,#113661),.UNSPECIFIED.,.F.,.F.)
B_SPLINE_CURVE_WITH_KNOTS((3,3),(0.,0.0209957934101575),.UNSPECIFIED.)
CURVE()
GEOMETRIC_REPRESENTATION_ITEM()
RATIONAL_B_SPLINE_CURVE((1.,1.00138583461801,1.00144169675869))
REPRESENTATION_ITEM('')
);
#491=(
BOUNDED_CURVE()
B_SPLINE_CURVE(2,(#113664,#113665,#113666),.UNSPECIFIED.,.F.,.F.)
B_SPLINE_CURVE_WITH_KNOTS((3,3),(0.0227595441420447,0.04375533755221),
 .UNSPECIFIED.)
CURVE()
GEOMETRIC_REPRESENTATION_ITEM()
RATIONAL_B_SPLINE_CURVE((1.00144169676208,1.00138583462127,1.))
REPRESENTATION_ITEM('')
);
#492=(
BOUNDED_CURVE()
B_SPLINE_CURVE(2,(#113673,#113674,#113675),.UNSPECIFIED.,.F.,.F.)
B_SPLINE_CURVE_WITH_KNOTS((3,3),(0.,0.0209957934102153),.UNSPECIFIED.)
CURVE()
GEOMETRIC_REPRESENTATION_ITEM()
RATIONAL_B_SPLINE_CURVE((1.,1.00138583461588,1.00144169675647))
REPRESENTATION_ITEM('')
);
#493=(
BOUNDED_CURVE()
B_SPLINE_CURVE(2,(#113678,#113679,#113680),.UNSPECIFIED.,.F.,.F.)
B_SPLINE_CURVE_WITH_KNOTS((3,3),(0.0227595441420092,0.04375533755221),
 .UNSPECIFIED.)
CURVE()
GEOMETRIC_REPRESENTATION_ITEM()
RATIONAL_B_SPLINE_CURVE((1.00144169675677,1.00138583461617,1.))
REPRESENTATION_ITEM('')
);
#494=(
BOUNDED_CURVE()
B_SPLINE_CURVE(2,(#113687,#113688,#113689),.UNSPECIFIED.,.F.,.F.)
B_SPLINE_CURVE_WITH_KNOTS((3,3),(0.,0.0209957934101552),.UNSPECIFIED.)
CURVE()
GEOMETRIC_REPRESENTATION_ITEM()
RATIONAL_B_SPLINE_CURVE((1.,1.00138583461929,1.00144169676002))
REPRESENTATION_ITEM('')
);
#495=(
BOUNDED_CURVE()
B_SPLINE_CURVE(2,(#113692,#113693,#113694),.UNSPECIFIED.,.F.,.F.)
B_SPLINE_CURVE_WITH_KNOTS((3,3),(0.0227595441419908,0.0437553375522098),
 .UNSPECIFIED.)
CURVE()
GEOMETRIC_REPRESENTATION_ITEM()
RATIONAL_B_SPLINE_CURVE((1.00144169675614,1.00138583461556,1.))
REPRESENTATION_ITEM('')
);
#496=(
BOUNDED_CURVE()
B_SPLINE_CURVE(2,(#113701,#113702,#113703),.UNSPECIFIED.,.F.,.F.)
B_SPLINE_CURVE_WITH_KNOTS((3,3),(0.,0.0209957934101925),.UNSPECIFIED.)
CURVE()
GEOMETRIC_REPRESENTATION_ITEM()
RATIONAL_B_SPLINE_CURVE((1.,1.00138583461381,1.00144169675432))
REPRESENTATION_ITEM('')
);
#497=(
BOUNDED_CURVE()
B_SPLINE_CURVE(2,(#113706,#113707,#113708),.UNSPECIFIED.,.F.,.F.)
B_SPLINE_CURVE_WITH_KNOTS((3,3),(0.0227595441420215,0.0437553375522099),
 .UNSPECIFIED.)
CURVE()
GEOMETRIC_REPRESENTATION_ITEM()
RATIONAL_B_SPLINE_CURVE((1.00144169675677,1.00138583461617,1.))
REPRESENTATION_ITEM('')
);
#498=(
BOUNDED_CURVE()
B_SPLINE_CURVE(2,(#113715,#113716,#113717),.UNSPECIFIED.,.F.,.F.)
B_SPLINE_CURVE_WITH_KNOTS((3,3),(0.,0.0209957934101895),.UNSPECIFIED.)
CURVE()
GEOMETRIC_REPRESENTATION_ITEM()
RATIONAL_B_SPLINE_CURVE((1.,1.00138583461732,1.00144169675797))
REPRESENTATION_ITEM('')
);
#499=(
BOUNDED_CURVE()
B_SPLINE_CURVE(2,(#113720,#113721,#113722),.UNSPECIFIED.,.F.,.F.)
B_SPLINE_CURVE_WITH_KNOTS((3,3),(0.0227595441420421,0.0437553375522098),
 .UNSPECIFIED.)
CURVE()
GEOMETRIC_REPRESENTATION_ITEM()
RATIONAL_B_SPLINE_CURVE((1.00144169675667,1.00138583461607,1.))
REPRESENTATION_ITEM('')
);
#500=(
BOUNDED_CURVE()
B_SPLINE_CURVE(2,(#113729,#113730,#113731),.UNSPECIFIED.,.F.,.F.)
B_SPLINE_CURVE_WITH_KNOTS((3,3),(0.,0.020995793410204),.UNSPECIFIED.)
CURVE()
GEOMETRIC_REPRESENTATION_ITEM()
RATIONAL_B_SPLINE_CURVE((1.,1.00138583461502,1.00144169675558))
REPRESENTATION_ITEM('')
);
#501=(
BOUNDED_CURVE()
B_SPLINE_CURVE(2,(#113734,#113735,#113736),.UNSPECIFIED.,.F.,.F.)
B_SPLINE_CURVE_WITH_KNOTS((3,3),(0.0227595441420457,0.0437553375522097),
 .UNSPECIFIED.)
CURVE()
GEOMETRIC_REPRESENTATION_ITEM()
RATIONAL_B_SPLINE_CURVE((1.00144169675951,1.0013858346188,1.))
REPRESENTATION_ITEM('')
);
#502=(
BOUNDED_CURVE()
B_SPLINE_CURVE(2,(#113743,#113744,#113745),.UNSPECIFIED.,.F.,.F.)
B_SPLINE_CURVE_WITH_KNOTS((3,3),(0.,0.020995793410164),.UNSPECIFIED.)
CURVE()
GEOMETRIC_REPRESENTATION_ITEM()
RATIONAL_B_SPLINE_CURVE((1.,1.0013858346188,1.00144169675951))
REPRESENTATION_ITEM('')
);
#503=(
BOUNDED_CURVE()
B_SPLINE_CURVE(2,(#113759,#113760,#113761),.UNSPECIFIED.,.F.,.F.)
B_SPLINE_CURVE_WITH_KNOTS((3,3),(0.,0.0129989367050987),.UNSPECIFIED.)
CURVE()
GEOMETRIC_REPRESENTATION_ITEM()
RATIONAL_B_SPLINE_CURVE((1.,1.00368858134443,1.0050923555823))
REPRESENTATION_ITEM('')
);
#504=(
BOUNDED_CURVE()
B_SPLINE_CURVE(2,(#113765,#113766,#113767),.UNSPECIFIED.,.F.,.F.)
B_SPLINE_CURVE_WITH_KNOTS((3,3),(0.0289719021373686,0.041970838842468),
 .UNSPECIFIED.)
CURVE()
GEOMETRIC_REPRESENTATION_ITEM()
RATIONAL_B_SPLINE_CURVE((1.00509235558236,1.00368858134447,1.))
REPRESENTATION_ITEM('')
);
#505=(
BOUNDED_CURVE()
B_SPLINE_CURVE(2,(#113769,#113770,#113771),.UNSPECIFIED.,.F.,.F.)
B_SPLINE_CURVE_WITH_KNOTS((3,3),(0.,0.012998936705099),.UNSPECIFIED.)
CURVE()
GEOMETRIC_REPRESENTATION_ITEM()
RATIONAL_B_SPLINE_CURVE((1.,1.0036885813445,1.0050923555824))
REPRESENTATION_ITEM('')
);
#506=(
BOUNDED_CURVE()
B_SPLINE_CURVE(2,(#113775,#113776,#113777),.UNSPECIFIED.,.F.,.F.)
B_SPLINE_CURVE_WITH_KNOTS((3,3),(0.0289719021373694,0.0419708388424683),
 .UNSPECIFIED.)
CURVE()
GEOMETRIC_REPRESENTATION_ITEM()
RATIONAL_B_SPLINE_CURVE((1.0050923555824,1.0036885813445,1.))
REPRESENTATION_ITEM('')
);
#507=(
BOUNDED_CURVE()
B_SPLINE_CURVE(2,(#113779,#113780,#113781),.UNSPECIFIED.,.F.,.F.)
B_SPLINE_CURVE_WITH_KNOTS((3,3),(0.,0.0129989367050987),.UNSPECIFIED.)
CURVE()
GEOMETRIC_REPRESENTATION_ITEM()
RATIONAL_B_SPLINE_CURVE((1.,1.00368858134463,1.00509235558257))
REPRESENTATION_ITEM('')
);
#508=(
BOUNDED_CURVE()
B_SPLINE_CURVE(2,(#113785,#113786,#113787),.UNSPECIFIED.,.F.,.F.)
B_SPLINE_CURVE_WITH_KNOTS((3,3),(0.0289719021373689,0.0419708388424683),
 .UNSPECIFIED.)
CURVE()
GEOMETRIC_REPRESENTATION_ITEM()
RATIONAL_B_SPLINE_CURVE((1.00509235558232,1.00368858134444,1.))
REPRESENTATION_ITEM('')
);
#509=(
BOUNDED_CURVE()
B_SPLINE_CURVE(2,(#113789,#113790,#113791),.UNSPECIFIED.,.F.,.F.)
B_SPLINE_CURVE_WITH_KNOTS((3,3),(0.,0.0129989367050993),.UNSPECIFIED.)
CURVE()
GEOMETRIC_REPRESENTATION_ITEM()
RATIONAL_B_SPLINE_CURVE((1.,1.0036885813444,1.00509235558225))
REPRESENTATION_ITEM('')
);
#510=(
BOUNDED_CURVE()
B_SPLINE_CURVE(2,(#113795,#113796,#113797),.UNSPECIFIED.,.F.,.F.)
B_SPLINE_CURVE_WITH_KNOTS((3,3),(0.0289719021373687,0.041970838842468),
 .UNSPECIFIED.)
CURVE()
GEOMETRIC_REPRESENTATION_ITEM()
RATIONAL_B_SPLINE_CURVE((1.00509235558236,1.00368858134447,1.))
REPRESENTATION_ITEM('')
);
#511=(
BOUNDED_CURVE()
B_SPLINE_CURVE(2,(#113799,#113800,#113801),.UNSPECIFIED.,.F.,.F.)
B_SPLINE_CURVE_WITH_KNOTS((3,3),(0.,0.0129989367050989),.UNSPECIFIED.)
CURVE()
GEOMETRIC_REPRESENTATION_ITEM()
RATIONAL_B_SPLINE_CURVE((1.,1.0036885813445,1.0050923555824))
REPRESENTATION_ITEM('')
);
#512=(
BOUNDED_CURVE()
B_SPLINE_CURVE(2,(#113805,#113806,#113807),.UNSPECIFIED.,.F.,.F.)
B_SPLINE_CURVE_WITH_KNOTS((3,3),(0.0289719021373694,0.0419708388424683),
 .UNSPECIFIED.)
CURVE()
GEOMETRIC_REPRESENTATION_ITEM()
RATIONAL_B_SPLINE_CURVE((1.0050923555824,1.0036885813445,1.))
REPRESENTATION_ITEM('')
);
#513=(
BOUNDED_CURVE()
B_SPLINE_CURVE(2,(#113809,#113810,#113811),.UNSPECIFIED.,.F.,.F.)
B_SPLINE_CURVE_WITH_KNOTS((3,3),(0.,0.0129989367050992),.UNSPECIFIED.)
CURVE()
GEOMETRIC_REPRESENTATION_ITEM()
RATIONAL_B_SPLINE_CURVE((1.,1.00368858134448,1.00509235558236))
REPRESENTATION_ITEM('')
);
#514=(
BOUNDED_CURVE()
B_SPLINE_CURVE(2,(#113814,#113815,#113816),.UNSPECIFIED.,.F.,.F.)
B_SPLINE_CURVE_WITH_KNOTS((3,3),(0.0289719021373676,0.0419708388424684),
 .UNSPECIFIED.)
CURVE()
GEOMETRIC_REPRESENTATION_ITEM()
RATIONAL_B_SPLINE_CURVE((1.00509235558214,1.00368858134432,1.))
REPRESENTATION_ITEM('')
);
#531=SHAPE_REPRESENTATION_RELATIONSHIP('SRR','None',#114068,#549);
#549=ADVANCED_BREP_SHAPE_REPRESENTATION('',(#585),#113982);
#567=STYLED_ITEM('',(#114317),#585);
#585=MANIFOLD_SOLID_BREP('ISO 4762 - M2.5 x 6 - 12.9 (Rack Screw)',#60408);
#840=CYLINDRICAL_SURFACE('',#63463,1.215);
#841=CYLINDRICAL_SURFACE('',#63465,1.215);
#842=CYLINDRICAL_SURFACE('',#63466,1.215);
#843=CYLINDRICAL_SURFACE('',#63467,1.215);
#844=CYLINDRICAL_SURFACE('',#63468,1.215);
#845=CYLINDRICAL_SURFACE('',#63469,1.215);
#846=CYLINDRICAL_SURFACE('',#63470,1.215);
#847=CYLINDRICAL_SURFACE('',#63471,1.215);
#848=CYLINDRICAL_SURFACE('',#63472,1.215);
#849=CYLINDRICAL_SURFACE('',#63473,1.215);
#850=CYLINDRICAL_SURFACE('',#63474,1.215);
#851=CYLINDRICAL_SURFACE('',#63475,1.215);
#852=CYLINDRICAL_SURFACE('',#63476,1.215);
#853=CYLINDRICAL_SURFACE('',#63477,0.958249999999999);
#854=CYLINDRICAL_SURFACE('',#63479,0.958249999999999);
#855=CYLINDRICAL_SURFACE('',#63480,0.958249999999999);
#856=CYLINDRICAL_SURFACE('',#63481,0.958249999999999);
#857=CYLINDRICAL_SURFACE('',#63482,0.958249999999999);
#858=CYLINDRICAL_SURFACE('',#63483,0.958249999999999);
#859=CYLINDRICAL_SURFACE('',#63484,0.958249999999999);
#860=CYLINDRICAL_SURFACE('',#63485,0.958249999999999);
#861=CYLINDRICAL_SURFACE('',#63486,0.958249999999999);
#862=CYLINDRICAL_SURFACE('',#63487,0.958249999999999);
#863=CYLINDRICAL_SURFACE('',#63488,0.958249999999999);
#864=CYLINDRICAL_SURFACE('',#63489,0.958249999999999);
#865=CYLINDRICAL_SURFACE('',#63497,0.958249999999999);
#866=CYLINDRICAL_SURFACE('',#63501,1.215);
#867=CYLINDRICAL_SURFACE('',#63512,2.25);
#868=CYLINDRICAL_SURFACE('',#63705,1.10470053837925);
#869=CYLINDRICAL_SURFACE('',#63707,1.10470053837925);
#870=CYLINDRICAL_SURFACE('',#63709,1.10470053837925);
#871=CYLINDRICAL_SURFACE('',#63711,1.10470053837925);
#872=CYLINDRICAL_SURFACE('',#63713,1.10470053837925);
#873=CYLINDRICAL_SURFACE('',#63715,1.10470053837925);
#951=CONICAL_SURFACE('',#63505,1.04,0.785398163397448);
#952=CONICAL_SURFACE('',#63694,2.1,0.785398163397448);
#953=CONICAL_SURFACE('',#63698,1.20470053837925,0.785398163397454);
#954=CONICAL_SURFACE('',#63738,1.15470053837925,1.02974425867666);
#1430=CIRCLE('',#63464,1.215);
#1431=CIRCLE('',#63478,0.958249999999999);
#1432=CIRCLE('',#63491,1.215);
#1433=CIRCLE('',#63492,1.215);
#1434=CIRCLE('',#63494,1.215);
#1435=CIRCLE('',#63495,0.958249999999999);
#1436=CIRCLE('',#63496,1.215);
#1437=CIRCLE('',#63499,0.1);
#1438=CIRCLE('',#63500,1.315);
#1439=CIRCLE('',#63502,1.215);
#1440=CIRCLE('',#63504,2.05);
#1441=CIRCLE('',#63506,0.865);
#1442=CIRCLE('',#63510,2.25);
#1443=CIRCLE('',#63513,2.25);
#1444=CIRCLE('',#63514,2.25);
#1445=CIRCLE('',#63515,2.25);
#1446=CIRCLE('',#63516,2.25);
#1447=CIRCLE('',#63517,2.25);
#1448=CIRCLE('',#63518,2.25);
#1449=CIRCLE('',#63519,2.25);
#1450=CIRCLE('',#63520,2.25);
#1451=CIRCLE('',#63521,2.25);
#1452=CIRCLE('',#63522,2.25);
#1453=CIRCLE('',#63523,2.25);
#1454=CIRCLE('',#63524,2.25);
#1455=CIRCLE('',#63525,2.25);
#1456=CIRCLE('',#63526,2.25);
#1457=CIRCLE('',#63527,2.25);
#1458=CIRCLE('',#63528,2.25);
#1459=CIRCLE('',#63529,2.25);
#1460=CIRCLE('',#63530,2.25);
#1461=CIRCLE('',#63531,2.25);
#1462=CIRCLE('',#63532,2.25);
#1463=CIRCLE('',#63533,2.25);
#1464=CIRCLE('',#63534,2.25);
#1465=CIRCLE('',#63535,2.25);
#1466=CIRCLE('',#63536,2.25);
#1467=CIRCLE('',#63537,2.25);
#1468=CIRCLE('',#63538,2.25);
#1469=CIRCLE('',#63539,2.25);
#1470=CIRCLE('',#63540,2.25);
#1471=CIRCLE('',#63541,2.25);
#1472=CIRCLE('',#63542,2.25);
#1473=CIRCLE('',#63543,2.25);
#1474=CIRCLE('',#63544,2.25);
#1475=CIRCLE('',#63545,2.25);
#1476=CIRCLE('',#63546,2.25);
#1477=CIRCLE('',#63547,2.25);
#1478=CIRCLE('',#63548,2.25);
#1479=CIRCLE('',#63549,2.25);
#1480=CIRCLE('',#63550,2.25);
#1481=CIRCLE('',#63551,2.25);
#1482=CIRCLE('',#63552,2.25);
#1483=CIRCLE('',#63553,2.25);
#1484=CIRCLE('',#63554,2.25);
#1485=CIRCLE('',#63555,2.25);
#1486=CIRCLE('',#63556,2.25);
#1487=CIRCLE('',#63557,2.25);
#1488=CIRCLE('',#63558,2.25);
#1489=CIRCLE('',#63559,2.25);
#1490=CIRCLE('',#63560,2.25);
#1491=CIRCLE('',#63561,2.25);
#1492=CIRCLE('',#63562,2.25);
#1493=CIRCLE('',#63563,2.25);
#1494=CIRCLE('',#63564,2.25);
#1495=CIRCLE('',#63565,2.25);
#1496=CIRCLE('',#63566,2.25);
#1497=CIRCLE('',#63567,2.25);
#1498=CIRCLE('',#63568,2.25);
#1499=CIRCLE('',#63569,2.25);
#1500=CIRCLE('',#63570,2.25);
#1501=CIRCLE('',#63571,2.25);
#1502=CIRCLE('',#63572,2.25);
#1503=CIRCLE('',#63573,2.25);
#1504=CIRCLE('',#63574,2.25);
#1505=CIRCLE('',#63575,2.25);
#1506=CIRCLE('',#63576,2.25);
#1507=CIRCLE('',#63577,2.25);
#1508=CIRCLE('',#63578,2.25);
#1509=CIRCLE('',#63579,2.25);
#1510=CIRCLE('',#63580,2.25);
#1511=CIRCLE('',#63581,2.25);
#1512=CIRCLE('',#63582,2.25);
#1513=CIRCLE('',#63583,2.25);
#1514=CIRCLE('',#63584,2.25);
#1515=CIRCLE('',#63585,2.25);
#1516=CIRCLE('',#63586,2.25);
#1517=CIRCLE('',#63693,0.2);
#1518=CIRCLE('',#63695,1.95);
#1519=CIRCLE('',#63697,1.30470053837925);
#1520=CIRCLE('',#63699,1.10470053837925);
#1521=CIRCLE('',#63700,1.10470053837925);
#1522=CIRCLE('',#63701,1.10470053837925);
#1523=CIRCLE('',#63702,1.10470053837925);
#1524=CIRCLE('',#63703,1.10470053837925);
#1525=CIRCLE('',#63704,1.10470053837925);
#1526=CIRCLE('',#63706,1.10470053837925);
#1527=CIRCLE('',#63708,1.10470053837925);
#1528=CIRCLE('',#63710,1.10470053837925);
#1529=CIRCLE('',#63712,1.10470053837925);
#1530=CIRCLE('',#63714,1.10470053837925);
#1531=CIRCLE('',#63716,1.10470053837925);
#1532=CIRCLE('',#63727,1.15470053837925);
#1533=CIRCLE('',#63729,1.15470053837925);
#1534=CIRCLE('',#63731,1.15470053837925);
#1535=CIRCLE('',#63733,1.15470053837925);
#1536=CIRCLE('',#63735,1.15470053837925);
#1537=CIRCLE('',#63737,1.15470053837925);
#1857=FACE_BOUND('',#10729,.T.);
#1858=FACE_BOUND('',#10844,.T.);
#3892=PLANE('',#63490);
#3893=PLANE('',#63493);
#3894=PLANE('',#63503);
#3895=PLANE('',#63507);
#3896=PLANE('',#63508);
#3897=PLANE('',#63509);
#3898=PLANE('',#63511);
#3899=PLANE('',#63587);
#3900=PLANE('',#63588);
#3901=PLANE('',#63589);
#3902=PLANE('',#63590);
#3903=PLANE('',#63591);
#3904=PLANE('',#63592);
#3905=PLANE('',#63593);
#3906=PLANE('',#63594);
#3907=PLANE('',#63595);
#3908=PLANE('',#63596);
#3909=PLANE('',#63597);
#3910=PLANE('',#63598);
#3911=PLANE('',#63599);
#3912=PLANE('',#63600);
#3913=PLANE('',#63601);
#3914=PLANE('',#63602);
#3915=PLANE('',#63603);
#3916=PLANE('',#63604);
#3917=PLANE('',#63605);
#3918=PLANE('',#63606);
#3919=PLANE('',#63607);
#3920=PLANE('',#63608);
#3921=PLANE('',#63609);
#3922=PLANE('',#63610);
#3923=PLANE('',#63611);
#3924=PLANE('',#63612);
#3925=PLANE('',#63613);
#3926=PLANE('',#63614);
#3927=PLANE('',#63615);
#3928=PLANE('',#63616);
#3929=PLANE('',#63617);
#3930=PLANE('',#63618);
#3931=PLANE('',#63619);
#3932=PLANE('',#63620);
#3933=PLANE('',#63621);
#3934=PLANE('',#63622);
#3935=PLANE('',#63623);
#3936=PLANE('',#63624);
#3937=PLANE('',#63625);
#3938=PLANE('',#63626);
#3939=PLANE('',#63627);
#3940=PLANE('',#63628);
#3941=PLANE('',#63629);
#3942=PLANE('',#63630);
#3943=PLANE('',#63631);
#3944=PLANE('',#63632);
#3945=PLANE('',#63633);
#3946=PLANE('',#63634);
#3947=PLANE('',#63635);
#3948=PLANE('',#63636);
#3949=PLANE('',#63637);
#3950=PLANE('',#63638);
#3951=PLANE('',#63639);
#3952=PLANE('',#63640);
#3953=PLANE('',#63641);
#3954=PLANE('',#63642);
#3955=PLANE('',#63643);
#3956=PLANE('',#63644);
#3957=PLANE('',#63645);
#3958=PLANE('',#63646);
#3959=PLANE('',#63647);
#3960=PLANE('',#63648);
#3961=PLANE('',#63649);
#3962=PLANE('',#63650);
#3963=PLANE('',#63651);
#3964=PLANE('',#63652);
#3965=PLANE('',#63653);
#3966=PLANE('',#63654);
#3967=PLANE('',#63655);
#3968=PLANE('',#63656);
#3969=PLANE('',#63657);
#3970=PLANE('',#63658);
#3971=PLANE('',#63659);
#3972=PLANE('',#63660);
#3973=PLANE('',#63661);
#3974=PLANE('',#63662);
#3975=PLANE('',#63663);
#3976=PLANE('',#63664);
#3977=PLANE('',#63665);
#3978=PLANE('',#63666);
#3979=PLANE('',#63667);
#3980=PLANE('',#63668);
#3981=PLANE('',#63669);
#3982=PLANE('',#63670);
#3983=PLANE('',#63671);
#3984=PLANE('',#63672);
#3985=PLANE('',#63673);
#3986=PLANE('',#63674);
#3987=PLANE('',#63675);
#3988=PLANE('',#63676);
#3989=PLANE('',#63677);
#3990=PLANE('',#63678);
#3991=PLANE('',#63679);
#3992=PLANE('',#63680);
#3993=PLANE('',#63681);
#3994=PLANE('',#63682);
#3995=PLANE('',#63683);
#3996=PLANE('',#63684);
#3997=PLANE('',#63685);
#3998=PLANE('',#63686);
#3999=PLANE('',#63687);
#4000=PLANE('',#63688);
#4001=PLANE('',#63689);
#4002=PLANE('',#63690);
#4003=PLANE('',#63691);
#4004=PLANE('',#63696);
#4005=PLANE('',#63717);
#4006=PLANE('',#63718);
#4007=PLANE('',#63719);
#4008=PLANE('',#63720);
#4009=PLANE('',#63721);
#4010=PLANE('',#63722);
#4011=PLANE('',#63723);
#4012=PLANE('',#63724);
#4013=PLANE('',#63725);
#4014=PLANE('',#63726);
#4015=PLANE('',#63728);
#4016=PLANE('',#63730);
#4017=PLANE('',#63732);
#4018=PLANE('',#63734);
#4019=PLANE('',#63736);
#4020=PLANE('',#63739);
#4021=PLANE('',#63740);
#4022=PLANE('',#63741);
#7114=FACE_OUTER_BOUND('',#10696,.T.);
#7115=FACE_OUTER_BOUND('',#10697,.T.);
#7116=FACE_OUTER_BOUND('',#10698,.T.);
#7117=FACE_OUTER_BOUND('',#10699,.T.);
#7118=FACE_OUTER_BOUND('',#10700,.T.);
#7119=FACE_OUTER_BOUND('',#10701,.T.);
#7120=FACE_OUTER_BOUND('',#10702,.T.);
#7121=FACE_OUTER_BOUND('',#10703,.T.);
#7122=FACE_OUTER_BOUND('',#10704,.T.);
#7123=FACE_OUTER_BOUND('',#10705,.T.);
#7124=FACE_OUTER_BOUND('',#10706,.T.);
#7125=FACE_OUTER_BOUND('',#10707,.T.);
#7126=FACE_OUTER_BOUND('',#10708,.T.);
#7127=FACE_OUTER_BOUND('',#10709,.T.);
#7128=FACE_OUTER_BOUND('',#10710,.T.);
#7129=FACE_OUTER_BOUND('',#10711,.T.);
#7130=FACE_OUTER_BOUND('',#10712,.T.);
#7131=FACE_OUTER_BOUND('',#10713,.T.);
#7132=FACE_OUTER_BOUND('',#10714,.T.);
#7133=FACE_OUTER_BOUND('',#10715,.T.);
#7134=FACE_OUTER_BOUND('',#10716,.T.);
#7135=FACE_OUTER_BOUND('',#10717,.T.);
#7136=FACE_OUTER_BOUND('',#10718,.T.);
#7137=FACE_OUTER_BOUND('',#10719,.T.);
#7138=FACE_OUTER_BOUND('',#10720,.T.);
#7139=FACE_OUTER_BOUND('',#10721,.T.);
#7140=FACE_OUTER_BOUND('',#10722,.T.);
#7141=FACE_OUTER_BOUND('',#10723,.T.);
#7142=FACE_OUTER_BOUND('',#10724,.T.);
#7143=FACE_OUTER_BOUND('',#10725,.T.);
#7144=FACE_OUTER_BOUND('',#10726,.T.);
#7145=FACE_OUTER_BOUND('',#10727,.T.);
#7146=FACE_OUTER_BOUND('',#10728,.T.);
#7147=FACE_OUTER_BOUND('',#10730,.T.);
#7148=FACE_OUTER_BOUND('',#10731,.T.);
#7149=FACE_OUTER_BOUND('',#10732,.T.);
#7150=FACE_OUTER_BOUND('',#10733,.T.);
#7151=FACE_OUTER_BOUND('',#10734,.T.);
#7152=FACE_OUTER_BOUND('',#10735,.T.);
#7153=FACE_OUTER_BOUND('',#10736,.T.);
#7154=FACE_OUTER_BOUND('',#10737,.T.);
#7155=FACE_OUTER_BOUND('',#10738,.T.);
#7156=FACE_OUTER_BOUND('',#10739,.T.);
#7157=FACE_OUTER_BOUND('',#10740,.T.);
#7158=FACE_OUTER_BOUND('',#10741,.T.);
#7159=FACE_OUTER_BOUND('',#10742,.T.);
#7160=FACE_OUTER_BOUND('',#10743,.T.);
#7161=FACE_OUTER_BOUND('',#10744,.T.);
#7162=FACE_OUTER_BOUND('',#10745,.T.);
#7163=FACE_OUTER_BOUND('',#10746,.T.);
#7164=FACE_OUTER_BOUND('',#10747,.T.);
#7165=FACE_OUTER_BOUND('',#10748,.T.);
#7166=FACE_OUTER_BOUND('',#10749,.T.);
#7167=FACE_OUTER_BOUND('',#10750,.T.);
#7168=FACE_OUTER_BOUND('',#10751,.T.);
#7169=FACE_OUTER_BOUND('',#10752,.T.);
#7170=FACE_OUTER_BOUND('',#10753,.T.);
#7171=FACE_OUTER_BOUND('',#10754,.T.);
#7172=FACE_OUTER_BOUND('',#10755,.T.);
#7173=FACE_OUTER_BOUND('',#10756,.T.);
#7174=FACE_OUTER_BOUND('',#10757,.T.);
#7175=FACE_OUTER_BOUND('',#10758,.T.);
#7176=FACE_OUTER_BOUND('',#10759,.T.);
#7177=FACE_OUTER_BOUND('',#10760,.T.);
#7178=FACE_OUTER_BOUND('',#10761,.T.);
#7179=FACE_OUTER_BOUND('',#10762,.T.);
#7180=FACE_OUTER_BOUND('',#10763,.T.);
#7181=FACE_OUTER_BOUND('',#10764,.T.);
#7182=FACE_OUTER_BOUND('',#10765,.T.);
#7183=FACE_OUTER_BOUND('',#10766,.T.);
#7184=FACE_OUTER_BOUND('',#10767,.T.);
#7185=FACE_OUTER_BOUND('',#10768,.T.);
#7186=FACE_OUTER_BOUND('',#10769,.T.);
#7187=FACE_OUTER_BOUND('',#10770,.T.);
#7188=FACE_OUTER_BOUND('',#10771,.T.);
#7189=FACE_OUTER_BOUND('',#10772,.T.);
#7190=FACE_OUTER_BOUND('',#10773,.T.);
#7191=FACE_OUTER_BOUND('',#10774,.T.);
#7192=FACE_OUTER_BOUND('',#10775,.T.);
#7193=FACE_OUTER_BOUND('',#10776,.T.);
#7194=FACE_OUTER_BOUND('',#10777,.T.);
#7195=FACE_OUTER_BOUND('',#10778,.T.);
#7196=FACE_OUTER_BOUND('',#10779,.T.);
#7197=FACE_OUTER_BOUND('',#10780,.T.);
#7198=FACE_OUTER_BOUND('',#10781,.T.);
#7199=FACE_OUTER_BOUND('',#10782,.T.);
#7200=FACE_OUTER_BOUND('',#10783,.T.);
#7201=FACE_OUTER_BOUND('',#10784,.T.);
#7202=FACE_OUTER_BOUND('',#10785,.T.);
#7203=FACE_OUTER_BOUND('',#10786,.T.);
#7204=FACE_OUTER_BOUND('',#10787,.T.);
#7205=FACE_OUTER_BOUND('',#10788,.T.);
#7206=FACE_OUTER_BOUND('',#10789,.T.);
#7207=FACE_OUTER_BOUND('',#10790,.T.);
#7208=FACE_OUTER_BOUND('',#10791,.T.);
#7209=FACE_OUTER_BOUND('',#10792,.T.);
#7210=FACE_OUTER_BOUND('',#10793,.T.);
#7211=FACE_OUTER_BOUND('',#10794,.T.);
#7212=FACE_OUTER_BOUND('',#10795,.T.);
#7213=FACE_OUTER_BOUND('',#10796,.T.);
#7214=FACE_OUTER_BOUND('',#10797,.T.);
#7215=FACE_OUTER_BOUND('',#10798,.T.);
#7216=FACE_OUTER_BOUND('',#10799,.T.);
#7217=FACE_OUTER_BOUND('',#10800,.T.);
#7218=FACE_OUTER_BOUND('',#10801,.T.);
#7219=FACE_OUTER_BOUND('',#10802,.T.);
#7220=FACE_OUTER_BOUND('',#10803,.T.);
#7221=FACE_OUTER_BOUND('',#10804,.T.);
#7222=FACE_OUTER_BOUND('',#10805,.T.);
#7223=FACE_OUTER_BOUND('',#10806,.T.);
#7224=FACE_OUTER_BOUND('',#10807,.T.);
#7225=FACE_OUTER_BOUND('',#10808,.T.);
#7226=FACE_OUTER_BOUND('',#10809,.T.);
#7227=FACE_OUTER_BOUND('',#10810,.T.);
#7228=FACE_OUTER_BOUND('',#10811,.T.);
#7229=FACE_OUTER_BOUND('',#10812,.T.);
#7230=FACE_OUTER_BOUND('',#10813,.T.);
#7231=FACE_OUTER_BOUND('',#10814,.T.);
#7232=FACE_OUTER_BOUND('',#10815,.T.);
#7233=FACE_OUTER_BOUND('',#10816,.T.);
#7234=FACE_OUTER_BOUND('',#10817,.T.);
#7235=FACE_OUTER_BOUND('',#10818,.T.);
#7236=FACE_OUTER_BOUND('',#10819,.T.);
#7237=FACE_OUTER_BOUND('',#10820,.T.);
#7238=FACE_OUTER_BOUND('',#10821,.T.);
#7239=FACE_OUTER_BOUND('',#10822,.T.);
#7240=FACE_OUTER_BOUND('',#10823,.T.);
#7241=FACE_OUTER_BOUND('',#10824,.T.);
#7242=FACE_OUTER_BOUND('',#10825,.T.);
#7243=FACE_OUTER_BOUND('',#10826,.T.);
#7244=FACE_OUTER_BOUND('',#10827,.T.);
#7245=FACE_OUTER_BOUND('',#10828,.T.);
#7246=FACE_OUTER_BOUND('',#10829,.T.);
#7247=FACE_OUTER_BOUND('',#10830,.T.);
#7248=FACE_OUTER_BOUND('',#10831,.T.);
#7249=FACE_OUTER_BOUND('',#10832,.T.);
#7250=FACE_OUTER_BOUND('',#10833,.T.);
#7251=FACE_OUTER_BOUND('',#10834,.T.);
#7252=FACE_OUTER_BOUND('',#10835,.T.);
#7253=FACE_OUTER_BOUND('',#10836,.T.);
#7254=FACE_OUTER_BOUND('',#10837,.T.);
#7255=FACE_OUTER_BOUND('',#10838,.T.);
#7256=FACE_OUTER_BOUND('',#10839,.T.);
#7257=FACE_OUTER_BOUND('',#10840,.T.);
#7258=FACE_OUTER_BOUND('',#10841,.T.);
#7259=FACE_OUTER_BOUND('',#10842,.T.);
#7260=FACE_OUTER_BOUND('',#10843,.T.);
#7261=FACE_OUTER_BOUND('',#10845,.T.);
#7262=FACE_OUTER_BOUND('',#10846,.T.);
#7263=FACE_OUTER_BOUND('',#10847,.T.);
#7264=FACE_OUTER_BOUND('',#10848,.T.);
#7265=FACE_OUTER_BOUND('',#10849,.T.);
#7266=FACE_OUTER_BOUND('',#10850,.T.);
#7267=FACE_OUTER_BOUND('',#10851,.T.);
#7268=FACE_OUTER_BOUND('',#10852,.T.);
#7269=FACE_OUTER_BOUND('',#10853,.T.);
#7270=FACE_OUTER_BOUND('',#10854,.T.);
#7271=FACE_OUTER_BOUND('',#10855,.T.);
#7272=FACE_OUTER_BOUND('',#10856,.T.);
#7273=FACE_OUTER_BOUND('',#10857,.T.);
#7274=FACE_OUTER_BOUND('',#10858,.T.);
#7275=FACE_OUTER_BOUND('',#10859,.T.);
#7276=FACE_OUTER_BOUND('',#10860,.T.);
#7277=FACE_OUTER_BOUND('',#10861,.T.);
#7278=FACE_OUTER_BOUND('',#10862,.T.);
#7279=FACE_OUTER_BOUND('',#10863,.T.);
#7280=FACE_OUTER_BOUND('',#10864,.T.);
#7281=FACE_OUTER_BOUND('',#10865,.T.);
#7282=FACE_OUTER_BOUND('',#10866,.T.);
#7283=FACE_OUTER_BOUND('',#10867,.T.);
#7284=FACE_OUTER_BOUND('',#10868,.T.);
#7285=FACE_OUTER_BOUND('',#10869,.T.);
#7286=FACE_OUTER_BOUND('',#10870,.T.);
#10696=EDGE_LOOP('',(#55419,#55420,#55421,#55422));
#10697=EDGE_LOOP('',(#55423,#55424,#55425,#55426));
#10698=EDGE_LOOP('',(#55427,#55428,#55429,#55430));
#10699=EDGE_LOOP('',(#55431,#55432,#55433,#55434));
#10700=EDGE_LOOP('',(#55435,#55436,#55437,#55438));
#10701=EDGE_LOOP('',(#55439,#55440,#55441,#55442));
#10702=EDGE_LOOP('',(#55443,#55444,#55445,#55446));
#10703=EDGE_LOOP('',(#55447,#55448,#55449,#55450));
#10704=EDGE_LOOP('',(#55451,#55452,#55453,#55454));
#10705=EDGE_LOOP('',(#55455,#55456,#55457,#55458));
#10706=EDGE_LOOP('',(#55459,#55460,#55461,#55462));
#10707=EDGE_LOOP('',(#55463,#55464,#55465,#55466));
#10708=EDGE_LOOP('',(#55467,#55468,#55469,#55470));
#10709=EDGE_LOOP('',(#55471,#55472,#55473,#55474));
#10710=EDGE_LOOP('',(#55475,#55476,#55477,#55478));
#10711=EDGE_LOOP('',(#55479,#55480,#55481,#55482));
#10712=EDGE_LOOP('',(#55483,#55484,#55485,#55486));
#10713=EDGE_LOOP('',(#55487,#55488,#55489,#55490));
#10714=EDGE_LOOP('',(#55491,#55492,#55493,#55494));
#10715=EDGE_LOOP('',(#55495,#55496,#55497,#55498));
#10716=EDGE_LOOP('',(#55499,#55500,#55501,#55502));
#10717=EDGE_LOOP('',(#55503,#55504,#55505,#55506));
#10718=EDGE_LOOP('',(#55507,#55508,#55509,#55510));
#10719=EDGE_LOOP('',(#55511,#55512,#55513,#55514));
#10720=EDGE_LOOP('',(#55515,#55516,#55517,#55518));
#10721=EDGE_LOOP('',(#55519,#55520,#55521,#55522,#55523));
#10722=EDGE_LOOP('',(#55524,#55525,#55526,#55527,#55528,#55529,#55530,#55531,
#55532,#55533,#55534,#55535,#55536,#55537,#55538,#55539,#55540,#55541,#55542,
#55543,#55544,#55545,#55546,#55547,#55548,#55549,#55550,#55551,#55552));
#10723=EDGE_LOOP('',(#55553,#55554,#55555,#55556,#55557));
#10724=EDGE_LOOP('',(#55558,#55559,#55560,#55561));
#10725=EDGE_LOOP('',(#55562,#55563,#55564,#55565,#55566,#55567,#55568,#55569,
#55570,#55571,#55572,#55573,#55574,#55575,#55576,#55577,#55578,#55579,#55580,
#55581,#55582,#55583,#55584,#55585,#55586,#55587,#55588,#55589,#55590));
#10726=EDGE_LOOP('',(#55591,#55592,#55593,#55594,#55595,#55596));
#10727=EDGE_LOOP('',(#55597,#55598,#55599,#55600));
#10728=EDGE_LOOP('',(#55601));
#10729=EDGE_LOOP('',(#55602));
#10730=EDGE_LOOP('',(#55603,#55604,#55605,#55606,#55607,#55608));
#10731=EDGE_LOOP('',(#55609));
#10732=EDGE_LOOP('',(#55610,#55611,#55612,#55613));
#10733=EDGE_LOOP('',(#55614,#55615,#55616));
#10734=EDGE_LOOP('',(#55617,#55618,#55619,#55620));
#10735=EDGE_LOOP('',(#55621,#55622,#55623,#55624,#55625,#55626,#55627,#55628,
#55629,#55630,#55631,#55632,#55633,#55634,#55635,#55636,#55637,#55638,#55639,
#55640,#55641,#55642,#55643,#55644,#55645,#55646,#55647,#55648,#55649,#55650,
#55651,#55652,#55653,#55654,#55655,#55656,#55657,#55658,#55659,#55660,#55661,
#55662,#55663,#55664,#55665,#55666,#55667,#55668,#55669,#55670,#55671,#55672,
#55673,#55674,#55675,#55676,#55677,#55678,#55679,#55680,#55681,#55682,#55683,
#55684,#55685,#55686,#55687,#55688,#55689,#55690,#55691,#55692,#55693,#55694,
#55695,#55696,#55697,#55698,#55699,#55700,#55701,#55702,#55703,#55704,#55705,
#55706,#55707,#55708,#55709,#55710,#55711,#55712,#55713,#55714,#55715,#55716,
#55717,#55718,#55719,#55720,#55721,#55722,#55723,#55724,#55725,#55726,#55727,
#55728,#55729,#55730,#55731,#55732,#55733,#55734,#55735,#55736,#55737,#55738,
#55739,#55740,#55741,#55742,#55743,#55744,#55745,#55746,#55747,#55748,#55749,
#55750,#55751,#55752,#55753,#55754,#55755,#55756,#55757,#55758,#55759,#55760,
#55761,#55762,#55763,#55764,#55765,#55766,#55767,#55768,#55769));
#10736=EDGE_LOOP('',(#55770,#55771,#55772,#55773));
#10737=EDGE_LOOP('',(#55774,#55775,#55776));
#10738=EDGE_LOOP('',(#55777,#55778,#55779,#55780));
#10739=EDGE_LOOP('',(#55781,#55782,#55783,#55784));
#10740=EDGE_LOOP('',(#55785,#55786,#55787));
#10741=EDGE_LOOP('',(#55788,#55789,#55790,#55791));
#10742=EDGE_LOOP('',(#55792,#55793,#55794,#55795));
#10743=EDGE_LOOP('',(#55796,#55797,#55798));
#10744=EDGE_LOOP('',(#55799,#55800,#55801,#55802));
#10745=EDGE_LOOP('',(#55803,#55804,#55805,#55806));
#10746=EDGE_LOOP('',(#55807,#55808,#55809));
#10747=EDGE_LOOP('',(#55810,#55811,#55812,#55813));
#10748=EDGE_LOOP('',(#55814,#55815,#55816,#55817));
#10749=EDGE_LOOP('',(#55818,#55819,#55820));
#10750=EDGE_LOOP('',(#55821,#55822,#55823,#55824));
#10751=EDGE_LOOP('',(#55825,#55826,#55827,#55828));
#10752=EDGE_LOOP('',(#55829,#55830,#55831));
#10753=EDGE_LOOP('',(#55832,#55833,#55834,#55835));
#10754=EDGE_LOOP('',(#55836,#55837,#55838,#55839));
#10755=EDGE_LOOP('',(#55840,#55841,#55842));
#10756=EDGE_LOOP('',(#55843,#55844,#55845,#55846));
#10757=EDGE_LOOP('',(#55847,#55848,#55849,#55850));
#10758=EDGE_LOOP('',(#55851,#55852,#55853));
#10759=EDGE_LOOP('',(#55854,#55855,#55856,#55857));
#10760=EDGE_LOOP('',(#55858,#55859,#55860,#55861));
#10761=EDGE_LOOP('',(#55862,#55863,#55864));
#10762=EDGE_LOOP('',(#55865,#55866,#55867,#55868));
#10763=EDGE_LOOP('',(#55869,#55870,#55871,#55872));
#10764=EDGE_LOOP('',(#55873,#55874,#55875));
#10765=EDGE_LOOP('',(#55876,#55877,#55878,#55879));
#10766=EDGE_LOOP('',(#55880,#55881,#55882,#55883));
#10767=EDGE_LOOP('',(#55884,#55885,#55886));
#10768=EDGE_LOOP('',(#55887,#55888,#55889,#55890));
#10769=EDGE_LOOP('',(#55891,#55892,#55893,#55894));
#10770=EDGE_LOOP('',(#55895,#55896,#55897));
#10771=EDGE_LOOP('',(#55898,#55899,#55900,#55901));
#10772=EDGE_LOOP('',(#55902,#55903,#55904,#55905));
#10773=EDGE_LOOP('',(#55906,#55907,#55908));
#10774=EDGE_LOOP('',(#55909,#55910,#55911,#55912));
#10775=EDGE_LOOP('',(#55913,#55914,#55915,#55916));
#10776=EDGE_LOOP('',(#55917,#55918,#55919));
#10777=EDGE_LOOP('',(#55920,#55921,#55922,#55923));
#10778=EDGE_LOOP('',(#55924,#55925,#55926,#55927));
#10779=EDGE_LOOP('',(#55928,#55929,#55930));
#10780=EDGE_LOOP('',(#55931,#55932,#55933,#55934));
#10781=EDGE_LOOP('',(#55935,#55936,#55937,#55938));
#10782=EDGE_LOOP('',(#55939,#55940,#55941));
#10783=EDGE_LOOP('',(#55942,#55943,#55944,#55945));
#10784=EDGE_LOOP('',(#55946,#55947,#55948,#55949));
#10785=EDGE_LOOP('',(#55950,#55951,#55952,#55953));
#10786=EDGE_LOOP('',(#55954,#55955,#55956,#55957));
#10787=EDGE_LOOP('',(#55958,#55959,#55960,#55961));
#10788=EDGE_LOOP('',(#55962,#55963,#55964));
#10789=EDGE_LOOP('',(#55965,#55966,#55967,#55968));
#10790=EDGE_LOOP('',(#55969,#55970,#55971,#55972));
#10791=EDGE_LOOP('',(#55973,#55974,#55975));
#10792=EDGE_LOOP('',(#55976,#55977,#55978,#55979));
#10793=EDGE_LOOP('',(#55980,#55981,#55982,#55983));
#10794=EDGE_LOOP('',(#55984,#55985,#55986));
#10795=EDGE_LOOP('',(#55987,#55988,#55989,#55990));
#10796=EDGE_LOOP('',(#55991,#55992,#55993,#55994));
#10797=EDGE_LOOP('',(#55995,#55996,#55997));
#10798=EDGE_LOOP('',(#55998,#55999,#56000,#56001));
#10799=EDGE_LOOP('',(#56002,#56003,#56004,#56005));
#10800=EDGE_LOOP('',(#56006,#56007,#56008));
#10801=EDGE_LOOP('',(#56009,#56010,#56011,#56012));
#10802=EDGE_LOOP('',(#56013,#56014,#56015,#56016));
#10803=EDGE_LOOP('',(#56017,#56018,#56019));
#10804=EDGE_LOOP('',(#56020,#56021,#56022,#56023));
#10805=EDGE_LOOP('',(#56024,#56025,#56026,#56027));
#10806=EDGE_LOOP('',(#56028,#56029,#56030));
#10807=EDGE_LOOP('',(#56031,#56032,#56033,#56034));
#10808=EDGE_LOOP('',(#56035,#56036,#56037,#56038));
#10809=EDGE_LOOP('',(#56039,#56040,#56041));
#10810=EDGE_LOOP('',(#56042,#56043,#56044,#56045));
#10811=EDGE_LOOP('',(#56046,#56047,#56048,#56049));
#10812=EDGE_LOOP('',(#56050,#56051,#56052));
#10813=EDGE_LOOP('',(#56053,#56054,#56055,#56056));
#10814=EDGE_LOOP('',(#56057,#56058,#56059,#56060));
#10815=EDGE_LOOP('',(#56061,#56062,#56063));
#10816=EDGE_LOOP('',(#56064,#56065,#56066,#56067));
#10817=EDGE_LOOP('',(#56068,#56069,#56070,#56071));
#10818=EDGE_LOOP('',(#56072,#56073,#56074));
#10819=EDGE_LOOP('',(#56075,#56076,#56077,#56078));
#10820=EDGE_LOOP('',(#56079,#56080,#56081,#56082));
#10821=EDGE_LOOP('',(#56083,#56084,#56085));
#10822=EDGE_LOOP('',(#56086,#56087,#56088,#56089));
#10823=EDGE_LOOP('',(#56090,#56091,#56092,#56093));
#10824=EDGE_LOOP('',(#56094,#56095,#56096));
#10825=EDGE_LOOP('',(#56097,#56098,#56099,#56100));
#10826=EDGE_LOOP('',(#56101,#56102,#56103,#56104));
#10827=EDGE_LOOP('',(#56105,#56106,#56107));
#10828=EDGE_LOOP('',(#56108,#56109,#56110,#56111));
#10829=EDGE_LOOP('',(#56112,#56113,#56114,#56115));
#10830=EDGE_LOOP('',(#56116,#56117,#56118));
#10831=EDGE_LOOP('',(#56119,#56120,#56121,#56122));
#10832=EDGE_LOOP('',(#56123,#56124,#56125,#56126));
#10833=EDGE_LOOP('',(#56127,#56128,#56129));
#10834=EDGE_LOOP('',(#56130,#56131,#56132,#56133));
#10835=EDGE_LOOP('',(#56134,#56135,#56136,#56137));
#10836=EDGE_LOOP('',(#56138,#56139,#56140));
#10837=EDGE_LOOP('',(#56141,#56142,#56143,#56144));
#10838=EDGE_LOOP('',(#56145,#56146,#56147,#56148));
#10839=EDGE_LOOP('',(#56149,#56150,#56151));
#10840=EDGE_LOOP('',(#56152,#56153,#56154,#56155));
#10841=EDGE_LOOP('',(#56156,#56157,#56158,#56159,#56160));
#10842=EDGE_LOOP('',(#56161,#56162,#56163,#56164,#56165,#56166,#56167,#56168,
#56169,#56170,#56171,#56172,#56173,#56174,#56175,#56176,#56177,#56178,#56179,
#56180,#56181,#56182,#56183,#56184,#56185,#56186,#56187,#56188,#56189,#56190,
#56191,#56192,#56193,#56194,#56195,#56196,#56197,#56198,#56199,#56200,#56201,
#56202,#56203,#56204,#56205,#56206,#56207,#56208,#56209,#56210,#56211,#56212,
#56213,#56214,#56215,#56216,#56217,#56218,#56219,#56220,#56221,#56222,#56223,
#56224,#56225,#56226,#56227,#56228,#56229,#56230,#56231,#56232,#56233,#56234,
#56235,#56236,#56237,#56238,#56239,#56240,#56241,#56242,#56243,#56244,#56245,
#56246,#56247,#56248,#56249,#56250,#56251,#56252,#56253,#56254,#56255,#56256,
#56257,#56258,#56259,#56260,#56261,#56262,#56263,#56264,#56265,#56266,#56267,
#56268,#56269,#56270,#56271));
#10843=EDGE_LOOP('',(#56272));
#10844=EDGE_LOOP('',(#56273));
#10845=EDGE_LOOP('',(#56274,#56275,#56276,#56277,#56278,#56279,#56280,#56281,
#56282,#56283,#56284,#56285,#56286,#56287,#56288,#56289,#56290,#56291,#56292,
#56293,#56294));
#10846=EDGE_LOOP('',(#56295,#56296,#56297,#56298));
#10847=EDGE_LOOP('',(#56299,#56300,#56301,#56302));
#10848=EDGE_LOOP('',(#56303,#56304,#56305,#56306));
#10849=EDGE_LOOP('',(#56307,#56308,#56309,#56310));
#10850=EDGE_LOOP('',(#56311,#56312,#56313,#56314));
#10851=EDGE_LOOP('',(#56315,#56316,#56317,#56318));
#10852=EDGE_LOOP('',(#56319,#56320,#56321,#56322,#56323,#56324,#56325,#56326));
#10853=EDGE_LOOP('',(#56327,#56328,#56329,#56330,#56331,#56332,#56333,#56334));
#10854=EDGE_LOOP('',(#56335,#56336,#56337,#56338,#56339,#56340,#56341,#56342));
#10855=EDGE_LOOP('',(#56343,#56344));
#10856=EDGE_LOOP('',(#56345,#56346));
#10857=EDGE_LOOP('',(#56347,#56348));
#10858=EDGE_LOOP('',(#56349,#56350));
#10859=EDGE_LOOP('',(#56351,#56352));
#10860=EDGE_LOOP('',(#56353,#56354));
#10861=EDGE_LOOP('',(#56355,#56356));
#10862=EDGE_LOOP('',(#56357,#56358));
#10863=EDGE_LOOP('',(#56359,#56360));
#10864=EDGE_LOOP('',(#56361,#56362));
#10865=EDGE_LOOP('',(#56363,#56364));
#10866=EDGE_LOOP('',(#56365,#56366));
#10867=EDGE_LOOP('',(#56367,#56368,#56369,#56370,#56371,#56372,#56373,#56374));
#10868=EDGE_LOOP('',(#56375,#56376,#56377,#56378,#56379,#56380,#56381,#56382));
#10869=EDGE_LOOP('',(#56383,#56384,#56385,#56386,#56387,#56388,#56389,#56390));
#10870=EDGE_LOOP('',(#56391,#56392,#56393,#56394,#56395,#56396,#56397,#56398));
#16667=LINE('',#110991,#22701);
#16668=LINE('',#111015,#22702);
#16669=LINE('',#111063,#22703);
#16670=LINE('',#111111,#22704);
#16671=LINE('',#111165,#22705);
#16672=LINE('',#111213,#22706);
#16673=LINE('',#111261,#22707);
#16674=LINE('',#111315,#22708);
#16675=LINE('',#111363,#22709);
#16676=LINE('',#111411,#22710);
#16677=LINE('',#111459,#22711);
#16678=LINE('',#111513,#22712);
#16679=LINE('',#111561,#22713);
#16680=LINE('',#111609,#22714);
#16681=LINE('',#111631,#22715);
#16682=LINE('',#111655,#22716);
#16683=LINE('',#111680,#22717);
#16684=LINE('',#111705,#22718);
#16685=LINE('',#111729,#22719);
#16686=LINE('',#111753,#22720);
#16687=LINE('',#111778,#22721);
#16688=LINE('',#111803,#22722);
#16689=LINE('',#111827,#22723);
#16690=LINE('',#111852,#22724);
#16691=LINE('',#111877,#22725);
#16692=LINE('',#112943,#22726);
#16693=LINE('',#112953,#22727);
#16694=LINE('',#112955,#22728);
#16695=LINE('',#112956,#22729);
#16696=LINE('',#112960,#22730);
#16697=LINE('',#112966,#22731);
#16698=LINE('',#112971,#22732);
#16699=LINE('',#112975,#22733);
#16700=LINE('',#112979,#22734);
#16701=LINE('',#112983,#22735);
#16702=LINE('',#112987,#22736);
#16703=LINE('',#112991,#22737);
#16704=LINE('',#112995,#22738);
#16705=LINE('',#112999,#22739);
#16706=LINE('',#113003,#22740);
#16707=LINE('',#113007,#22741);
#16708=LINE('',#113011,#22742);
#16709=LINE('',#113015,#22743);
#16710=LINE('',#113019,#22744);
#16711=LINE('',#113023,#22745);
#16712=LINE('',#113027,#22746);
#16713=LINE('',#113031,#22747);
#16714=LINE('',#113035,#22748);
#16715=LINE('',#113039,#22749);
#16716=LINE('',#113043,#22750);
#16717=LINE('',#113047,#22751);
#16718=LINE('',#113051,#22752);
#16719=LINE('',#113055,#22753);
#16720=LINE('',#113059,#22754);
#16721=LINE('',#113063,#22755);
#16722=LINE('',#113067,#22756);
#16723=LINE('',#113071,#22757);
#16724=LINE('',#113075,#22758);
#16725=LINE('',#113079,#22759);
#16726=LINE('',#113083,#22760);
#16727=LINE('',#113087,#22761);
#16728=LINE('',#113091,#22762);
#16729=LINE('',#113095,#22763);
#16730=LINE('',#113099,#22764);
#16731=LINE('',#113103,#22765);
#16732=LINE('',#113107,#22766);
#16733=LINE('',#113111,#22767);
#16734=LINE('',#113115,#22768);
#16735=LINE('',#113119,#22769);
#16736=LINE('',#113126,#22770);
#16737=LINE('',#113130,#22771);
#16738=LINE('',#113134,#22772);
#16739=LINE('',#113138,#22773);
#16740=LINE('',#113142,#22774);
#16741=LINE('',#113146,#22775);
#16742=LINE('',#113150,#22776);
#16743=LINE('',#113154,#22777);
#16744=LINE('',#113158,#22778);
#16745=LINE('',#113162,#22779);
#16746=LINE('',#113166,#22780);
#16747=LINE('',#113170,#22781);
#16748=LINE('',#113174,#22782);
#16749=LINE('',#113178,#22783);
#16750=LINE('',#113182,#22784);
#16751=LINE('',#113186,#22785);
#16752=LINE('',#113190,#22786);
#16753=LINE('',#113194,#22787);
#16754=LINE('',#113198,#22788);
#16755=LINE('',#113202,#22789);
#16756=LINE('',#113206,#22790);
#16757=LINE('',#113210,#22791);
#16758=LINE('',#113214,#22792);
#16759=LINE('',#113218,#22793);
#16760=LINE('',#113222,#22794);
#16761=LINE('',#113226,#22795);
#16762=LINE('',#113230,#22796);
#16763=LINE('',#113234,#22797);
#16764=LINE('',#113238,#22798);
#16765=LINE('',#113242,#22799);
#16766=LINE('',#113246,#22800);
#16767=LINE('',#113250,#22801);
#16768=LINE('',#113254,#22802);
#16769=LINE('',#113262,#22803);
#16770=LINE('',#113263,#22804);
#16771=LINE('',#113265,#22805);
#16772=LINE('',#113276,#22806);
#16773=LINE('',#113277,#22807);
#16774=LINE('',#113279,#22808);
#16775=LINE('',#113290,#22809);
#16776=LINE('',#113291,#22810);
#16777=LINE('',#113293,#22811);
#16778=LINE('',#113304,#22812);
#16779=LINE('',#113305,#22813);
#16780=LINE('',#113307,#22814);
#16781=LINE('',#113318,#22815);
#16782=LINE('',#113319,#22816);
#16783=LINE('',#113321,#22817);
#16784=LINE('',#113332,#22818);
#16785=LINE('',#113333,#22819);
#16786=LINE('',#113335,#22820);
#16787=LINE('',#113346,#22821);
#16788=LINE('',#113347,#22822);
#16789=LINE('',#113349,#22823);
#16790=LINE('',#113360,#22824);
#16791=LINE('',#113361,#22825);
#16792=LINE('',#113363,#22826);
#16793=LINE('',#113374,#22827);
#16794=LINE('',#113375,#22828);
#16795=LINE('',#113377,#22829);
#16796=LINE('',#113388,#22830);
#16797=LINE('',#113389,#22831);
#16798=LINE('',#113391,#22832);
#16799=LINE('',#113402,#22833);
#16800=LINE('',#113403,#22834);
#16801=LINE('',#113405,#22835);
#16802=LINE('',#113416,#22836);
#16803=LINE('',#113417,#22837);
#16804=LINE('',#113419,#22838);
#16805=LINE('',#113430,#22839);
#16806=LINE('',#113431,#22840);
#16807=LINE('',#113433,#22841);
#16808=LINE('',#113444,#22842);
#16809=LINE('',#113445,#22843);
#16810=LINE('',#113447,#22844);
#16811=LINE('',#113458,#22845);
#16812=LINE('',#113459,#22846);
#16813=LINE('',#113461,#22847);
#16814=LINE('',#113472,#22848);
#16815=LINE('',#113473,#22849);
#16816=LINE('',#113475,#22850);
#16817=LINE('',#113486,#22851);
#16818=LINE('',#113487,#22852);
#16819=LINE('',#113489,#22853);
#16820=LINE('',#113500,#22854);
#16821=LINE('',#113501,#22855);
#16822=LINE('',#113503,#22856);
#16823=LINE('',#113514,#22857);
#16824=LINE('',#113515,#22858);
#16825=LINE('',#113517,#22859);
#16826=LINE('',#113528,#22860);
#16827=LINE('',#113529,#22861);
#16828=LINE('',#113531,#22862);
#16829=LINE('',#113542,#22863);
#16830=LINE('',#113543,#22864);
#16831=LINE('',#113545,#22865);
#16832=LINE('',#113556,#22866);
#16833=LINE('',#113557,#22867);
#16834=LINE('',#113559,#22868);
#16835=LINE('',#113570,#22869);
#16836=LINE('',#113571,#22870);
#16837=LINE('',#113573,#22871);
#16838=LINE('',#113584,#22872);
#16839=LINE('',#113585,#22873);
#16840=LINE('',#113587,#22874);
#16841=LINE('',#113598,#22875);
#16842=LINE('',#113599,#22876);
#16843=LINE('',#113601,#22877);
#16844=LINE('',#113612,#22878);
#16845=LINE('',#113613,#22879);
#16846=LINE('',#113615,#22880);
#16847=LINE('',#113626,#22881);
#16848=LINE('',#113627,#22882);
#16849=LINE('',#113629,#22883);
#16850=LINE('',#113640,#22884);
#16851=LINE('',#113641,#22885);
#16852=LINE('',#113643,#22886);
#16853=LINE('',#113654,#22887);
#16854=LINE('',#113655,#22888);
#16855=LINE('',#113657,#22889);
#16856=LINE('',#113668,#22890);
#16857=LINE('',#113669,#22891);
#16858=LINE('',#113671,#22892);
#16859=LINE('',#113682,#22893);
#16860=LINE('',#113683,#22894);
#16861=LINE('',#113685,#22895);
#16862=LINE('',#113696,#22896);
#16863=LINE('',#113697,#22897);
#16864=LINE('',#113699,#22898);
#16865=LINE('',#113710,#22899);
#16866=LINE('',#113711,#22900);
#16867=LINE('',#113713,#22901);
#16868=LINE('',#113724,#22902);
#16869=LINE('',#113725,#22903);
#16870=LINE('',#113727,#22904);
#16871=LINE('',#113738,#22905);
#16872=LINE('',#113739,#22906);
#16873=LINE('',#113741,#22907);
#16874=LINE('',#113751,#22908);
#16875=LINE('',#113757,#22909);
#16876=LINE('',#113819,#22910);
#16877=LINE('',#113821,#22911);
#16878=LINE('',#113825,#22912);
#16879=LINE('',#113827,#22913);
#16880=LINE('',#113831,#22914);
#16881=LINE('',#113834,#22915);
#16882=LINE('',#113837,#22916);
#16883=LINE('',#113839,#22917);
#16884=LINE('',#113843,#22918);
#16885=LINE('',#113846,#22919);
#16886=LINE('',#113849,#22920);
#16887=LINE('',#113852,#22921);
#16888=LINE('',#113854,#22922);
#16889=LINE('',#113856,#22923);
#16890=LINE('',#113858,#22924);
#16891=LINE('',#113859,#22925);
#16892=LINE('',#113861,#22926);
#16893=LINE('',#113863,#22927);
#16894=LINE('',#113864,#22928);
#16895=LINE('',#113866,#22929);
#16896=LINE('',#113868,#22930);
#16897=LINE('',#113869,#22931);
#16898=LINE('',#113873,#22932);
#16899=LINE('',#113876,#22933);
#16900=LINE('',#113878,#22934);
#16901=LINE('',#113881,#22935);
#16902=LINE('',#113891,#22936);
#16903=LINE('',#113894,#22937);
#16904=LINE('',#113898,#22938);
#16905=LINE('',#113900,#22939);
#16906=LINE('',#113902,#22940);
#22701=VECTOR('',#75277,1.25);
#22702=VECTOR('',#75282,1.25);
#22703=VECTOR('',#75285,1.25);
#22704=VECTOR('',#75288,1.25);
#22705=VECTOR('',#75291,1.25);
#22706=VECTOR('',#75294,1.25);
#22707=VECTOR('',#75297,1.25);
#22708=VECTOR('',#75300,1.25);
#22709=VECTOR('',#75303,1.25);
#22710=VECTOR('',#75306,1.25);
#22711=VECTOR('',#75309,1.25);
#22712=VECTOR('',#75312,1.25);
#22713=VECTOR('',#75315,1.25);
#22714=VECTOR('',#75318,0.958249999999999);
#22715=VECTOR('',#75323,0.958249999999999);
#22716=VECTOR('',#75326,0.958249999999999);
#22717=VECTOR('',#75329,0.958249999999999);
#22718=VECTOR('',#75332,0.958249999999999);
#22719=VECTOR('',#75335,0.958249999999999);
#22720=VECTOR('',#75338,0.958249999999999);
#22721=VECTOR('',#75341,0.958249999999999);
#22722=VECTOR('',#75344,0.958249999999999);
#22723=VECTOR('',#75347,0.958249999999999);
#22724=VECTOR('',#75350,0.958249999999999);
#22725=VECTOR('',#75353,0.958249999999999);
#22726=VECTOR('',#75386,1.04);
#22727=VECTOR('',#75393,10.);
#22728=VECTOR('',#75394,10.);
#22729=VECTOR('',#75395,10.);
#22730=VECTOR('',#75400,10.);
#22731=VECTOR('',#75403,10.);
#22732=VECTOR('',#75408,10.);
#22733=VECTOR('',#75411,10.);
#22734=VECTOR('',#75414,10.);
#22735=VECTOR('',#75417,10.);
#22736=VECTOR('',#75420,10.);
#22737=VECTOR('',#75423,10.);
#22738=VECTOR('',#75426,10.);
#22739=VECTOR('',#75429,10.);
#22740=VECTOR('',#75432,10.);
#22741=VECTOR('',#75435,10.);
#22742=VECTOR('',#75438,10.);
#22743=VECTOR('',#75441,10.);
#22744=VECTOR('',#75444,10.);
#22745=VECTOR('',#75447,10.);
#22746=VECTOR('',#75450,10.);
#22747=VECTOR('',#75453,10.);
#22748=VECTOR('',#75456,10.);
#22749=VECTOR('',#75459,10.);
#22750=VECTOR('',#75462,10.);
#22751=VECTOR('',#75465,10.);
#22752=VECTOR('',#75468,10.);
#22753=VECTOR('',#75471,10.);
#22754=VECTOR('',#75474,10.);
#22755=VECTOR('',#75477,10.);
#22756=VECTOR('',#75480,10.);
#22757=VECTOR('',#75483,10.);
#22758=VECTOR('',#75486,10.);
#22759=VECTOR('',#75489,10.);
#22760=VECTOR('',#75492,10.);
#22761=VECTOR('',#75495,10.);
#22762=VECTOR('',#75498,10.);
#22763=VECTOR('',#75501,10.);
#22764=VECTOR('',#75504,10.);
#22765=VECTOR('',#75507,10.);
#22766=VECTOR('',#75510,10.);
#22767=VECTOR('',#75513,10.);
#22768=VECTOR('',#75516,10.);
#22769=VECTOR('',#75519,2.25);
#22770=VECTOR('',#75526,10.);
#22771=VECTOR('',#75529,10.);
#22772=VECTOR('',#75532,10.);
#22773=VECTOR('',#75535,10.);
#22774=VECTOR('',#75538,10.);
#22775=VECTOR('',#75541,10.);
#22776=VECTOR('',#75544,10.);
#22777=VECTOR('',#75547,10.);
#22778=VECTOR('',#75550,10.);
#22779=VECTOR('',#75553,10.);
#22780=VECTOR('',#75556,10.);
#22781=VECTOR('',#75559,10.);
#22782=VECTOR('',#75562,10.);
#22783=VECTOR('',#75565,10.);
#22784=VECTOR('',#75568,10.);
#22785=VECTOR('',#75571,10.);
#22786=VECTOR('',#75574,10.);
#22787=VECTOR('',#75577,10.);
#22788=VECTOR('',#75580,10.);
#22789=VECTOR('',#75583,10.);
#22790=VECTOR('',#75586,10.);
#22791=VECTOR('',#75589,10.);
#22792=VECTOR('',#75592,10.);
#22793=VECTOR('',#75595,10.);
#22794=VECTOR('',#75598,10.);
#22795=VECTOR('',#75601,10.);
#22796=VECTOR('',#75604,10.);
#22797=VECTOR('',#75607,10.);
#22798=VECTOR('',#75610,10.);
#22799=VECTOR('',#75613,10.);
#22800=VECTOR('',#75616,10.);
#22801=VECTOR('',#75619,10.);
#22802=VECTOR('',#75622,10.);
#22803=VECTOR('',#75627,10.);
#22804=VECTOR('',#75628,10.);
#22805=VECTOR('',#75631,10.);
#22806=VECTOR('',#75636,10.);
#22807=VECTOR('',#75637,10.);
#22808=VECTOR('',#75640,10.);
#22809=VECTOR('',#75645,10.);
#22810=VECTOR('',#75646,10.);
#22811=VECTOR('',#75649,10.);
#22812=VECTOR('',#75654,10.);
#22813=VECTOR('',#75655,10.);
#22814=VECTOR('',#75658,10.);
#22815=VECTOR('',#75663,10.);
#22816=VECTOR('',#75664,10.);
#22817=VECTOR('',#75667,10.);
#22818=VECTOR('',#75672,10.);
#22819=VECTOR('',#75673,10.);
#22820=VECTOR('',#75676,10.);
#22821=VECTOR('',#75681,10.);
#22822=VECTOR('',#75682,10.);
#22823=VECTOR('',#75685,10.);
#22824=VECTOR('',#75690,10.);
#22825=VECTOR('',#75691,10.);
#22826=VECTOR('',#75694,10.);
#22827=VECTOR('',#75699,10.);
#22828=VECTOR('',#75700,10.);
#22829=VECTOR('',#75703,10.);
#22830=VECTOR('',#75708,10.);
#22831=VECTOR('',#75709,10.);
#22832=VECTOR('',#75712,10.);
#22833=VECTOR('',#75717,10.);
#22834=VECTOR('',#75718,10.);
#22835=VECTOR('',#75721,10.);
#22836=VECTOR('',#75726,10.);
#22837=VECTOR('',#75727,10.);
#22838=VECTOR('',#75730,10.);
#22839=VECTOR('',#75735,10.);
#22840=VECTOR('',#75736,10.);
#22841=VECTOR('',#75739,10.);
#22842=VECTOR('',#75744,10.);
#22843=VECTOR('',#75745,10.);
#22844=VECTOR('',#75748,10.);
#22845=VECTOR('',#75753,10.);
#22846=VECTOR('',#75754,10.);
#22847=VECTOR('',#75757,10.);
#22848=VECTOR('',#75762,10.);
#22849=VECTOR('',#75763,10.);
#22850=VECTOR('',#75766,10.);
#22851=VECTOR('',#75771,10.);
#22852=VECTOR('',#75772,10.);
#22853=VECTOR('',#75775,10.);
#22854=VECTOR('',#75780,10.);
#22855=VECTOR('',#75781,10.);
#22856=VECTOR('',#75784,10.);
#22857=VECTOR('',#75789,10.);
#22858=VECTOR('',#75790,10.);
#22859=VECTOR('',#75793,10.);
#22860=VECTOR('',#75798,10.);
#22861=VECTOR('',#75799,10.);
#22862=VECTOR('',#75802,10.);
#22863=VECTOR('',#75807,10.);
#22864=VECTOR('',#75808,10.);
#22865=VECTOR('',#75811,10.);
#22866=VECTOR('',#75816,10.);
#22867=VECTOR('',#75817,10.);
#22868=VECTOR('',#75820,10.);
#22869=VECTOR('',#75825,10.);
#22870=VECTOR('',#75826,10.);
#22871=VECTOR('',#75829,10.);
#22872=VECTOR('',#75834,10.);
#22873=VECTOR('',#75835,10.);
#22874=VECTOR('',#75838,10.);
#22875=VECTOR('',#75843,10.);
#22876=VECTOR('',#75844,10.);
#22877=VECTOR('',#75847,10.);
#22878=VECTOR('',#75852,10.);
#22879=VECTOR('',#75853,10.);
#22880=VECTOR('',#75856,10.);
#22881=VECTOR('',#75861,10.);
#22882=VECTOR('',#75862,10.);
#22883=VECTOR('',#75865,10.);
#22884=VECTOR('',#75870,10.);
#22885=VECTOR('',#75871,10.);
#22886=VECTOR('',#75874,10.);
#22887=VECTOR('',#75879,10.);
#22888=VECTOR('',#75880,10.);
#22889=VECTOR('',#75883,10.);
#22890=VECTOR('',#75888,10.);
#22891=VECTOR('',#75889,10.);
#22892=VECTOR('',#75892,10.);
#22893=VECTOR('',#75897,10.);
#22894=VECTOR('',#75898,10.);
#22895=VECTOR('',#75901,10.);
#22896=VECTOR('',#75906,10.);
#22897=VECTOR('',#75907,10.);
#22898=VECTOR('',#75910,10.);
#22899=VECTOR('',#75915,10.);
#22900=VECTOR('',#75916,10.);
#22901=VECTOR('',#75919,10.);
#22902=VECTOR('',#75924,10.);
#22903=VECTOR('',#75925,10.);
#22904=VECTOR('',#75928,10.);
#22905=VECTOR('',#75933,10.);
#22906=VECTOR('',#75934,10.);
#22907=VECTOR('',#75937,10.);
#22908=VECTOR('',#75948,2.1);
#22909=VECTOR('',#75955,1.20470053837925);
#22910=VECTOR('',#75970,10.);
#22911=VECTOR('',#75971,10.);
#22912=VECTOR('',#75976,10.);
#22913=VECTOR('',#75977,10.);
#22914=VECTOR('',#75982,10.);
#22915=VECTOR('',#75985,10.);
#22916=VECTOR('',#75988,10.);
#22917=VECTOR('',#75989,10.);
#22918=VECTOR('',#75994,10.);
#22919=VECTOR('',#75997,10.);
#22920=VECTOR('',#76000,10.);
#22921=VECTOR('',#76003,10.);
#22922=VECTOR('',#76006,10.);
#22923=VECTOR('',#76007,10.);
#22924=VECTOR('',#76008,10.);
#22925=VECTOR('',#76009,10.);
#22926=VECTOR('',#76012,10.);
#22927=VECTOR('',#76013,10.);
#22928=VECTOR('',#76014,10.);
#22929=VECTOR('',#76017,10.);
#22930=VECTOR('',#76018,10.);
#22931=VECTOR('',#76019,10.);
#22932=VECTOR('',#76026,10.);
#22933=VECTOR('',#76031,10.);
#22934=VECTOR('',#76034,10.);
#22935=VECTOR('',#76037,10.);
#22936=VECTOR('',#76054,10.);
#22937=VECTOR('',#76059,10.);
#22938=VECTOR('',#76064,1.15470053837925);
#22939=VECTOR('',#76067,10.);
#22940=VECTOR('',#76070,10.);
#24565=B_SPLINE_CURVE_WITH_KNOTS('',3,(#110993,#110994,#110995,#110996,
#110997,#110998,#110999,#111000,#111001,#111002),.UNSPECIFIED.,.F.,.F.,
(4,3,3,4),(-4.09282965349932,-3.97811826982011,-2.98358870236508,-2.06974660785394),
 .UNSPECIFIED.);
#24566=B_SPLINE_CURVE_WITH_KNOTS('',3,(#111005,#111006,#111007,#111008,
#111009,#111010,#111011),.UNSPECIFIED.,.F.,.F.,(4,3,4),(0.,0.99452956745502,
1.11850960794437),.UNSPECIFIED.);
#24567=B_SPLINE_CURVE_WITH_KNOTS('',3,(#111016,#111017,#111018,#111019,
#111020,#111021,#111022,#111023,#111024,#111025,#111026,#111027,#111028,
#111029,#111030,#111031,#111032,#111033,#111034,#111035,#111036,#111037),
 .UNSPECIFIED.,.F.,.F.,(4,3,3,3,3,3,3,4),(-10.3760149606789,-9.94529567455027,
-8.95076610709525,-7.95623653964022,-6.96170697218519,-5.96717740473016,
-4.97264783727514,-4.09282965349932),.UNSPECIFIED.);
#24568=B_SPLINE_CURVE_WITH_KNOTS('',3,(#111038,#111039,#111040,#111041,
#111042,#111043,#111044,#111045,#111046,#111047,#111048,#111049,#111050,
#111051,#111052,#111053,#111054,#111055,#111056,#111057,#111058,#111059),
 .UNSPECIFIED.,.F.,.F.,(4,3,3,3,3,3,3,4),(1.11850960794437,1.98905913491005,
2.98358870236508,3.97811826982011,4.97264783727514,5.96717740473017,6.9617069721852,
7.40169491512398),.UNSPECIFIED.);
#24569=B_SPLINE_CURVE_WITH_KNOTS('',3,(#111064,#111065,#111066,#111067,
#111068,#111069,#111070,#111071,#111072,#111073,#111074,#111075,#111076,
#111077,#111078,#111079,#111080,#111081,#111082,#111083,#111084,#111085),
 .UNSPECIFIED.,.F.,.F.,(4,3,3,3,3,3,3,4),(-16.6592002678585,-15.9124730792804,
-14.9179435118254,-13.9234139443704,-12.9288843769154,-11.9343548094603,
-10.9398252420053,-10.3760149606789),.UNSPECIFIED.);
#24570=B_SPLINE_CURVE_WITH_KNOTS('',3,(#111086,#111087,#111088,#111089,
#111090,#111091,#111092,#111093,#111094,#111095,#111096,#111097,#111098,
#111099,#111100,#111101,#111102,#111103,#111104,#111105,#111106,#111107),
 .UNSPECIFIED.,.F.,.F.,(4,3,3,3,3,3,3,4),(7.40169491512398,7.95623653964023,
8.95076610709526,9.94529567455028,10.9398252420053,11.9343548094603,12.9288843769154,
13.6848802223036),.UNSPECIFIED.);
#24571=B_SPLINE_CURVE_WITH_KNOTS('',3,(#111112,#111113,#111114,#111115,
#111116,#111117,#111118,#111119,#111120,#111121,#111122,#111123,#111124,
#111125,#111126,#111127,#111128,#111129,#111130,#111131,#111132,#111133,
#111134,#111135,#111136),.UNSPECIFIED.,.F.,.F.,(4,3,3,3,3,3,3,3,4),(-22.9423855750381,
-22.8741800514656,-21.8796504840106,-20.8851209165556,-19.8905913491005,
-18.8960617816455,-17.9015322141905,-16.9070026467355,-16.6592002678585),
 .UNSPECIFIED.);
#24572=B_SPLINE_CURVE_WITH_KNOTS('',3,(#111137,#111138,#111139,#111140,
#111141,#111142,#111143,#111144,#111145,#111146,#111147,#111148,#111149,
#111150,#111151,#111152,#111153,#111154,#111155,#111156,#111157,#111158,
#111159,#111160,#111161),.UNSPECIFIED.,.F.,.F.,(4,3,3,3,3,3,3,3,4),(13.6848802223036,
13.9234139443704,14.9179435118254,15.9124730792804,16.9070026467355,17.9015322141905,
18.8960617816455,19.8905913491005,19.9680655294831),.UNSPECIFIED.);
#24573=B_SPLINE_CURVE_WITH_KNOTS('',3,(#111166,#111167,#111168,#111169,
#111170,#111171,#111172,#111173,#111174,#111175,#111176,#111177,#111178,
#111179,#111180,#111181,#111182,#111183,#111184,#111185,#111186,#111187),
 .UNSPECIFIED.,.F.,.F.,(4,3,3,3,3,3,3,4),(-29.2255708822177,-28.8413574561958,
-27.8468278887408,-26.8522983212857,-25.8577687538307,-24.8632391863757,
-23.8687096189207,-22.9423855750381),.UNSPECIFIED.);
#24574=B_SPLINE_CURVE_WITH_KNOTS('',3,(#111188,#111189,#111190,#111191,
#111192,#111193,#111194,#111195,#111196,#111197,#111198,#111199,#111200,
#111201,#111202,#111203,#111204,#111205,#111206,#111207,#111208,#111209),
 .UNSPECIFIED.,.F.,.F.,(4,3,3,3,3,3,3,4),(19.9680655294831,20.8851209165556,
21.8796504840106,22.8741800514656,23.8687096189207,24.8632391863757,25.8577687538307,
26.2512508366627),.UNSPECIFIED.);
#24575=B_SPLINE_CURVE_WITH_KNOTS('',3,(#111214,#111215,#111216,#111217,
#111218,#111219,#111220,#111221,#111222,#111223,#111224,#111225,#111226,
#111227,#111228,#111229,#111230,#111231,#111232,#111233,#111234,#111235),
 .UNSPECIFIED.,.F.,.F.,(4,3,3,3,3,3,3,4),(-35.5087561893973,-34.808534860926,
-33.8140052934709,-32.8194757260159,-31.8249461585609,-30.8304165911058,
-29.8358870236508,-29.2255708822177),.UNSPECIFIED.);
#24576=B_SPLINE_CURVE_WITH_KNOTS('',3,(#111236,#111237,#111238,#111239,
#111240,#111241,#111242,#111243,#111244,#111245,#111246,#111247,#111248,
#111249,#111250,#111251,#111252,#111253,#111254,#111255,#111256,#111257),
 .UNSPECIFIED.,.F.,.F.,(4,3,3,3,3,3,3,4),(26.2512508366627,26.8522983212857,
27.8468278887408,28.8413574561958,29.8358870236508,30.8304165911058,31.8249461585609,
32.5344361438423),.UNSPECIFIED.);
#24577=B_SPLINE_CURVE_WITH_KNOTS('',3,(#111262,#111263,#111264,#111265,
#111266,#111267,#111268,#111269,#111270,#111271,#111272,#111273,#111274,
#111275,#111276,#111277,#111278,#111279,#111280,#111281,#111282,#111283,
#111284,#111285,#111286),.UNSPECIFIED.,.F.,.F.,(4,3,3,3,3,3,3,3,4),(-41.7919414965769,
-41.7702418331111,-40.7757122656561,-39.7811826982011,-38.7866531307461,
-37.792123563291,-36.797593995836,-35.803064428381,-35.5087561893973),
 .UNSPECIFIED.);
#24578=B_SPLINE_CURVE_WITH_KNOTS('',3,(#111287,#111288,#111289,#111290,
#111291,#111292,#111293,#111294,#111295,#111296,#111297,#111298,#111299,
#111300,#111301,#111302,#111303,#111304,#111305,#111306,#111307,#111308,
#111309,#111310,#111311),.UNSPECIFIED.,.F.,.F.,(4,3,3,3,3,3,3,3,4),(32.5344361438423,
32.8194757260159,33.8140052934709,34.808534860926,35.803064428381,36.797593995836,
37.792123563291,38.7866531307461,38.8176214510219),.UNSPECIFIED.);
#24579=B_SPLINE_CURVE_WITH_KNOTS('',3,(#111316,#111317,#111318,#111319,
#111320,#111321,#111322,#111323,#111324,#111325,#111326,#111327,#111328,
#111329,#111330,#111331,#111332,#111333,#111334,#111335,#111336,#111337),
 .UNSPECIFIED.,.F.,.F.,(4,3,3,3,3,3,3,4),(-48.0751268037564,-47.7374192378413,
-46.7428896703863,-45.7483601029313,-44.7538305354762,-43.7593009680212,
-42.7647714005662,-41.7919414965769),.UNSPECIFIED.);
#24580=B_SPLINE_CURVE_WITH_KNOTS('',3,(#111338,#111339,#111340,#111341,
#111342,#111343,#111344,#111345,#111346,#111347,#111348,#111349,#111350,
#111351,#111352,#111353,#111354,#111355,#111356,#111357,#111358,#111359),
 .UNSPECIFIED.,.F.,.F.,(4,3,3,3,3,3,3,4),(38.8176214510219,39.7811826982011,
40.7757122656561,41.7702418331111,42.7647714005662,43.7593009680212,44.7538305354762,
45.1008067582015),.UNSPECIFIED.);
#24581=B_SPLINE_CURVE_WITH_KNOTS('',3,(#111364,#111365,#111366,#111367,
#111368,#111369,#111370,#111371,#111372,#111373,#111374,#111375,#111376,
#111377,#111378,#111379,#111380,#111381,#111382,#111383,#111384,#111385),
 .UNSPECIFIED.,.F.,.F.,(4,3,3,3,3,3,3,4),(-54.358312110936,-53.7045966425715,
-52.7100670751164,-51.7155375076614,-50.7210079402064,-49.7264783727514,
-48.7319488052963,-48.0751268037564),.UNSPECIFIED.);
#24582=B_SPLINE_CURVE_WITH_KNOTS('',3,(#111386,#111387,#111388,#111389,
#111390,#111391,#111392,#111393,#111394,#111395,#111396,#111397,#111398,
#111399,#111400,#111401,#111402,#111403,#111404,#111405,#111406,#111407),
 .UNSPECIFIED.,.F.,.F.,(4,3,3,3,3,3,3,4),(45.1008067582015,45.7483601029313,
46.7428896703863,47.7374192378413,48.7319488052963,49.7264783727514,50.7210079402064,
51.3839920653811),.UNSPECIFIED.);
#24583=B_SPLINE_CURVE_WITH_KNOTS('',3,(#111412,#111413,#111414,#111415,
#111416,#111417,#111418,#111419,#111420,#111421,#111422,#111423,#111424,
#111425,#111426,#111427,#111428,#111429,#111430,#111431,#111432,#111433),
 .UNSPECIFIED.,.F.,.F.,(4,3,3,3,3,3,3,4),(-60.6414974181156,-59.6717740473017,
-58.6772444798466,-57.6827149123916,-56.6881853449366,-55.6936557774815,
-54.6991262100265,-54.358312110936),.UNSPECIFIED.);
#24584=B_SPLINE_CURVE_WITH_KNOTS('',3,(#111434,#111435,#111436,#111437,
#111438,#111439,#111440,#111441,#111442,#111443,#111444,#111445,#111446,
#111447,#111448,#111449,#111450,#111451,#111452,#111453,#111454,#111455),
 .UNSPECIFIED.,.F.,.F.,(4,3,3,3,3,3,3,4),(51.3839920653811,51.7155375076614,
52.7100670751164,53.7045966425715,54.6991262100265,55.6936557774815,56.6881853449365,
57.6671773725607),.UNSPECIFIED.);
#24585=B_SPLINE_CURVE_WITH_KNOTS('',3,(#111460,#111461,#111462,#111463,
#111464,#111465,#111466,#111467,#111468,#111469,#111470,#111471,#111472,
#111473,#111474,#111475,#111476,#111477,#111478,#111479,#111480,#111481,
#111482,#111483,#111484),.UNSPECIFIED.,.F.,.F.,(4,3,3,3,3,3,3,3,4),(-66.9246827252952,
-66.6334810194868,-65.6389514520318,-64.6444218845768,-63.6498923171218,
-62.6553627496667,-61.6608331822117,-60.6663036147567,-60.6414974181156),
 .UNSPECIFIED.);
#24586=B_SPLINE_CURVE_WITH_KNOTS('',3,(#111485,#111486,#111487,#111488,
#111489,#111490,#111491,#111492,#111493,#111494,#111495,#111496,#111497,
#111498,#111499,#111500,#111501,#111502,#111503,#111504,#111505,#111506,
#111507,#111508,#111509),.UNSPECIFIED.,.F.,.F.,(4,3,3,3,3,3,3,3,4),(57.6671773725607,
57.6827149123916,58.6772444798466,59.6717740473016,60.6663036147567,61.6608331822117,
62.6553627496667,63.6498923171217,63.9503626797403),.UNSPECIFIED.);
#24587=B_SPLINE_CURVE_WITH_KNOTS('',3,(#111514,#111515,#111516,#111517,
#111518,#111519,#111520,#111521,#111522,#111523,#111524,#111525,#111526,
#111527,#111528,#111529,#111530,#111531,#111532,#111533,#111534,#111535),
 .UNSPECIFIED.,.F.,.F.,(4,3,3,3,3,3,3,4),(-73.2078680324748,-72.600658424217,
-71.606128856762,-70.6115992893069,-69.6170697218519,-68.6225401543969,
-67.6280105869419,-66.9246827252952),.UNSPECIFIED.);
#24588=B_SPLINE_CURVE_WITH_KNOTS('',3,(#111536,#111537,#111538,#111539,
#111540,#111541,#111542,#111543,#111544,#111545,#111546,#111547,#111548,
#111549,#111550,#111551,#111552,#111553,#111554,#111555,#111556,#111557),
 .UNSPECIFIED.,.F.,.F.,(4,3,3,3,3,3,3,4),(63.9503626797403,64.6444218845768,
65.6389514520318,66.6334810194868,67.6280105869419,68.6225401543969,69.6170697218519,
70.2335479869199),.UNSPECIFIED.);
#24589=B_SPLINE_CURVE_WITH_KNOTS('',3,(#111562,#111563,#111564,#111565,
#111566,#111567,#111568,#111569,#111570,#111571,#111572,#111573,#111574,
#111575,#111576,#111577,#111578,#111579,#111580,#111581,#111582,#111583),
 .UNSPECIFIED.,.F.,.F.,(4,3,3,3,3,3,3,4),(-79.4910533396544,-78.5678358289472,
-77.5733062614921,-76.5787766940371,-75.5842471265821,-74.5897175591271,
-73.595187991672,-73.2078680324748),.UNSPECIFIED.);
#24590=B_SPLINE_CURVE_WITH_KNOTS('',3,(#111584,#111585,#111586,#111587,
#111588,#111589,#111590,#111591,#111592,#111593,#111594,#111595,#111596,
#111597,#111598,#111599,#111600,#111601,#111602,#111603,#111604,#111605),
 .UNSPECIFIED.,.F.,.F.,(4,3,3,3,3,3,3,4),(70.2335479869199,70.6115992893069,
71.606128856762,72.600658424217,73.595187991672,74.589717559127,75.5842471265821,
76.5167332940995),.UNSPECIFIED.);
#24591=B_SPLINE_CURVE_WITH_KNOTS('',3,(#111611,#111612,#111613,#111614,
#111615,#111616,#111617,#111618),.UNSPECIFIED.,.F.,.F.,(4,1,1,1,1,4),(84.8230016469244,
85.2103216061216,86.2048511735766,87.1993807410316,88.1939103084867,89.1077524029978),
 .UNSPECIFIED.);
#24592=B_SPLINE_CURVE_WITH_KNOTS('',3,(#111621,#111622,#111623,#111624,
#111625,#111626,#111627),.UNSPECIFIED.,.F.,.F.,(4,1,1,1,4),(84.8230016469244,
84.8850450468619,85.879574614317,86.874104181772,87.868633749227),
 .UNSPECIFIED.);
#24593=B_SPLINE_CURVE_WITH_KNOTS('',3,(#111632,#111633,#111634,#111635,
#111636,#111637,#111638,#111639,#111640,#111641),.UNSPECIFIED.,.F.,.F.,
(4,1,1,1,1,1,1,4),(78.5398163397448,79.2431442013914,80.2376737688465,81.2322033363015,
82.2267329037565,83.2212624712115,84.2157920386666,84.8230016469244),
 .UNSPECIFIED.);
#24594=B_SPLINE_CURVE_WITH_KNOTS('',3,(#111642,#111643,#111644,#111645,
#111646,#111647,#111648,#111649,#111650,#111651),.UNSPECIFIED.,.F.,.F.,
(4,1,1,1,1,1,1,4),(78.5398163397448,78.9178676421318,79.9123972095868,80.9069267770418,
81.9014563444969,82.8959859119519,83.8905154794069,84.8230016469244),
 .UNSPECIFIED.);
#24595=B_SPLINE_CURVE_WITH_KNOTS('',3,(#111656,#111657,#111658,#111659,
#111660,#111661,#111662,#111663,#111664,#111665,#111666),.UNSPECIFIED.,
 .F.,.F.,(4,1,1,1,1,1,1,1,4),(72.2566310325652,72.2814372292062,73.2759667966613,
74.2704963641163,75.2650259315713,76.2595554990263,77.2540850664814,78.2486146339364,
78.5398163397448),.UNSPECIFIED.);
#24596=B_SPLINE_CURVE_WITH_KNOTS('',3,(#111667,#111668,#111669,#111670,
#111671,#111672,#111673,#111674,#111675,#111676),.UNSPECIFIED.,.F.,.F.,
(4,1,1,1,1,1,1,4),(72.2566310325652,72.9506902374016,73.9452198048566,74.9397493723117,
75.9342789397667,76.9288085072217,77.9233380746768,78.5398163397448),
 .UNSPECIFIED.);
#24597=B_SPLINE_CURVE_WITH_KNOTS('',3,(#111681,#111682,#111683,#111684,
#111685,#111686,#111687,#111688,#111689,#111690),.UNSPECIFIED.,.F.,.F.,
(4,1,1,1,1,1,1,4),(65.9734457253856,66.3142598244761,67.3087893919311,68.3033189593861,
69.2978485268412,70.2923780942962,71.2869076617512,72.2566310325652),
 .UNSPECIFIED.);
#24598=B_SPLINE_CURVE_WITH_KNOTS('',3,(#111691,#111692,#111693,#111694,
#111695,#111696,#111697,#111698,#111699,#111700,#111701),.UNSPECIFIED.,
 .F.,.F.,(4,1,1,1,1,1,1,1,4),(65.9734457253856,65.9889832652164,66.9835128326715,
67.9780424001265,68.9725719675815,69.9671015350365,70.9616311024916,71.9561606699466,
72.2566310325652),.UNSPECIFIED.);
#24599=B_SPLINE_CURVE_WITH_KNOTS('',3,(#111706,#111707,#111708,#111709,
#111710,#111711,#111712,#111713,#111714,#111715),.UNSPECIFIED.,.F.,.F.,
(4,1,1,1,1,1,1,4),(59.6902604182061,60.3470824197459,61.3416119872009,62.336141554656,
63.330671122111,64.325200689566,65.319730257021,65.9734457253856),
 .UNSPECIFIED.);
#24600=B_SPLINE_CURVE_WITH_KNOTS('',3,(#111716,#111717,#111718,#111719,
#111720,#111721,#111722,#111723,#111724,#111725),.UNSPECIFIED.,.F.,.F.,
(4,1,1,1,1,1,1,4),(59.690260418206,60.0218058604863,61.0163354279413,62.0108649953963,
63.0053945628514,63.9999241303064,64.9944536977614,65.9734457253856),
 .UNSPECIFIED.);
#24601=B_SPLINE_CURVE_WITH_KNOTS('',3,(#111730,#111731,#111732,#111733,
#111734,#111735,#111736,#111737,#111738,#111739),.UNSPECIFIED.,.F.,.F.,
(4,1,1,1,1,1,1,4),(53.4070751110265,54.3799050150157,55.3744345824708,56.3689641499258,
57.3634937173808,58.3580232848359,59.3525528522909,59.6902604182061),
 .UNSPECIFIED.);
#24602=B_SPLINE_CURVE_WITH_KNOTS('',3,(#111740,#111741,#111742,#111743,
#111744,#111745,#111746,#111747,#111748,#111749),.UNSPECIFIED.,.F.,.F.,
(4,1,1,1,1,1,1,4),(53.4070751110265,54.0546284557561,55.0491580232111,56.0436875906662,
57.0382171581212,58.0327467255762,59.0272762930312,59.690260418206),
 .UNSPECIFIED.);
#24603=B_SPLINE_CURVE_WITH_KNOTS('',3,(#111754,#111755,#111756,#111757,
#111758,#111759,#111760,#111761,#111762,#111763,#111764),.UNSPECIFIED.,
 .F.,.F.,(4,1,1,1,1,1,1,1,4),(47.1238898038469,47.4181980428306,48.4127276102856,
49.4072571777406,50.4017867451956,51.3963163126507,52.3908458801057,53.3853754475607,
53.4070751110265),.UNSPECIFIED.);
#24604=B_SPLINE_CURVE_WITH_KNOTS('',3,(#111765,#111766,#111767,#111768,
#111769,#111770,#111771,#111772,#111773,#111774),.UNSPECIFIED.,.F.,.F.,
(4,1,1,1,1,1,1,4),(47.1238898038468,48.0874510510259,49.081980618481,50.076510185936,
51.071039753391,52.0655693208461,53.0600988883011,53.4070751110265),
 .UNSPECIFIED.);
#24605=B_SPLINE_CURVE_WITH_KNOTS('',3,(#111779,#111780,#111781,#111782,
#111783,#111784,#111785,#111786,#111787,#111788),.UNSPECIFIED.,.F.,.F.,
(4,1,1,1,1,1,1,4),(40.8407044966673,41.4510206381004,42.4455502055554,43.4400797730104,
44.4346093404655,45.4291389079205,46.4236684753755,47.1238898038469),
 .UNSPECIFIED.);
#24606=B_SPLINE_CURVE_WITH_KNOTS('',3,(#111789,#111790,#111791,#111792,
#111793,#111794,#111795,#111796,#111797,#111798,#111799),.UNSPECIFIED.,
 .F.,.F.,(4,1,1,1,1,1,1,1,4),(40.8407044966673,41.1257440788408,42.1202736462958,
43.1148032137508,44.1093327812058,45.1038623486609,46.0983919161159,47.0929214835709,
47.1238898038468),.UNSPECIFIED.);
#24607=B_SPLINE_CURVE_WITH_KNOTS('',3,(#111804,#111805,#111806,#111807,
#111808,#111809,#111810,#111811,#111812,#111813),.UNSPECIFIED.,.F.,.F.,
(4,1,1,1,1,1,1,4),(34.5575191894877,35.4838432333702,36.4783728008253,37.4729023682803,
38.4674319357353,39.4619615031903,40.4564910706454,40.8407044966673),
 .UNSPECIFIED.);
#24608=B_SPLINE_CURVE_WITH_KNOTS('',3,(#111814,#111815,#111816,#111817,
#111818,#111819,#111820,#111821,#111822,#111823),.UNSPECIFIED.,.F.,.F.,
(4,1,1,1,1,1,1,4),(34.5575191894877,35.1585666741106,36.1530962415656,37.1476258090206,
38.1421553764757,39.1366849439307,40.1312145113857,40.8407044966673),
 .UNSPECIFIED.);
#24609=B_SPLINE_CURVE_WITH_KNOTS('',3,(#111828,#111829,#111830,#111831,
#111832,#111833,#111834,#111835,#111836,#111837,#111838),.UNSPECIFIED.,
 .F.,.F.,(4,1,1,1,1,1,1,1,4),(28.2743338823081,28.522136261185,29.5166658286401,
30.5111953960951,31.5057249635501,32.5002545310051,33.4947840984602,34.4893136659152,
34.5575191894877),.UNSPECIFIED.);
#24610=B_SPLINE_CURVE_WITH_KNOTS('',3,(#111839,#111840,#111841,#111842,
#111843,#111844,#111845,#111846,#111847,#111848),.UNSPECIFIED.,.F.,.F.,
(4,1,1,1,1,1,1,4),(28.2743338823081,29.1913892693804,30.1859188368355,31.1804484042905,
32.1749779717455,33.1695075392005,34.1640371066556,34.5575191894877),
 .UNSPECIFIED.);
#24611=B_SPLINE_CURVE_WITH_KNOTS('',3,(#111853,#111854,#111855,#111856,
#111857,#111858,#111859,#111860,#111861,#111862),.UNSPECIFIED.,.F.,.F.,
(4,1,1,1,1,1,1,4),(21.9911485751285,22.5549588564549,23.5494884239099,24.5440179913649,
25.53854755882,26.533077126275,27.52760669373,28.2743338823081),
 .UNSPECIFIED.);
#24612=B_SPLINE_CURVE_WITH_KNOTS('',3,(#111863,#111864,#111865,#111866,
#111867,#111868,#111869,#111870,#111871,#111872,#111873),.UNSPECIFIED.,
 .F.,.F.,(4,1,1,1,1,1,1,1,4),(21.9911485751285,22.2296822971952,23.2242118646503,
24.2187414321053,25.2132709995603,26.2078005670153,27.2023301344704,28.1968597019254,
28.2743338823081),.UNSPECIFIED.);
#24613=B_SPLINE_CURVE_WITH_KNOTS('',3,(#111878,#111879,#111880,#111881,
#111882,#111883,#111884,#111885,#111886,#111887),.UNSPECIFIED.,.F.,.F.,
(4,1,1,1,1,1,1,4),(15.7079632679489,16.5877814517247,17.5823110191797,18.5768405866348,
19.5713701540898,20.5658997215448,21.5604292889998,21.9911485751285),
 .UNSPECIFIED.);
#24614=B_SPLINE_CURVE_WITH_KNOTS('',3,(#111888,#111889,#111890,#111891,
#111892,#111893,#111894,#111895,#111896,#111897),.UNSPECIFIED.,.F.,.F.,
(4,1,1,1,1,1,1,4),(15.7079632679489,16.2625048924651,17.2570344599201,18.2515640273751,
19.2460935948302,20.2406231622852,21.2351527297402,21.9911485751285),
 .UNSPECIFIED.);
#24615=B_SPLINE_CURVE_WITH_KNOTS('',3,(#111900,#111901,#111902,#111903,
#111904,#111905,#111906,#111907,#111908,#111909,#111910,#111911,#111912,
#111913,#111914,#111915,#111916,#111917,#111918,#111919,#111920,#111921,
#111922,#111923,#111924,#111925,#111926,#111927,#111928,#111929,#111930,
#111931,#111932,#111933,#111934,#111935,#111936,#111937,#111938,#111939,
#111940,#111941,#111942,#111943,#111944,#111945,#111946,#111947,#111948,
#111949,#111950,#111951,#111952,#111953,#111954,#111955,#111956,#111957,
#111958,#111959,#111960,#111961,#111962,#111963,#111964,#111965,#111966,
#111967,#111968,#111969,#111970,#111971,#111972,#111973,#111974,#111975,
#111976,#111977,#111978,#111979,#111980,#111981),.UNSPECIFIED.,.F.,.F.,
(4,3,3,3,3,3,3,3,3,3,3,3,3,3,3,3,3,3,3,3,3,3,3,3,3,3,3,4),(-0.22752384543732,
-0.219644941593229,-0.206672788411731,-0.201988504816839,-0.199228673818224,
-0.186142187643616,-0.17735787870582,-0.174280837207973,-0.171522085977862,
-0.157608493518707,-0.143805082530456,-0.136820740933153,-0.133782689272465,
-0.130929890576033,-0.116671801511094,-0.115867716141243,-0.10211356834673,
-0.0955239922338215,-0.0919125451791094,-0.0890238524864623,-0.0747164121491554,
-0.0600826688674195,-0.0525723352589921,-0.0471438779813513,-0.044400099706211,
-0.0292633397771947,-0.0142357759108071,0.),.UNSPECIFIED.);
#24616=B_SPLINE_CURVE_WITH_KNOTS('',3,(#111986,#111987,#111988,#111989,
#111990,#111991,#111992,#111993,#111994,#111995,#111996,#111997,#111998,
#111999,#112000,#112001,#112002,#112003,#112004,#112005,#112006,#112007,
#112008,#112009,#112010,#112011,#112012,#112013,#112014,#112015,#112016,
#112017,#112018,#112019,#112020,#112021,#112022,#112023,#112024,#112025,
#112026,#112027,#112028,#112029,#112030,#112031,#112032,#112033,#112034,
#112035,#112036,#112037,#112038,#112039,#112040,#112041,#112042,#112043,
#112044,#112045,#112046,#112047,#112048,#112049,#112050,#112051,#112052,
#112053,#112054,#112055,#112056,#112057,#112058,#112059,#112060,#112061,
#112062,#112063,#112064,#112065,#112066,#112067),.UNSPECIFIED.,.F.,.F.,
(4,3,3,3,3,3,3,3,3,3,3,3,3,3,3,3,3,3,3,3,3,3,3,3,3,3,3,4),(-0.226379821609573,
-0.216598310100724,-0.202320352416955,-0.197194587028726,-0.193788187974472,
-0.178894738696219,-0.169329727438014,-0.165216054886868,-0.161050933351805,
-0.146381862171498,-0.132316768710259,-0.124831238690339,-0.120870158045062,
-0.117643417161341,-0.104003776331328,-0.102374648630577,-0.0883202432056002,
-0.0820195682337035,-0.0785432646891857,-0.0759675957890928,-0.062423681066772,
-0.0489709890027446,-0.0428226697475022,-0.0393194641576752,-0.0361992866354357,
-0.0232864813778267,-0.0108353570978016,0.),.UNSPECIFIED.);
#24617=B_SPLINE_CURVE_WITH_KNOTS('',3,(#112400,#112401,#112402,#112403,
#112404,#112405,#112406),.UNSPECIFIED.,.F.,.F.,(4,3,4),(76.5167332940995,
76.5787766940371,77.4926187885482),.UNSPECIFIED.);
#24618=B_SPLINE_CURVE_WITH_KNOTS('',3,(#112408,#112409,#112410,#112411,
#112412,#112413,#112414,#112415,#112416,#112417,#112418,#112419,#112420,
#112421,#112422,#112423,#112424,#112425,#112426,#112427,#112428,#112429,
#112430,#112431,#112432,#112433,#112434,#112435,#112436,#112437,#112438,
#112439,#112440,#112441,#112442,#112443,#112444,#112445,#112446,#112447,
#112448,#112449,#112450,#112451,#112452,#112453,#112454,#112455,#112456,
#112457,#112458,#112459,#112460,#112461,#112462,#112463,#112464,#112465,
#112466,#112467,#112468,#112469,#112470,#112471,#112472,#112473,#112474,
#112475,#112476,#112477,#112478,#112479,#112480,#112481,#112482,#112483,
#112484,#112485,#112486,#112487,#112488,#112489),.UNSPECIFIED.,.F.,.F.,
(4,3,3,3,3,3,3,3,3,3,3,3,3,3,3,3,3,3,3,3,3,3,3,3,3,3,3,4),(-0.227523845437304,
-0.219644941593212,-0.206672788411716,-0.201988507240929,-0.199228678135215,
-0.186142197116225,-0.177357886994353,-0.174280886377888,-0.171522097642482,
-0.157608502267172,-0.143805090711497,-0.136820747068934,-0.133782715582441,
-0.130929893645298,-0.116671804148527,-0.115867716141243,-0.102113570864824,
-0.0955239927945993,-0.0919125441244498,-0.0890238521567004,-0.0747164149647553,
-0.0600826747802964,-0.0525723404327594,-0.0471438710041018,-0.0444000939394238,
-0.0292633362002102,-0.0142357658394895,0.),.UNSPECIFIED.);
#24619=B_SPLINE_CURVE_WITH_KNOTS('',3,(#112490,#112491,#112492,#112493,
#112494,#112495,#112496,#112497,#112498),.UNSPECIFIED.,.F.,.F.,(4,1,1,1,
1,1,4),(10.3760149606788,11.2898570551899,12.284386622645,13.2789161901,
14.273445757555,15.26797532501,15.7079632679489),.UNSPECIFIED.);
#24620=B_SPLINE_CURVE_WITH_KNOTS('',3,(#112503,#112504,#112505,#112506,
#112507,#112508,#112509,#112510,#112511,#112512,#112513,#112514,#112515,
#112516,#112517,#112518,#112519,#112520,#112521,#112522,#112523,#112524,
#112525,#112526,#112527,#112528,#112529,#112530,#112531,#112532,#112533,
#112534,#112535,#112536,#112537,#112538,#112539,#112540,#112541,#112542,
#112543,#112544,#112545,#112546,#112547,#112548,#112549,#112550,#112551,
#112552,#112553,#112554,#112555,#112556,#112557,#112558,#112559,#112560,
#112561,#112562,#112563,#112564,#112565,#112566,#112567,#112568,#112569,
#112570,#112571,#112572,#112573,#112574,#112575,#112576,#112577,#112578,
#112579,#112580,#112581,#112582,#112583,#112584),.UNSPECIFIED.,.F.,.F.,
(4,3,3,3,3,3,3,3,3,3,3,3,3,3,3,3,3,3,3,3,3,3,3,3,3,3,3,4),(-0.226379821609617,
-0.216598310100761,-0.202320352416989,-0.197194584463025,-0.193788183076757,
-0.178894733706718,-0.169329723072201,-0.165216045592835,-0.161050933697972,
-0.146381862431125,-0.132316761525014,-0.124831233301406,-0.120870151653617,
-0.117643414358862,-0.104003766621399,-0.102374648630583,-0.0883203225023742,
-0.0820195870500072,-0.0785433310585492,-0.0759676655609074,-0.0624237500455779,
-0.0489710625427503,-0.0428226961256205,-0.0393194822861717,-0.0361992934244102,
-0.0232864953899939,-0.0108353829046375,0.),.UNSPECIFIED.);
#24621=B_SPLINE_CURVE_WITH_KNOTS('',3,(#112588,#112589,#112590,#112591,
#112592,#112593,#112594,#112595),.UNSPECIFIED.,.F.,.F.,(4,1,1,1,1,4),(11.6151336144496,
12.6096631819046,13.6041927493596,14.5987223168147,15.5932518842697,15.7079632679489),
 .UNSPECIFIED.);
#24622=B_SPLINE_CURVE_WITH_KNOTS('',3,(#112928,#112929,#112930,#112931),
 .UNSPECIFIED.,.F.,.F.,(4,4),(-79.5623653964022,-79.4910533396544),
 .UNSPECIFIED.);
#30027=VERTEX_POINT('',#110989);
#30028=VERTEX_POINT('',#110990);
#30029=VERTEX_POINT('',#110992);
#30030=VERTEX_POINT('',#111003);
#30031=VERTEX_POINT('',#111013);
#30032=VERTEX_POINT('',#111014);
#30033=VERTEX_POINT('',#111061);
#30034=VERTEX_POINT('',#111062);
#30035=VERTEX_POINT('',#111109);
#30036=VERTEX_POINT('',#111110);
#30037=VERTEX_POINT('',#111163);
#30038=VERTEX_POINT('',#111164);
#30039=VERTEX_POINT('',#111211);
#30040=VERTEX_POINT('',#111212);
#30041=VERTEX_POINT('',#111259);
#30042=VERTEX_POINT('',#111260);
#30043=VERTEX_POINT('',#111313);
#30044=VERTEX_POINT('',#111314);
#30045=VERTEX_POINT('',#111361);
#30046=VERTEX_POINT('',#111362);
#30047=VERTEX_POINT('',#111409);
#30048=VERTEX_POINT('',#111410);
#30049=VERTEX_POINT('',#111457);
#30050=VERTEX_POINT('',#111458);
#30051=VERTEX_POINT('',#111511);
#30052=VERTEX_POINT('',#111512);
#30053=VERTEX_POINT('',#111559);
#30054=VERTEX_POINT('',#111560);
#30055=VERTEX_POINT('',#111607);
#30056=VERTEX_POINT('',#111608);
#30057=VERTEX_POINT('',#111610);
#30058=VERTEX_POINT('',#111619);
#30059=VERTEX_POINT('',#111629);
#30060=VERTEX_POINT('',#111630);
#30061=VERTEX_POINT('',#111653);
#30062=VERTEX_POINT('',#111654);
#30063=VERTEX_POINT('',#111678);
#30064=VERTEX_POINT('',#111679);
#30065=VERTEX_POINT('',#111703);
#30066=VERTEX_POINT('',#111704);
#30067=VERTEX_POINT('',#111727);
#30068=VERTEX_POINT('',#111728);
#30069=VERTEX_POINT('',#111751);
#30070=VERTEX_POINT('',#111752);
#30071=VERTEX_POINT('',#111776);
#30072=VERTEX_POINT('',#111777);
#30073=VERTEX_POINT('',#111801);
#30074=VERTEX_POINT('',#111802);
#30075=VERTEX_POINT('',#111825);
#30076=VERTEX_POINT('',#111826);
#30077=VERTEX_POINT('',#111850);
#30078=VERTEX_POINT('',#111851);
#30079=VERTEX_POINT('',#111875);
#30080=VERTEX_POINT('',#111876);
#30081=VERTEX_POINT('',#111899);
#30082=VERTEX_POINT('',#111982);
#30083=VERTEX_POINT('',#111984);
#30084=VERTEX_POINT('',#112407);
#30085=VERTEX_POINT('',#112500);
#30086=VERTEX_POINT('',#112502);
#30087=VERTEX_POINT('',#112933);
#30088=VERTEX_POINT('',#112939);
#30089=VERTEX_POINT('',#112942);
#30090=VERTEX_POINT('',#112947);
#30091=VERTEX_POINT('',#112948);
#30092=VERTEX_POINT('',#112952);
#30093=VERTEX_POINT('',#112954);
#30094=VERTEX_POINT('',#112958);
#30095=VERTEX_POINT('',#112962);
#30096=VERTEX_POINT('',#112968);
#30097=VERTEX_POINT('',#112970);
#30098=VERTEX_POINT('',#112972);
#30099=VERTEX_POINT('',#112974);
#30100=VERTEX_POINT('',#112976);
#30101=VERTEX_POINT('',#112978);
#30102=VERTEX_POINT('',#112980);
#30103=VERTEX_POINT('',#112982);
#30104=VERTEX_POINT('',#112984);
#30105=VERTEX_POINT('',#112986);
#30106=VERTEX_POINT('',#112988);
#30107=VERTEX_POINT('',#112990);
#30108=VERTEX_POINT('',#112992);
#30109=VERTEX_POINT('',#112994);
#30110=VERTEX_POINT('',#112996);
#30111=VERTEX_POINT('',#112998);
#30112=VERTEX_POINT('',#113000);
#30113=VERTEX_POINT('',#113002);
#30114=VERTEX_POINT('',#113004);
#30115=VERTEX_POINT('',#113006);
#30116=VERTEX_POINT('',#113008);
#30117=VERTEX_POINT('',#113010);
#30118=VERTEX_POINT('',#113012);
#30119=VERTEX_POINT('',#113014);
#30120=VERTEX_POINT('',#113016);
#30121=VERTEX_POINT('',#113018);
#30122=VERTEX_POINT('',#113020);
#30123=VERTEX_POINT('',#113022);
#30124=VERTEX_POINT('',#113024);
#30125=VERTEX_POINT('',#113026);
#30126=VERTEX_POINT('',#113028);
#30127=VERTEX_POINT('',#113030);
#30128=VERTEX_POINT('',#113032);
#30129=VERTEX_POINT('',#113034);
#30130=VERTEX_POINT('',#113036);
#30131=VERTEX_POINT('',#113038);
#30132=VERTEX_POINT('',#113040);
#30133=VERTEX_POINT('',#113042);
#30134=VERTEX_POINT('',#113044);
#30135=VERTEX_POINT('',#113046);
#30136=VERTEX_POINT('',#113048);
#30137=VERTEX_POINT('',#113050);
#30138=VERTEX_POINT('',#113052);
#30139=VERTEX_POINT('',#113054);
#30140=VERTEX_POINT('',#113056);
#30141=VERTEX_POINT('',#113058);
#30142=VERTEX_POINT('',#113060);
#30143=VERTEX_POINT('',#113062);
#30144=VERTEX_POINT('',#113064);
#30145=VERTEX_POINT('',#113066);
#30146=VERTEX_POINT('',#113068);
#30147=VERTEX_POINT('',#113070);
#30148=VERTEX_POINT('',#113072);
#30149=VERTEX_POINT('',#113074);
#30150=VERTEX_POINT('',#113076);
#30151=VERTEX_POINT('',#113078);
#30152=VERTEX_POINT('',#113080);
#30153=VERTEX_POINT('',#113082);
#30154=VERTEX_POINT('',#113084);
#30155=VERTEX_POINT('',#113086);
#30156=VERTEX_POINT('',#113088);
#30157=VERTEX_POINT('',#113090);
#30158=VERTEX_POINT('',#113092);
#30159=VERTEX_POINT('',#113094);
#30160=VERTEX_POINT('',#113096);
#30161=VERTEX_POINT('',#113098);
#30162=VERTEX_POINT('',#113100);
#30163=VERTEX_POINT('',#113102);
#30164=VERTEX_POINT('',#113104);
#30165=VERTEX_POINT('',#113106);
#30166=VERTEX_POINT('',#113108);
#30167=VERTEX_POINT('',#113110);
#30168=VERTEX_POINT('',#113112);
#30169=VERTEX_POINT('',#113114);
#30170=VERTEX_POINT('',#113116);
#30171=VERTEX_POINT('',#113118);
#30172=VERTEX_POINT('',#113120);
#30173=VERTEX_POINT('',#113123);
#30174=VERTEX_POINT('',#113125);
#30175=VERTEX_POINT('',#113127);
#30176=VERTEX_POINT('',#113129);
#30177=VERTEX_POINT('',#113131);
#30178=VERTEX_POINT('',#113133);
#30179=VERTEX_POINT('',#113135);
#30180=VERTEX_POINT('',#113137);
#30181=VERTEX_POINT('',#113139);
#30182=VERTEX_POINT('',#113141);
#30183=VERTEX_POINT('',#113143);
#30184=VERTEX_POINT('',#113145);
#30185=VERTEX_POINT('',#113147);
#30186=VERTEX_POINT('',#113149);
#30187=VERTEX_POINT('',#113151);
#30188=VERTEX_POINT('',#113153);
#30189=VERTEX_POINT('',#113155);
#30190=VERTEX_POINT('',#113157);
#30191=VERTEX_POINT('',#113159);
#30192=VERTEX_POINT('',#113161);
#30193=VERTEX_POINT('',#113163);
#30194=VERTEX_POINT('',#113165);
#30195=VERTEX_POINT('',#113167);
#30196=VERTEX_POINT('',#113169);
#30197=VERTEX_POINT('',#113171);
#30198=VERTEX_POINT('',#113173);
#30199=VERTEX_POINT('',#113175);
#30200=VERTEX_POINT('',#113177);
#30201=VERTEX_POINT('',#113179);
#30202=VERTEX_POINT('',#113181);
#30203=VERTEX_POINT('',#113183);
#30204=VERTEX_POINT('',#113185);
#30205=VERTEX_POINT('',#113187);
#30206=VERTEX_POINT('',#113189);
#30207=VERTEX_POINT('',#113191);
#30208=VERTEX_POINT('',#113193);
#30209=VERTEX_POINT('',#113195);
#30210=VERTEX_POINT('',#113197);
#30211=VERTEX_POINT('',#113199);
#30212=VERTEX_POINT('',#113201);
#30213=VERTEX_POINT('',#113203);
#30214=VERTEX_POINT('',#113205);
#30215=VERTEX_POINT('',#113207);
#30216=VERTEX_POINT('',#113209);
#30217=VERTEX_POINT('',#113211);
#30218=VERTEX_POINT('',#113213);
#30219=VERTEX_POINT('',#113215);
#30220=VERTEX_POINT('',#113217);
#30221=VERTEX_POINT('',#113219);
#30222=VERTEX_POINT('',#113221);
#30223=VERTEX_POINT('',#113223);
#30224=VERTEX_POINT('',#113225);
#30225=VERTEX_POINT('',#113227);
#30226=VERTEX_POINT('',#113229);
#30227=VERTEX_POINT('',#113231);
#30228=VERTEX_POINT('',#113233);
#30229=VERTEX_POINT('',#113235);
#30230=VERTEX_POINT('',#113237);
#30231=VERTEX_POINT('',#113239);
#30232=VERTEX_POINT('',#113241);
#30233=VERTEX_POINT('',#113243);
#30234=VERTEX_POINT('',#113245);
#30235=VERTEX_POINT('',#113247);
#30236=VERTEX_POINT('',#113249);
#30237=VERTEX_POINT('',#113251);
#30238=VERTEX_POINT('',#113253);
#30239=VERTEX_POINT('',#113257);
#30240=VERTEX_POINT('',#113261);
#30241=VERTEX_POINT('',#113271);
#30242=VERTEX_POINT('',#113275);
#30243=VERTEX_POINT('',#113285);
#30244=VERTEX_POINT('',#113289);
#30245=VERTEX_POINT('',#113299);
#30246=VERTEX_POINT('',#113303);
#30247=VERTEX_POINT('',#113313);
#30248=VERTEX_POINT('',#113317);
#30249=VERTEX_POINT('',#113327);
#30250=VERTEX_POINT('',#113331);
#30251=VERTEX_POINT('',#113341);
#30252=VERTEX_POINT('',#113345);
#30253=VERTEX_POINT('',#113355);
#30254=VERTEX_POINT('',#113359);
#30255=VERTEX_POINT('',#113369);
#30256=VERTEX_POINT('',#113373);
#30257=VERTEX_POINT('',#113383);
#30258=VERTEX_POINT('',#113387);
#30259=VERTEX_POINT('',#113397);
#30260=VERTEX_POINT('',#113401);
#30261=VERTEX_POINT('',#113411);
#30262=VERTEX_POINT('',#113415);
#30263=VERTEX_POINT('',#113425);
#30264=VERTEX_POINT('',#113429);
#30265=VERTEX_POINT('',#113439);
#30266=VERTEX_POINT('',#113443);
#30267=VERTEX_POINT('',#113453);
#30268=VERTEX_POINT('',#113457);
#30269=VERTEX_POINT('',#113467);
#30270=VERTEX_POINT('',#113471);
#30271=VERTEX_POINT('',#113481);
#30272=VERTEX_POINT('',#113485);
#30273=VERTEX_POINT('',#113495);
#30274=VERTEX_POINT('',#113499);
#30275=VERTEX_POINT('',#113509);
#30276=VERTEX_POINT('',#113513);
#30277=VERTEX_POINT('',#113523);
#30278=VERTEX_POINT('',#113527);
#30279=VERTEX_POINT('',#113537);
#30280=VERTEX_POINT('',#113541);
#30281=VERTEX_POINT('',#113551);
#30282=VERTEX_POINT('',#113555);
#30283=VERTEX_POINT('',#113565);
#30284=VERTEX_POINT('',#113569);
#30285=VERTEX_POINT('',#113579);
#30286=VERTEX_POINT('',#113583);
#30287=VERTEX_POINT('',#113593);
#30288=VERTEX_POINT('',#113597);
#30289=VERTEX_POINT('',#113607);
#30290=VERTEX_POINT('',#113611);
#30291=VERTEX_POINT('',#113621);
#30292=VERTEX_POINT('',#113625);
#30293=VERTEX_POINT('',#113635);
#30294=VERTEX_POINT('',#113639);
#30295=VERTEX_POINT('',#113649);
#30296=VERTEX_POINT('',#113653);
#30297=VERTEX_POINT('',#113663);
#30298=VERTEX_POINT('',#113667);
#30299=VERTEX_POINT('',#113677);
#30300=VERTEX_POINT('',#113681);
#30301=VERTEX_POINT('',#113691);
#30302=VERTEX_POINT('',#113695);
#30303=VERTEX_POINT('',#113705);
#30304=VERTEX_POINT('',#113709);
#30305=VERTEX_POINT('',#113719);
#30306=VERTEX_POINT('',#113723);
#30307=VERTEX_POINT('',#113733);
#30308=VERTEX_POINT('',#113737);
#30309=VERTEX_POINT('',#113749);
#30310=VERTEX_POINT('',#113753);
#30311=VERTEX_POINT('',#113756);
#30312=VERTEX_POINT('',#113758);
#30313=VERTEX_POINT('',#113762);
#30314=VERTEX_POINT('',#113764);
#30315=VERTEX_POINT('',#113768);
#30316=VERTEX_POINT('',#113772);
#30317=VERTEX_POINT('',#113774);
#30318=VERTEX_POINT('',#113778);
#30319=VERTEX_POINT('',#113782);
#30320=VERTEX_POINT('',#113784);
#30321=VERTEX_POINT('',#113788);
#30322=VERTEX_POINT('',#113792);
#30323=VERTEX_POINT('',#113794);
#30324=VERTEX_POINT('',#113798);
#30325=VERTEX_POINT('',#113802);
#30326=VERTEX_POINT('',#113804);
#30327=VERTEX_POINT('',#113808);
#30328=VERTEX_POINT('',#113812);
#30329=VERTEX_POINT('',#113818);
#30330=VERTEX_POINT('',#113820);
#30331=VERTEX_POINT('',#113824);
#30332=VERTEX_POINT('',#113826);
#30333=VERTEX_POINT('',#113830);
#30334=VERTEX_POINT('',#113832);
#30335=VERTEX_POINT('',#113836);
#30336=VERTEX_POINT('',#113838);
#30337=VERTEX_POINT('',#113842);
#30338=VERTEX_POINT('',#113844);
#30339=VERTEX_POINT('',#113848);
#30340=VERTEX_POINT('',#113850);
#30341=VERTEX_POINT('',#113855);
#30342=VERTEX_POINT('',#113857);
#30343=VERTEX_POINT('',#113862);
#30344=VERTEX_POINT('',#113867);
#30345=VERTEX_POINT('',#113880);
#30346=VERTEX_POINT('',#113890);
#30347=VERTEX_POINT('',#113897);
#38542=EDGE_CURVE('',#30027,#30028,#16667,.T.);
#38543=EDGE_CURVE('',#30027,#30029,#24565,.T.);
#38544=EDGE_CURVE('',#30030,#30029,#1430,.T.);
#38545=EDGE_CURVE('',#30030,#30028,#24566,.T.);
#38546=EDGE_CURVE('',#30031,#30032,#16668,.T.);
#38547=EDGE_CURVE('',#30031,#30027,#24567,.T.);
#38548=EDGE_CURVE('',#30028,#30032,#24568,.T.);
#38549=EDGE_CURVE('',#30033,#30034,#16669,.T.);
#38550=EDGE_CURVE('',#30033,#30031,#24569,.T.);
#38551=EDGE_CURVE('',#30032,#30034,#24570,.T.);
#38552=EDGE_CURVE('',#30035,#30036,#16670,.T.);
#38553=EDGE_CURVE('',#30035,#30033,#24571,.T.);
#38554=EDGE_CURVE('',#30034,#30036,#24572,.T.);
#38555=EDGE_CURVE('',#30037,#30038,#16671,.T.);
#38556=EDGE_CURVE('',#30037,#30035,#24573,.T.);
#38557=EDGE_CURVE('',#30036,#30038,#24574,.T.);
#38558=EDGE_CURVE('',#30039,#30040,#16672,.T.);
#38559=EDGE_CURVE('',#30039,#30037,#24575,.T.);
#38560=EDGE_CURVE('',#30038,#30040,#24576,.T.);
#38561=EDGE_CURVE('',#30041,#30042,#16673,.T.);
#38562=EDGE_CURVE('',#30041,#30039,#24577,.T.);
#38563=EDGE_CURVE('',#30040,#30042,#24578,.T.);
#38564=EDGE_CURVE('',#30043,#30044,#16674,.T.);
#38565=EDGE_CURVE('',#30043,#30041,#24579,.T.);
#38566=EDGE_CURVE('',#30042,#30044,#24580,.T.);
#38567=EDGE_CURVE('',#30045,#30046,#16675,.T.);
#38568=EDGE_CURVE('',#30045,#30043,#24581,.T.);
#38569=EDGE_CURVE('',#30044,#30046,#24582,.T.);
#38570=EDGE_CURVE('',#30047,#30048,#16676,.T.);
#38571=EDGE_CURVE('',#30047,#30045,#24583,.T.);
#38572=EDGE_CURVE('',#30046,#30048,#24584,.T.);
#38573=EDGE_CURVE('',#30049,#30050,#16677,.T.);
#38574=EDGE_CURVE('',#30049,#30047,#24585,.T.);
#38575=EDGE_CURVE('',#30048,#30050,#24586,.T.);
#38576=EDGE_CURVE('',#30051,#30052,#16678,.T.);
#38577=EDGE_CURVE('',#30051,#30049,#24587,.T.);
#38578=EDGE_CURVE('',#30050,#30052,#24588,.T.);
#38579=EDGE_CURVE('',#30053,#30054,#16679,.T.);
#38580=EDGE_CURVE('',#30053,#30051,#24589,.T.);
#38581=EDGE_CURVE('',#30052,#30054,#24590,.T.);
#38582=EDGE_CURVE('',#30055,#30056,#16680,.T.);
#38583=EDGE_CURVE('',#30055,#30057,#24591,.T.);
#38584=EDGE_CURVE('',#30058,#30057,#1431,.T.);
#38585=EDGE_CURVE('',#30056,#30058,#24592,.T.);
#38586=EDGE_CURVE('',#30059,#30060,#16681,.T.);
#38587=EDGE_CURVE('',#30059,#30055,#24593,.T.);
#38588=EDGE_CURVE('',#30060,#30056,#24594,.T.);
#38589=EDGE_CURVE('',#30061,#30062,#16682,.T.);
#38590=EDGE_CURVE('',#30061,#30059,#24595,.T.);
#38591=EDGE_CURVE('',#30062,#30060,#24596,.T.);
#38592=EDGE_CURVE('',#30063,#30064,#16683,.T.);
#38593=EDGE_CURVE('',#30063,#30061,#24597,.T.);
#38594=EDGE_CURVE('',#30064,#30062,#24598,.T.);
#38595=EDGE_CURVE('',#30065,#30066,#16684,.T.);
#38596=EDGE_CURVE('',#30065,#30063,#24599,.T.);
#38597=EDGE_CURVE('',#30066,#30064,#24600,.T.);
#38598=EDGE_CURVE('',#30067,#30068,#16685,.T.);
#38599=EDGE_CURVE('',#30067,#30065,#24601,.T.);
#38600=EDGE_CURVE('',#30068,#30066,#24602,.T.);
#38601=EDGE_CURVE('',#30069,#30070,#16686,.T.);
#38602=EDGE_CURVE('',#30069,#30067,#24603,.T.);
#38603=EDGE_CURVE('',#30070,#30068,#24604,.T.);
#38604=EDGE_CURVE('',#30071,#30072,#16687,.T.);
#38605=EDGE_CURVE('',#30071,#30069,#24605,.T.);
#38606=EDGE_CURVE('',#30072,#30070,#24606,.T.);
#38607=EDGE_CURVE('',#30073,#30074,#16688,.T.);
#38608=EDGE_CURVE('',#30073,#30071,#24607,.T.);
#38609=EDGE_CURVE('',#30074,#30072,#24608,.T.);
#38610=EDGE_CURVE('',#30075,#30076,#16689,.T.);
#38611=EDGE_CURVE('',#30075,#30073,#24609,.T.);
#38612=EDGE_CURVE('',#30076,#30074,#24610,.T.);
#38613=EDGE_CURVE('',#30077,#30078,#16690,.T.);
#38614=EDGE_CURVE('',#30077,#30075,#24611,.T.);
#38615=EDGE_CURVE('',#30078,#30076,#24612,.T.);
#38616=EDGE_CURVE('',#30079,#30080,#16691,.T.);
#38617=EDGE_CURVE('',#30079,#30077,#24613,.T.);
#38618=EDGE_CURVE('',#30080,#30078,#24614,.T.);
#38619=EDGE_CURVE('',#30057,#30081,#24615,.T.);
#38620=EDGE_CURVE('',#30082,#30081,#1432,.T.);
#38621=EDGE_CURVE('',#30083,#30082,#1433,.T.);
#38622=EDGE_CURVE('',#30083,#30058,#24616,.T.);
#38623=EDGE_CURVE('',#30054,#30083,#24617,.T.);
#38624=EDGE_CURVE('',#30084,#30030,#24618,.T.);
#38625=EDGE_CURVE('',#30084,#30080,#24619,.T.);
#38626=EDGE_CURVE('',#30029,#30085,#1434,.T.);
#38627=EDGE_CURVE('',#30029,#30086,#24620,.T.);
#38628=EDGE_CURVE('',#30086,#30084,#1435,.T.);
#38629=EDGE_CURVE('',#30085,#30030,#1436,.T.);
#38630=EDGE_CURVE('',#30086,#30079,#24621,.T.);
#38631=EDGE_CURVE('',#30081,#30053,#24622,.T.);
#38632=EDGE_CURVE('',#30085,#30087,#1437,.T.);
#38633=EDGE_CURVE('',#30087,#30087,#1438,.T.);
#38634=EDGE_CURVE('',#30081,#30083,#1439,.T.);
#38635=EDGE_CURVE('',#30088,#30088,#1440,.T.);
#38636=EDGE_CURVE('',#30082,#30089,#16692,.T.);
#38637=EDGE_CURVE('',#30089,#30089,#1441,.T.);
#38638=EDGE_CURVE('',#30090,#30091,#431,.T.);
#38639=EDGE_CURVE('',#30090,#30092,#16693,.T.);
#38640=EDGE_CURVE('',#30092,#30093,#16694,.T.);
#38641=EDGE_CURVE('',#30091,#30093,#16695,.T.);
#38642=EDGE_CURVE('',#30093,#30094,#1442,.T.);
#38643=EDGE_CURVE('',#30094,#30092,#16696,.T.);
#38644=EDGE_CURVE('',#30095,#30090,#432,.T.);
#38645=EDGE_CURVE('',#30094,#30095,#16697,.T.);
#38646=EDGE_CURVE('',#30096,#30095,#1443,.T.);
#38647=EDGE_CURVE('',#30096,#30097,#16698,.T.);
#38648=EDGE_CURVE('',#30097,#30098,#1444,.T.);
#38649=EDGE_CURVE('',#30098,#30099,#16699,.T.);
#38650=EDGE_CURVE('',#30100,#30099,#1445,.T.);
#38651=EDGE_CURVE('',#30100,#30101,#16700,.T.);
#38652=EDGE_CURVE('',#30101,#30102,#1446,.T.);
#38653=EDGE_CURVE('',#30102,#30103,#16701,.T.);
#38654=EDGE_CURVE('',#30104,#30103,#1447,.T.);
#38655=EDGE_CURVE('',#30104,#30105,#16702,.T.);
#38656=EDGE_CURVE('',#30105,#30106,#1448,.T.);
#38657=EDGE_CURVE('',#30106,#30107,#16703,.T.);
#38658=EDGE_CURVE('',#30108,#30107,#1449,.T.);
#38659=EDGE_CURVE('',#30108,#30109,#16704,.T.);
#38660=EDGE_CURVE('',#30109,#30110,#1450,.T.);
#38661=EDGE_CURVE('',#30110,#30111,#16705,.T.);
#38662=EDGE_CURVE('',#30112,#30111,#1451,.T.);
#38663=EDGE_CURVE('',#30112,#30113,#16706,.T.);
#38664=EDGE_CURVE('',#30113,#30114,#1452,.T.);
#38665=EDGE_CURVE('',#30114,#30115,#16707,.T.);
#38666=EDGE_CURVE('',#30116,#30115,#1453,.T.);
#38667=EDGE_CURVE('',#30116,#30117,#16708,.T.);
#38668=EDGE_CURVE('',#30117,#30118,#1454,.T.);
#38669=EDGE_CURVE('',#30118,#30119,#16709,.T.);
#38670=EDGE_CURVE('',#30120,#30119,#1455,.T.);
#38671=EDGE_CURVE('',#30120,#30121,#16710,.T.);
#38672=EDGE_CURVE('',#30121,#30122,#1456,.T.);
#38673=EDGE_CURVE('',#30122,#30123,#16711,.T.);
#38674=EDGE_CURVE('',#30124,#30123,#1457,.T.);
#38675=EDGE_CURVE('',#30124,#30125,#16712,.T.);
#38676=EDGE_CURVE('',#30125,#30126,#1458,.T.);
#38677=EDGE_CURVE('',#30126,#30127,#16713,.T.);
#38678=EDGE_CURVE('',#30128,#30127,#1459,.T.);
#38679=EDGE_CURVE('',#30128,#30129,#16714,.T.);
#38680=EDGE_CURVE('',#30129,#30130,#1460,.T.);
#38681=EDGE_CURVE('',#30130,#30131,#16715,.T.);
#38682=EDGE_CURVE('',#30132,#30131,#1461,.T.);
#38683=EDGE_CURVE('',#30132,#30133,#16716,.T.);
#38684=EDGE_CURVE('',#30133,#30134,#1462,.T.);
#38685=EDGE_CURVE('',#30134,#30135,#16717,.T.);
#38686=EDGE_CURVE('',#30136,#30135,#1463,.T.);
#38687=EDGE_CURVE('',#30136,#30137,#16718,.T.);
#38688=EDGE_CURVE('',#30137,#30138,#1464,.T.);
#38689=EDGE_CURVE('',#30138,#30139,#16719,.T.);
#38690=EDGE_CURVE('',#30140,#30139,#1465,.T.);
#38691=EDGE_CURVE('',#30140,#30141,#16720,.T.);
#38692=EDGE_CURVE('',#30141,#30142,#1466,.T.);
#38693=EDGE_CURVE('',#30142,#30143,#16721,.T.);
#38694=EDGE_CURVE('',#30144,#30143,#1467,.T.);
#38695=EDGE_CURVE('',#30144,#30145,#16722,.T.);
#38696=EDGE_CURVE('',#30145,#30146,#1468,.T.);
#38697=EDGE_CURVE('',#30146,#30147,#16723,.T.);
#38698=EDGE_CURVE('',#30148,#30147,#1469,.T.);
#38699=EDGE_CURVE('',#30148,#30149,#16724,.T.);
#38700=EDGE_CURVE('',#30149,#30150,#1470,.T.);
#38701=EDGE_CURVE('',#30150,#30151,#16725,.T.);
#38702=EDGE_CURVE('',#30152,#30151,#1471,.T.);
#38703=EDGE_CURVE('',#30152,#30153,#16726,.T.);
#38704=EDGE_CURVE('',#30153,#30154,#1472,.T.);
#38705=EDGE_CURVE('',#30154,#30155,#16727,.T.);
#38706=EDGE_CURVE('',#30156,#30155,#1473,.T.);
#38707=EDGE_CURVE('',#30156,#30157,#16728,.T.);
#38708=EDGE_CURVE('',#30157,#30158,#1474,.T.);
#38709=EDGE_CURVE('',#30158,#30159,#16729,.T.);
#38710=EDGE_CURVE('',#30160,#30159,#1475,.T.);
#38711=EDGE_CURVE('',#30160,#30161,#16730,.T.);
#38712=EDGE_CURVE('',#30161,#30162,#1476,.T.);
#38713=EDGE_CURVE('',#30162,#30163,#16731,.T.);
#38714=EDGE_CURVE('',#30164,#30163,#1477,.T.);
#38715=EDGE_CURVE('',#30164,#30165,#16732,.T.);
#38716=EDGE_CURVE('',#30165,#30166,#1478,.T.);
#38717=EDGE_CURVE('',#30166,#30167,#16733,.T.);
#38718=EDGE_CURVE('',#30168,#30167,#1479,.T.);
#38719=EDGE_CURVE('',#30168,#30169,#16734,.T.);
#38720=EDGE_CURVE('',#30169,#30170,#1480,.T.);
#38721=EDGE_CURVE('',#30170,#30171,#16735,.T.);
#38722=EDGE_CURVE('',#30172,#30171,#1481,.T.);
#38723=EDGE_CURVE('',#30171,#30172,#1482,.T.);
#38724=EDGE_CURVE('',#30170,#30173,#1483,.T.);
#38725=EDGE_CURVE('',#30173,#30174,#16736,.T.);
#38726=EDGE_CURVE('',#30175,#30174,#1484,.T.);
#38727=EDGE_CURVE('',#30175,#30176,#16737,.T.);
#38728=EDGE_CURVE('',#30176,#30177,#1485,.T.);
#38729=EDGE_CURVE('',#30177,#30178,#16738,.T.);
#38730=EDGE_CURVE('',#30179,#30178,#1486,.T.);
#38731=EDGE_CURVE('',#30179,#30180,#16739,.T.);
#38732=EDGE_CURVE('',#30180,#30181,#1487,.T.);
#38733=EDGE_CURVE('',#30181,#30182,#16740,.T.);
#38734=EDGE_CURVE('',#30183,#30182,#1488,.T.);
#38735=EDGE_CURVE('',#30183,#30184,#16741,.T.);
#38736=EDGE_CURVE('',#30184,#30185,#1489,.T.);
#38737=EDGE_CURVE('',#30185,#30186,#16742,.T.);
#38738=EDGE_CURVE('',#30187,#30186,#1490,.T.);
#38739=EDGE_CURVE('',#30187,#30188,#16743,.T.);
#38740=EDGE_CURVE('',#30188,#30189,#1491,.T.);
#38741=EDGE_CURVE('',#30189,#30190,#16744,.T.);
#38742=EDGE_CURVE('',#30191,#30190,#1492,.T.);
#38743=EDGE_CURVE('',#30191,#30192,#16745,.T.);
#38744=EDGE_CURVE('',#30192,#30193,#1493,.T.);
#38745=EDGE_CURVE('',#30193,#30194,#16746,.T.);
#38746=EDGE_CURVE('',#30195,#30194,#1494,.T.);
#38747=EDGE_CURVE('',#30195,#30196,#16747,.T.);
#38748=EDGE_CURVE('',#30196,#30197,#1495,.T.);
#38749=EDGE_CURVE('',#30197,#30198,#16748,.T.);
#38750=EDGE_CURVE('',#30199,#30198,#1496,.T.);
#38751=EDGE_CURVE('',#30199,#30200,#16749,.T.);
#38752=EDGE_CURVE('',#30200,#30201,#1497,.T.);
#38753=EDGE_CURVE('',#30201,#30202,#16750,.T.);
#38754=EDGE_CURVE('',#30203,#30202,#1498,.T.);
#38755=EDGE_CURVE('',#30203,#30204,#16751,.T.);
#38756=EDGE_CURVE('',#30204,#30205,#1499,.T.);
#38757=EDGE_CURVE('',#30205,#30206,#16752,.T.);
#38758=EDGE_CURVE('',#30207,#30206,#1500,.T.);
#38759=EDGE_CURVE('',#30207,#30208,#16753,.T.);
#38760=EDGE_CURVE('',#30208,#30209,#1501,.T.);
#38761=EDGE_CURVE('',#30209,#30210,#16754,.T.);
#38762=EDGE_CURVE('',#30211,#30210,#1502,.T.);
#38763=EDGE_CURVE('',#30211,#30212,#16755,.T.);
#38764=EDGE_CURVE('',#30212,#30213,#1503,.T.);
#38765=EDGE_CURVE('',#30213,#30214,#16756,.T.);
#38766=EDGE_CURVE('',#30215,#30214,#1504,.T.);
#38767=EDGE_CURVE('',#30215,#30216,#16757,.T.);
#38768=EDGE_CURVE('',#30216,#30217,#1505,.T.);
#38769=EDGE_CURVE('',#30217,#30218,#16758,.T.);
#38770=EDGE_CURVE('',#30219,#30218,#1506,.T.);
#38771=EDGE_CURVE('',#30219,#30220,#16759,.T.);
#38772=EDGE_CURVE('',#30220,#30221,#1507,.T.);
#38773=EDGE_CURVE('',#30221,#30222,#16760,.T.);
#38774=EDGE_CURVE('',#30223,#30222,#1508,.T.);
#38775=EDGE_CURVE('',#30223,#30224,#16761,.T.);
#38776=EDGE_CURVE('',#30224,#30225,#1509,.T.);
#38777=EDGE_CURVE('',#30225,#30226,#16762,.T.);
#38778=EDGE_CURVE('',#30227,#30226,#1510,.T.);
#38779=EDGE_CURVE('',#30227,#30228,#16763,.T.);
#38780=EDGE_CURVE('',#30228,#30229,#1511,.T.);
#38781=EDGE_CURVE('',#30229,#30230,#16764,.T.);
#38782=EDGE_CURVE('',#30231,#30230,#1512,.T.);
#38783=EDGE_CURVE('',#30231,#30232,#16765,.T.);
#38784=EDGE_CURVE('',#30232,#30233,#1513,.T.);
#38785=EDGE_CURVE('',#30233,#30234,#16766,.T.);
#38786=EDGE_CURVE('',#30235,#30234,#1514,.T.);
#38787=EDGE_CURVE('',#30235,#30236,#16767,.T.);
#38788=EDGE_CURVE('',#30236,#30237,#1515,.T.);
#38789=EDGE_CURVE('',#30237,#30238,#16768,.T.);
#38790=EDGE_CURVE('',#30091,#30238,#1516,.T.);
#38791=EDGE_CURVE('',#30239,#30235,#433,.T.);
#38792=EDGE_CURVE('',#30239,#30240,#16769,.T.);
#38793=EDGE_CURVE('',#30240,#30236,#16770,.T.);
#38794=EDGE_CURVE('',#30237,#30240,#16771,.T.);
#38795=EDGE_CURVE('',#30238,#30239,#434,.T.);
#38796=EDGE_CURVE('',#30241,#30231,#435,.T.);
#38797=EDGE_CURVE('',#30241,#30242,#16772,.T.);
#38798=EDGE_CURVE('',#30242,#30232,#16773,.T.);
#38799=EDGE_CURVE('',#30233,#30242,#16774,.T.);
#38800=EDGE_CURVE('',#30234,#30241,#436,.T.);
#38801=EDGE_CURVE('',#30243,#30227,#437,.T.);
#38802=EDGE_CURVE('',#30243,#30244,#16775,.T.);
#38803=EDGE_CURVE('',#30244,#30228,#16776,.T.);
#38804=EDGE_CURVE('',#30229,#30244,#16777,.T.);
#38805=EDGE_CURVE('',#30230,#30243,#438,.T.);
#38806=EDGE_CURVE('',#30245,#30223,#439,.T.);
#38807=EDGE_CURVE('',#30245,#30246,#16778,.T.);
#38808=EDGE_CURVE('',#30246,#30224,#16779,.T.);
#38809=EDGE_CURVE('',#30225,#30246,#16780,.T.);
#38810=EDGE_CURVE('',#30226,#30245,#440,.T.);
#38811=EDGE_CURVE('',#30247,#30219,#441,.T.);
#38812=EDGE_CURVE('',#30247,#30248,#16781,.T.);
#38813=EDGE_CURVE('',#30248,#30220,#16782,.T.);
#38814=EDGE_CURVE('',#30221,#30248,#16783,.T.);
#38815=EDGE_CURVE('',#30222,#30247,#442,.T.);
#38816=EDGE_CURVE('',#30249,#30215,#443,.T.);
#38817=EDGE_CURVE('',#30249,#30250,#16784,.T.);
#38818=EDGE_CURVE('',#30250,#30216,#16785,.T.);
#38819=EDGE_CURVE('',#30217,#30250,#16786,.T.);
#38820=EDGE_CURVE('',#30218,#30249,#444,.T.);
#38821=EDGE_CURVE('',#30251,#30211,#445,.T.);
#38822=EDGE_CURVE('',#30251,#30252,#16787,.T.);
#38823=EDGE_CURVE('',#30252,#30212,#16788,.T.);
#38824=EDGE_CURVE('',#30213,#30252,#16789,.T.);
#38825=EDGE_CURVE('',#30214,#30251,#446,.T.);
#38826=EDGE_CURVE('',#30253,#30207,#447,.T.);
#38827=EDGE_CURVE('',#30253,#30254,#16790,.T.);
#38828=EDGE_CURVE('',#30254,#30208,#16791,.T.);
#38829=EDGE_CURVE('',#30209,#30254,#16792,.T.);
#38830=EDGE_CURVE('',#30210,#30253,#448,.T.);
#38831=EDGE_CURVE('',#30255,#30203,#449,.T.);
#38832=EDGE_CURVE('',#30255,#30256,#16793,.T.);
#38833=EDGE_CURVE('',#30256,#30204,#16794,.T.);
#38834=EDGE_CURVE('',#30205,#30256,#16795,.T.);
#38835=EDGE_CURVE('',#30206,#30255,#450,.T.);
#38836=EDGE_CURVE('',#30257,#30199,#451,.T.);
#38837=EDGE_CURVE('',#30257,#30258,#16796,.T.);
#38838=EDGE_CURVE('',#30258,#30200,#16797,.T.);
#38839=EDGE_CURVE('',#30201,#30258,#16798,.T.);
#38840=EDGE_CURVE('',#30202,#30257,#452,.T.);
#38841=EDGE_CURVE('',#30259,#30195,#453,.T.);
#38842=EDGE_CURVE('',#30259,#30260,#16799,.T.);
#38843=EDGE_CURVE('',#30260,#30196,#16800,.T.);
#38844=EDGE_CURVE('',#30197,#30260,#16801,.T.);
#38845=EDGE_CURVE('',#30198,#30259,#454,.T.);
#38846=EDGE_CURVE('',#30261,#30191,#455,.T.);
#38847=EDGE_CURVE('',#30261,#30262,#16802,.T.);
#38848=EDGE_CURVE('',#30262,#30192,#16803,.T.);
#38849=EDGE_CURVE('',#30193,#30262,#16804,.T.);
#38850=EDGE_CURVE('',#30194,#30261,#456,.T.);
#38851=EDGE_CURVE('',#30263,#30187,#457,.T.);
#38852=EDGE_CURVE('',#30263,#30264,#16805,.T.);
#38853=EDGE_CURVE('',#30264,#30188,#16806,.T.);
#38854=EDGE_CURVE('',#30189,#30264,#16807,.T.);
#38855=EDGE_CURVE('',#30190,#30263,#458,.T.);
#38856=EDGE_CURVE('',#30265,#30183,#459,.T.);
#38857=EDGE_CURVE('',#30265,#30266,#16808,.T.);
#38858=EDGE_CURVE('',#30266,#30184,#16809,.T.);
#38859=EDGE_CURVE('',#30185,#30266,#16810,.T.);
#38860=EDGE_CURVE('',#30186,#30265,#460,.T.);
#38861=EDGE_CURVE('',#30267,#30179,#461,.T.);
#38862=EDGE_CURVE('',#30267,#30268,#16811,.T.);
#38863=EDGE_CURVE('',#30268,#30180,#16812,.T.);
#38864=EDGE_CURVE('',#30181,#30268,#16813,.T.);
#38865=EDGE_CURVE('',#30182,#30267,#462,.T.);
#38866=EDGE_CURVE('',#30269,#30175,#463,.T.);
#38867=EDGE_CURVE('',#30269,#30270,#16814,.T.);
#38868=EDGE_CURVE('',#30270,#30176,#16815,.T.);
#38869=EDGE_CURVE('',#30177,#30270,#16816,.T.);
#38870=EDGE_CURVE('',#30178,#30269,#464,.T.);
#38871=EDGE_CURVE('',#30271,#30168,#465,.T.);
#38872=EDGE_CURVE('',#30271,#30272,#16817,.T.);
#38873=EDGE_CURVE('',#30272,#30169,#16818,.T.);
#38874=EDGE_CURVE('',#30173,#30272,#16819,.T.);
#38875=EDGE_CURVE('',#30174,#30271,#466,.T.);
#38876=EDGE_CURVE('',#30273,#30164,#467,.T.);
#38877=EDGE_CURVE('',#30273,#30274,#16820,.T.);
#38878=EDGE_CURVE('',#30274,#30165,#16821,.T.);
#38879=EDGE_CURVE('',#30166,#30274,#16822,.T.);
#38880=EDGE_CURVE('',#30167,#30273,#468,.T.);
#38881=EDGE_CURVE('',#30275,#30160,#469,.T.);
#38882=EDGE_CURVE('',#30275,#30276,#16823,.T.);
#38883=EDGE_CURVE('',#30276,#30161,#16824,.T.);
#38884=EDGE_CURVE('',#30162,#30276,#16825,.T.);
#38885=EDGE_CURVE('',#30163,#30275,#470,.T.);
#38886=EDGE_CURVE('',#30277,#30156,#471,.T.);
#38887=EDGE_CURVE('',#30277,#30278,#16826,.T.);
#38888=EDGE_CURVE('',#30278,#30157,#16827,.T.);
#38889=EDGE_CURVE('',#30158,#30278,#16828,.T.);
#38890=EDGE_CURVE('',#30159,#30277,#472,.T.);
#38891=EDGE_CURVE('',#30279,#30152,#473,.T.);
#38892=EDGE_CURVE('',#30279,#30280,#16829,.T.);
#38893=EDGE_CURVE('',#30280,#30153,#16830,.T.);
#38894=EDGE_CURVE('',#30154,#30280,#16831,.T.);
#38895=EDGE_CURVE('',#30155,#30279,#474,.T.);
#38896=EDGE_CURVE('',#30281,#30148,#475,.T.);
#38897=EDGE_CURVE('',#30281,#30282,#16832,.T.);
#38898=EDGE_CURVE('',#30282,#30149,#16833,.T.);
#38899=EDGE_CURVE('',#30150,#30282,#16834,.T.);
#38900=EDGE_CURVE('',#30151,#30281,#476,.T.);
#38901=EDGE_CURVE('',#30283,#30144,#477,.T.);
#38902=EDGE_CURVE('',#30283,#30284,#16835,.T.);
#38903=EDGE_CURVE('',#30284,#30145,#16836,.T.);
#38904=EDGE_CURVE('',#30146,#30284,#16837,.T.);
#38905=EDGE_CURVE('',#30147,#30283,#478,.T.);
#38906=EDGE_CURVE('',#30285,#30140,#479,.T.);
#38907=EDGE_CURVE('',#30285,#30286,#16838,.T.);
#38908=EDGE_CURVE('',#30286,#30141,#16839,.T.);
#38909=EDGE_CURVE('',#30142,#30286,#16840,.T.);
#38910=EDGE_CURVE('',#30143,#30285,#480,.T.);
#38911=EDGE_CURVE('',#30287,#30136,#481,.T.);
#38912=EDGE_CURVE('',#30287,#30288,#16841,.T.);
#38913=EDGE_CURVE('',#30288,#30137,#16842,.T.);
#38914=EDGE_CURVE('',#30138,#30288,#16843,.T.);
#38915=EDGE_CURVE('',#30139,#30287,#482,.T.);
#38916=EDGE_CURVE('',#30289,#30132,#483,.T.);
#38917=EDGE_CURVE('',#30289,#30290,#16844,.T.);
#38918=EDGE_CURVE('',#30290,#30133,#16845,.T.);
#38919=EDGE_CURVE('',#30134,#30290,#16846,.T.);
#38920=EDGE_CURVE('',#30135,#30289,#484,.T.);
#38921=EDGE_CURVE('',#30291,#30128,#485,.T.);
#38922=EDGE_CURVE('',#30291,#30292,#16847,.T.);
#38923=EDGE_CURVE('',#30292,#30129,#16848,.T.);
#38924=EDGE_CURVE('',#30130,#30292,#16849,.T.);
#38925=EDGE_CURVE('',#30131,#30291,#486,.T.);
#38926=EDGE_CURVE('',#30293,#30124,#487,.T.);
#38927=EDGE_CURVE('',#30293,#30294,#16850,.T.);
#38928=EDGE_CURVE('',#30294,#30125,#16851,.T.);
#38929=EDGE_CURVE('',#30126,#30294,#16852,.T.);
#38930=EDGE_CURVE('',#30127,#30293,#488,.T.);
#38931=EDGE_CURVE('',#30295,#30120,#489,.T.);
#38932=EDGE_CURVE('',#30295,#30296,#16853,.T.);
#38933=EDGE_CURVE('',#30296,#30121,#16854,.T.);
#38934=EDGE_CURVE('',#30122,#30296,#16855,.T.);
#38935=EDGE_CURVE('',#30123,#30295,#490,.T.);
#38936=EDGE_CURVE('',#30297,#30116,#491,.T.);
#38937=EDGE_CURVE('',#30297,#30298,#16856,.T.);
#38938=EDGE_CURVE('',#30298,#30117,#16857,.T.);
#38939=EDGE_CURVE('',#30118,#30298,#16858,.T.);
#38940=EDGE_CURVE('',#30119,#30297,#492,.T.);
#38941=EDGE_CURVE('',#30299,#30112,#493,.T.);
#38942=EDGE_CURVE('',#30299,#30300,#16859,.T.);
#38943=EDGE_CURVE('',#30300,#30113,#16860,.T.);
#38944=EDGE_CURVE('',#30114,#30300,#16861,.T.);
#38945=EDGE_CURVE('',#30115,#30299,#494,.T.);
#38946=EDGE_CURVE('',#30301,#30108,#495,.T.);
#38947=EDGE_CURVE('',#30301,#30302,#16862,.T.);
#38948=EDGE_CURVE('',#30302,#30109,#16863,.T.);
#38949=EDGE_CURVE('',#30110,#30302,#16864,.T.);
#38950=EDGE_CURVE('',#30111,#30301,#496,.T.);
#38951=EDGE_CURVE('',#30303,#30104,#497,.T.);
#38952=EDGE_CURVE('',#30303,#30304,#16865,.T.);
#38953=EDGE_CURVE('',#30304,#30105,#16866,.T.);
#38954=EDGE_CURVE('',#30106,#30304,#16867,.T.);
#38955=EDGE_CURVE('',#30107,#30303,#498,.T.);
#38956=EDGE_CURVE('',#30305,#30100,#499,.T.);
#38957=EDGE_CURVE('',#30305,#30306,#16868,.T.);
#38958=EDGE_CURVE('',#30306,#30101,#16869,.T.);
#38959=EDGE_CURVE('',#30102,#30306,#16870,.T.);
#38960=EDGE_CURVE('',#30103,#30305,#500,.T.);
#38961=EDGE_CURVE('',#30307,#30096,#501,.T.);
#38962=EDGE_CURVE('',#30307,#30308,#16871,.T.);
#38963=EDGE_CURVE('',#30308,#30097,#16872,.T.);
#38964=EDGE_CURVE('',#30098,#30308,#16873,.T.);
#38965=EDGE_CURVE('',#30099,#30307,#502,.T.);
#38966=EDGE_CURVE('',#30172,#30088,#1517,.T.);
#38967=EDGE_CURVE('',#30309,#30309,#1518,.T.);
#38968=EDGE_CURVE('',#30309,#30271,#16874,.T.);
#38969=EDGE_CURVE('',#30310,#30310,#1519,.T.);
#38970=EDGE_CURVE('',#30310,#30311,#16875,.T.);
#38971=EDGE_CURVE('',#30312,#30311,#503,.T.);
#38972=EDGE_CURVE('',#30312,#30313,#1520,.T.);
#38973=EDGE_CURVE('',#30314,#30313,#504,.T.);
#38974=EDGE_CURVE('',#30315,#30314,#505,.T.);
#38975=EDGE_CURVE('',#30315,#30316,#1521,.T.);
#38976=EDGE_CURVE('',#30317,#30316,#506,.T.);
#38977=EDGE_CURVE('',#30318,#30317,#507,.T.);
#38978=EDGE_CURVE('',#30318,#30319,#1522,.T.);
#38979=EDGE_CURVE('',#30320,#30319,#508,.T.);
#38980=EDGE_CURVE('',#30321,#30320,#509,.T.);
#38981=EDGE_CURVE('',#30321,#30322,#1523,.T.);
#38982=EDGE_CURVE('',#30323,#30322,#510,.T.);
#38983=EDGE_CURVE('',#30324,#30323,#511,.T.);
#38984=EDGE_CURVE('',#30324,#30325,#1524,.T.);
#38985=EDGE_CURVE('',#30326,#30325,#512,.T.);
#38986=EDGE_CURVE('',#30327,#30326,#513,.T.);
#38987=EDGE_CURVE('',#30327,#30328,#1525,.T.);
#38988=EDGE_CURVE('',#30311,#30328,#514,.T.);
#38989=EDGE_CURVE('',#30316,#30329,#16876,.T.);
#38990=EDGE_CURVE('',#30330,#30315,#16877,.T.);
#38991=EDGE_CURVE('',#30329,#30330,#1526,.T.);
#38992=EDGE_CURVE('',#30319,#30331,#16878,.T.);
#38993=EDGE_CURVE('',#30332,#30318,#16879,.T.);
#38994=EDGE_CURVE('',#30331,#30332,#1527,.T.);
#38995=EDGE_CURVE('',#30333,#30312,#16880,.T.);
#38996=EDGE_CURVE('',#30334,#30333,#1528,.T.);
#38997=EDGE_CURVE('',#30313,#30334,#16881,.T.);
#38998=EDGE_CURVE('',#30322,#30335,#16882,.T.);
#38999=EDGE_CURVE('',#30336,#30321,#16883,.T.);
#39000=EDGE_CURVE('',#30335,#30336,#1529,.T.);
#39001=EDGE_CURVE('',#30337,#30327,#16884,.T.);
#39002=EDGE_CURVE('',#30338,#30337,#1530,.T.);
#39003=EDGE_CURVE('',#30328,#30338,#16885,.T.);
#39004=EDGE_CURVE('',#30339,#30324,#16886,.T.);
#39005=EDGE_CURVE('',#30340,#30339,#1531,.T.);
#39006=EDGE_CURVE('',#30325,#30340,#16887,.T.);
#39007=EDGE_CURVE('',#30336,#30335,#16888,.T.);
#39008=EDGE_CURVE('',#30320,#30341,#16889,.T.);
#39009=EDGE_CURVE('',#30341,#30342,#16890,.T.);
#39010=EDGE_CURVE('',#30323,#30342,#16891,.T.);
#39011=EDGE_CURVE('',#30332,#30331,#16892,.T.);
#39012=EDGE_CURVE('',#30317,#30343,#16893,.T.);
#39013=EDGE_CURVE('',#30343,#30341,#16894,.T.);
#39014=EDGE_CURVE('',#30330,#30329,#16895,.T.);
#39015=EDGE_CURVE('',#30314,#30344,#16896,.T.);
#39016=EDGE_CURVE('',#30344,#30343,#16897,.T.);
#39017=EDGE_CURVE('',#30333,#30334,#16898,.T.);
#39018=EDGE_CURVE('',#30337,#30338,#16899,.T.);
#39019=EDGE_CURVE('',#30339,#30340,#16900,.T.);
#39020=EDGE_CURVE('',#30345,#30344,#16901,.T.);
#39021=EDGE_CURVE('',#30345,#30344,#1532,.T.);
#39022=EDGE_CURVE('',#30344,#30343,#1533,.T.);
#39023=EDGE_CURVE('',#30343,#30341,#1534,.T.);
#39024=EDGE_CURVE('',#30341,#30342,#1535,.T.);
#39025=EDGE_CURVE('',#30342,#30346,#16902,.T.);
#39026=EDGE_CURVE('',#30342,#30346,#1536,.T.);
#39027=EDGE_CURVE('',#30346,#30345,#16903,.T.);
#39028=EDGE_CURVE('',#30346,#30345,#1537,.T.);
#39029=EDGE_CURVE('',#30345,#30347,#16904,.T.);
#39030=EDGE_CURVE('',#30311,#30345,#16905,.T.);
#39031=EDGE_CURVE('',#30326,#30346,#16906,.T.);
#55419=ORIENTED_EDGE('',*,*,#38542,.F.);
#55420=ORIENTED_EDGE('',*,*,#38543,.T.);
#55421=ORIENTED_EDGE('',*,*,#38544,.F.);
#55422=ORIENTED_EDGE('',*,*,#38545,.T.);
#55423=ORIENTED_EDGE('',*,*,#38546,.F.);
#55424=ORIENTED_EDGE('',*,*,#38547,.T.);
#55425=ORIENTED_EDGE('',*,*,#38542,.T.);
#55426=ORIENTED_EDGE('',*,*,#38548,.T.);
#55427=ORIENTED_EDGE('',*,*,#38549,.F.);
#55428=ORIENTED_EDGE('',*,*,#38550,.T.);
#55429=ORIENTED_EDGE('',*,*,#38546,.T.);
#55430=ORIENTED_EDGE('',*,*,#38551,.T.);
#55431=ORIENTED_EDGE('',*,*,#38552,.F.);
#55432=ORIENTED_EDGE('',*,*,#38553,.T.);
#55433=ORIENTED_EDGE('',*,*,#38549,.T.);
#55434=ORIENTED_EDGE('',*,*,#38554,.T.);
#55435=ORIENTED_EDGE('',*,*,#38555,.F.);
#55436=ORIENTED_EDGE('',*,*,#38556,.T.);
#55437=ORIENTED_EDGE('',*,*,#38552,.T.);
#55438=ORIENTED_EDGE('',*,*,#38557,.T.);
#55439=ORIENTED_EDGE('',*,*,#38558,.F.);
#55440=ORIENTED_EDGE('',*,*,#38559,.T.);
#55441=ORIENTED_EDGE('',*,*,#38555,.T.);
#55442=ORIENTED_EDGE('',*,*,#38560,.T.);
#55443=ORIENTED_EDGE('',*,*,#38561,.F.);
#55444=ORIENTED_EDGE('',*,*,#38562,.T.);
#55445=ORIENTED_EDGE('',*,*,#38558,.T.);
#55446=ORIENTED_EDGE('',*,*,#38563,.T.);
#55447=ORIENTED_EDGE('',*,*,#38564,.F.);
#55448=ORIENTED_EDGE('',*,*,#38565,.T.);
#55449=ORIENTED_EDGE('',*,*,#38561,.T.);
#55450=ORIENTED_EDGE('',*,*,#38566,.T.);
#55451=ORIENTED_EDGE('',*,*,#38567,.F.);
#55452=ORIENTED_EDGE('',*,*,#38568,.T.);
#55453=ORIENTED_EDGE('',*,*,#38564,.T.);
#55454=ORIENTED_EDGE('',*,*,#38569,.T.);
#55455=ORIENTED_EDGE('',*,*,#38570,.F.);
#55456=ORIENTED_EDGE('',*,*,#38571,.T.);
#55457=ORIENTED_EDGE('',*,*,#38567,.T.);
#55458=ORIENTED_EDGE('',*,*,#38572,.T.);
#55459=ORIENTED_EDGE('',*,*,#38573,.F.);
#55460=ORIENTED_EDGE('',*,*,#38574,.T.);
#55461=ORIENTED_EDGE('',*,*,#38570,.T.);
#55462=ORIENTED_EDGE('',*,*,#38575,.T.);
#55463=ORIENTED_EDGE('',*,*,#38576,.F.);
#55464=ORIENTED_EDGE('',*,*,#38577,.T.);
#55465=ORIENTED_EDGE('',*,*,#38573,.T.);
#55466=ORIENTED_EDGE('',*,*,#38578,.T.);
#55467=ORIENTED_EDGE('',*,*,#38579,.F.);
#55468=ORIENTED_EDGE('',*,*,#38580,.T.);
#55469=ORIENTED_EDGE('',*,*,#38576,.T.);
#55470=ORIENTED_EDGE('',*,*,#38581,.T.);
#55471=ORIENTED_EDGE('',*,*,#38582,.F.);
#55472=ORIENTED_EDGE('',*,*,#38583,.T.);
#55473=ORIENTED_EDGE('',*,*,#38584,.F.);
#55474=ORIENTED_EDGE('',*,*,#38585,.F.);
#55475=ORIENTED_EDGE('',*,*,#38586,.F.);
#55476=ORIENTED_EDGE('',*,*,#38587,.T.);
#55477=ORIENTED_EDGE('',*,*,#38582,.T.);
#55478=ORIENTED_EDGE('',*,*,#38588,.F.);
#55479=ORIENTED_EDGE('',*,*,#38589,.F.);
#55480=ORIENTED_EDGE('',*,*,#38590,.T.);
#55481=ORIENTED_EDGE('',*,*,#38586,.T.);
#55482=ORIENTED_EDGE('',*,*,#38591,.F.);
#55483=ORIENTED_EDGE('',*,*,#38592,.F.);
#55484=ORIENTED_EDGE('',*,*,#38593,.T.);
#55485=ORIENTED_EDGE('',*,*,#38589,.T.);
#55486=ORIENTED_EDGE('',*,*,#38594,.F.);
#55487=ORIENTED_EDGE('',*,*,#38595,.F.);
#55488=ORIENTED_EDGE('',*,*,#38596,.T.);
#55489=ORIENTED_EDGE('',*,*,#38592,.T.);
#55490=ORIENTED_EDGE('',*,*,#38597,.F.);
#55491=ORIENTED_EDGE('',*,*,#38598,.F.);
#55492=ORIENTED_EDGE('',*,*,#38599,.T.);
#55493=ORIENTED_EDGE('',*,*,#38595,.T.);
#55494=ORIENTED_EDGE('',*,*,#38600,.F.);
#55495=ORIENTED_EDGE('',*,*,#38601,.F.);
#55496=ORIENTED_EDGE('',*,*,#38602,.T.);
#55497=ORIENTED_EDGE('',*,*,#38598,.T.);
#55498=ORIENTED_EDGE('',*,*,#38603,.F.);
#55499=ORIENTED_EDGE('',*,*,#38604,.F.);
#55500=ORIENTED_EDGE('',*,*,#38605,.T.);
#55501=ORIENTED_EDGE('',*,*,#38601,.T.);
#55502=ORIENTED_EDGE('',*,*,#38606,.F.);
#55503=ORIENTED_EDGE('',*,*,#38607,.F.);
#55504=ORIENTED_EDGE('',*,*,#38608,.T.);
#55505=ORIENTED_EDGE('',*,*,#38604,.T.);
#55506=ORIENTED_EDGE('',*,*,#38609,.F.);
#55507=ORIENTED_EDGE('',*,*,#38610,.F.);
#55508=ORIENTED_EDGE('',*,*,#38611,.T.);
#55509=ORIENTED_EDGE('',*,*,#38607,.T.);
#55510=ORIENTED_EDGE('',*,*,#38612,.F.);
#55511=ORIENTED_EDGE('',*,*,#38613,.F.);
#55512=ORIENTED_EDGE('',*,*,#38614,.T.);
#55513=ORIENTED_EDGE('',*,*,#38610,.T.);
#55514=ORIENTED_EDGE('',*,*,#38615,.F.);
#55515=ORIENTED_EDGE('',*,*,#38616,.F.);
#55516=ORIENTED_EDGE('',*,*,#38617,.T.);
#55517=ORIENTED_EDGE('',*,*,#38613,.T.);
#55518=ORIENTED_EDGE('',*,*,#38618,.F.);
#55519=ORIENTED_EDGE('',*,*,#38584,.T.);
#55520=ORIENTED_EDGE('',*,*,#38619,.T.);
#55521=ORIENTED_EDGE('',*,*,#38620,.F.);
#55522=ORIENTED_EDGE('',*,*,#38621,.F.);
#55523=ORIENTED_EDGE('',*,*,#38622,.T.);
#55524=ORIENTED_EDGE('',*,*,#38622,.F.);
#55525=ORIENTED_EDGE('',*,*,#38623,.F.);
#55526=ORIENTED_EDGE('',*,*,#38581,.F.);
#55527=ORIENTED_EDGE('',*,*,#38578,.F.);
#55528=ORIENTED_EDGE('',*,*,#38575,.F.);
#55529=ORIENTED_EDGE('',*,*,#38572,.F.);
#55530=ORIENTED_EDGE('',*,*,#38569,.F.);
#55531=ORIENTED_EDGE('',*,*,#38566,.F.);
#55532=ORIENTED_EDGE('',*,*,#38563,.F.);
#55533=ORIENTED_EDGE('',*,*,#38560,.F.);
#55534=ORIENTED_EDGE('',*,*,#38557,.F.);
#55535=ORIENTED_EDGE('',*,*,#38554,.F.);
#55536=ORIENTED_EDGE('',*,*,#38551,.F.);
#55537=ORIENTED_EDGE('',*,*,#38548,.F.);
#55538=ORIENTED_EDGE('',*,*,#38545,.F.);
#55539=ORIENTED_EDGE('',*,*,#38624,.F.);
#55540=ORIENTED_EDGE('',*,*,#38625,.T.);
#55541=ORIENTED_EDGE('',*,*,#38618,.T.);
#55542=ORIENTED_EDGE('',*,*,#38615,.T.);
#55543=ORIENTED_EDGE('',*,*,#38612,.T.);
#55544=ORIENTED_EDGE('',*,*,#38609,.T.);
#55545=ORIENTED_EDGE('',*,*,#38606,.T.);
#55546=ORIENTED_EDGE('',*,*,#38603,.T.);
#55547=ORIENTED_EDGE('',*,*,#38600,.T.);
#55548=ORIENTED_EDGE('',*,*,#38597,.T.);
#55549=ORIENTED_EDGE('',*,*,#38594,.T.);
#55550=ORIENTED_EDGE('',*,*,#38591,.T.);
#55551=ORIENTED_EDGE('',*,*,#38588,.T.);
#55552=ORIENTED_EDGE('',*,*,#38585,.T.);
#55553=ORIENTED_EDGE('',*,*,#38626,.F.);
#55554=ORIENTED_EDGE('',*,*,#38627,.T.);
#55555=ORIENTED_EDGE('',*,*,#38628,.T.);
#55556=ORIENTED_EDGE('',*,*,#38624,.T.);
#55557=ORIENTED_EDGE('',*,*,#38629,.F.);
#55558=ORIENTED_EDGE('',*,*,#38616,.T.);
#55559=ORIENTED_EDGE('',*,*,#38625,.F.);
#55560=ORIENTED_EDGE('',*,*,#38628,.F.);
#55561=ORIENTED_EDGE('',*,*,#38630,.T.);
#55562=ORIENTED_EDGE('',*,*,#38619,.F.);
#55563=ORIENTED_EDGE('',*,*,#38583,.F.);
#55564=ORIENTED_EDGE('',*,*,#38587,.F.);
#55565=ORIENTED_EDGE('',*,*,#38590,.F.);
#55566=ORIENTED_EDGE('',*,*,#38593,.F.);
#55567=ORIENTED_EDGE('',*,*,#38596,.F.);
#55568=ORIENTED_EDGE('',*,*,#38599,.F.);
#55569=ORIENTED_EDGE('',*,*,#38602,.F.);
#55570=ORIENTED_EDGE('',*,*,#38605,.F.);
#55571=ORIENTED_EDGE('',*,*,#38608,.F.);
#55572=ORIENTED_EDGE('',*,*,#38611,.F.);
#55573=ORIENTED_EDGE('',*,*,#38614,.F.);
#55574=ORIENTED_EDGE('',*,*,#38617,.F.);
#55575=ORIENTED_EDGE('',*,*,#38630,.F.);
#55576=ORIENTED_EDGE('',*,*,#38627,.F.);
#55577=ORIENTED_EDGE('',*,*,#38543,.F.);
#55578=ORIENTED_EDGE('',*,*,#38547,.F.);
#55579=ORIENTED_EDGE('',*,*,#38550,.F.);
#55580=ORIENTED_EDGE('',*,*,#38553,.F.);
#55581=ORIENTED_EDGE('',*,*,#38556,.F.);
#55582=ORIENTED_EDGE('',*,*,#38559,.F.);
#55583=ORIENTED_EDGE('',*,*,#38562,.F.);
#55584=ORIENTED_EDGE('',*,*,#38565,.F.);
#55585=ORIENTED_EDGE('',*,*,#38568,.F.);
#55586=ORIENTED_EDGE('',*,*,#38571,.F.);
#55587=ORIENTED_EDGE('',*,*,#38574,.F.);
#55588=ORIENTED_EDGE('',*,*,#38577,.F.);
#55589=ORIENTED_EDGE('',*,*,#38580,.F.);
#55590=ORIENTED_EDGE('',*,*,#38631,.F.);
#55591=ORIENTED_EDGE('',*,*,#38626,.T.);
#55592=ORIENTED_EDGE('',*,*,#38632,.T.);
#55593=ORIENTED_EDGE('',*,*,#38633,.T.);
#55594=ORIENTED_EDGE('',*,*,#38632,.F.);
#55595=ORIENTED_EDGE('',*,*,#38629,.T.);
#55596=ORIENTED_EDGE('',*,*,#38544,.T.);
#55597=ORIENTED_EDGE('',*,*,#38579,.T.);
#55598=ORIENTED_EDGE('',*,*,#38623,.T.);
#55599=ORIENTED_EDGE('',*,*,#38634,.F.);
#55600=ORIENTED_EDGE('',*,*,#38631,.T.);
#55601=ORIENTED_EDGE('',*,*,#38635,.F.);
#55602=ORIENTED_EDGE('',*,*,#38633,.F.);
#55603=ORIENTED_EDGE('',*,*,#38621,.T.);
#55604=ORIENTED_EDGE('',*,*,#38636,.T.);
#55605=ORIENTED_EDGE('',*,*,#38637,.T.);
#55606=ORIENTED_EDGE('',*,*,#38636,.F.);
#55607=ORIENTED_EDGE('',*,*,#38620,.T.);
#55608=ORIENTED_EDGE('',*,*,#38634,.T.);
#55609=ORIENTED_EDGE('',*,*,#38637,.F.);
#55610=ORIENTED_EDGE('',*,*,#38638,.F.);
#55611=ORIENTED_EDGE('',*,*,#38639,.T.);
#55612=ORIENTED_EDGE('',*,*,#38640,.T.);
#55613=ORIENTED_EDGE('',*,*,#38641,.F.);
#55614=ORIENTED_EDGE('',*,*,#38642,.F.);
#55615=ORIENTED_EDGE('',*,*,#38640,.F.);
#55616=ORIENTED_EDGE('',*,*,#38643,.F.);
#55617=ORIENTED_EDGE('',*,*,#38644,.F.);
#55618=ORIENTED_EDGE('',*,*,#38645,.F.);
#55619=ORIENTED_EDGE('',*,*,#38643,.T.);
#55620=ORIENTED_EDGE('',*,*,#38639,.F.);
#55621=ORIENTED_EDGE('',*,*,#38641,.T.);
#55622=ORIENTED_EDGE('',*,*,#38642,.T.);
#55623=ORIENTED_EDGE('',*,*,#38645,.T.);
#55624=ORIENTED_EDGE('',*,*,#38646,.F.);
#55625=ORIENTED_EDGE('',*,*,#38647,.T.);
#55626=ORIENTED_EDGE('',*,*,#38648,.T.);
#55627=ORIENTED_EDGE('',*,*,#38649,.T.);
#55628=ORIENTED_EDGE('',*,*,#38650,.F.);
#55629=ORIENTED_EDGE('',*,*,#38651,.T.);
#55630=ORIENTED_EDGE('',*,*,#38652,.T.);
#55631=ORIENTED_EDGE('',*,*,#38653,.T.);
#55632=ORIENTED_EDGE('',*,*,#38654,.F.);
#55633=ORIENTED_EDGE('',*,*,#38655,.T.);
#55634=ORIENTED_EDGE('',*,*,#38656,.T.);
#55635=ORIENTED_EDGE('',*,*,#38657,.T.);
#55636=ORIENTED_EDGE('',*,*,#38658,.F.);
#55637=ORIENTED_EDGE('',*,*,#38659,.T.);
#55638=ORIENTED_EDGE('',*,*,#38660,.T.);
#55639=ORIENTED_EDGE('',*,*,#38661,.T.);
#55640=ORIENTED_EDGE('',*,*,#38662,.F.);
#55641=ORIENTED_EDGE('',*,*,#38663,.T.);
#55642=ORIENTED_EDGE('',*,*,#38664,.T.);
#55643=ORIENTED_EDGE('',*,*,#38665,.T.);
#55644=ORIENTED_EDGE('',*,*,#38666,.F.);
#55645=ORIENTED_EDGE('',*,*,#38667,.T.);
#55646=ORIENTED_EDGE('',*,*,#38668,.T.);
#55647=ORIENTED_EDGE('',*,*,#38669,.T.);
#55648=ORIENTED_EDGE('',*,*,#38670,.F.);
#55649=ORIENTED_EDGE('',*,*,#38671,.T.);
#55650=ORIENTED_EDGE('',*,*,#38672,.T.);
#55651=ORIENTED_EDGE('',*,*,#38673,.T.);
#55652=ORIENTED_EDGE('',*,*,#38674,.F.);
#55653=ORIENTED_EDGE('',*,*,#38675,.T.);
#55654=ORIENTED_EDGE('',*,*,#38676,.T.);
#55655=ORIENTED_EDGE('',*,*,#38677,.T.);
#55656=ORIENTED_EDGE('',*,*,#38678,.F.);
#55657=ORIENTED_EDGE('',*,*,#38679,.T.);
#55658=ORIENTED_EDGE('',*,*,#38680,.T.);
#55659=ORIENTED_EDGE('',*,*,#38681,.T.);
#55660=ORIENTED_EDGE('',*,*,#38682,.F.);
#55661=ORIENTED_EDGE('',*,*,#38683,.T.);
#55662=ORIENTED_EDGE('',*,*,#38684,.T.);
#55663=ORIENTED_EDGE('',*,*,#38685,.T.);
#55664=ORIENTED_EDGE('',*,*,#38686,.F.);
#55665=ORIENTED_EDGE('',*,*,#38687,.T.);
#55666=ORIENTED_EDGE('',*,*,#38688,.T.);
#55667=ORIENTED_EDGE('',*,*,#38689,.T.);
#55668=ORIENTED_EDGE('',*,*,#38690,.F.);
#55669=ORIENTED_EDGE('',*,*,#38691,.T.);
#55670=ORIENTED_EDGE('',*,*,#38692,.T.);
#55671=ORIENTED_EDGE('',*,*,#38693,.T.);
#55672=ORIENTED_EDGE('',*,*,#38694,.F.);
#55673=ORIENTED_EDGE('',*,*,#38695,.T.);
#55674=ORIENTED_EDGE('',*,*,#38696,.T.);
#55675=ORIENTED_EDGE('',*,*,#38697,.T.);
#55676=ORIENTED_EDGE('',*,*,#38698,.F.);
#55677=ORIENTED_EDGE('',*,*,#38699,.T.);
#55678=ORIENTED_EDGE('',*,*,#38700,.T.);
#55679=ORIENTED_EDGE('',*,*,#38701,.T.);
#55680=ORIENTED_EDGE('',*,*,#38702,.F.);
#55681=ORIENTED_EDGE('',*,*,#38703,.T.);
#55682=ORIENTED_EDGE('',*,*,#38704,.T.);
#55683=ORIENTED_EDGE('',*,*,#38705,.T.);
#55684=ORIENTED_EDGE('',*,*,#38706,.F.);
#55685=ORIENTED_EDGE('',*,*,#38707,.T.);
#55686=ORIENTED_EDGE('',*,*,#38708,.T.);
#55687=ORIENTED_EDGE('',*,*,#38709,.T.);
#55688=ORIENTED_EDGE('',*,*,#38710,.F.);
#55689=ORIENTED_EDGE('',*,*,#38711,.T.);
#55690=ORIENTED_EDGE('',*,*,#38712,.T.);
#55691=ORIENTED_EDGE('',*,*,#38713,.T.);
#55692=ORIENTED_EDGE('',*,*,#38714,.F.);
#55693=ORIENTED_EDGE('',*,*,#38715,.T.);
#55694=ORIENTED_EDGE('',*,*,#38716,.T.);
#55695=ORIENTED_EDGE('',*,*,#38717,.T.);
#55696=ORIENTED_EDGE('',*,*,#38718,.F.);
#55697=ORIENTED_EDGE('',*,*,#38719,.T.);
#55698=ORIENTED_EDGE('',*,*,#38720,.T.);
#55699=ORIENTED_EDGE('',*,*,#38721,.T.);
#55700=ORIENTED_EDGE('',*,*,#38722,.F.);
#55701=ORIENTED_EDGE('',*,*,#38723,.F.);
#55702=ORIENTED_EDGE('',*,*,#38721,.F.);
#55703=ORIENTED_EDGE('',*,*,#38724,.T.);
#55704=ORIENTED_EDGE('',*,*,#38725,.T.);
#55705=ORIENTED_EDGE('',*,*,#38726,.F.);
#55706=ORIENTED_EDGE('',*,*,#38727,.T.);
#55707=ORIENTED_EDGE('',*,*,#38728,.T.);
#55708=ORIENTED_EDGE('',*,*,#38729,.T.);
#55709=ORIENTED_EDGE('',*,*,#38730,.F.);
#55710=ORIENTED_EDGE('',*,*,#38731,.T.);
#55711=ORIENTED_EDGE('',*,*,#38732,.T.);
#55712=ORIENTED_EDGE('',*,*,#38733,.T.);
#55713=ORIENTED_EDGE('',*,*,#38734,.F.);
#55714=ORIENTED_EDGE('',*,*,#38735,.T.);
#55715=ORIENTED_EDGE('',*,*,#38736,.T.);
#55716=ORIENTED_EDGE('',*,*,#38737,.T.);
#55717=ORIENTED_EDGE('',*,*,#38738,.F.);
#55718=ORIENTED_EDGE('',*,*,#38739,.T.);
#55719=ORIENTED_EDGE('',*,*,#38740,.T.);
#55720=ORIENTED_EDGE('',*,*,#38741,.T.);
#55721=ORIENTED_EDGE('',*,*,#38742,.F.);
#55722=ORIENTED_EDGE('',*,*,#38743,.T.);
#55723=ORIENTED_EDGE('',*,*,#38744,.T.);
#55724=ORIENTED_EDGE('',*,*,#38745,.T.);
#55725=ORIENTED_EDGE('',*,*,#38746,.F.);
#55726=ORIENTED_EDGE('',*,*,#38747,.T.);
#55727=ORIENTED_EDGE('',*,*,#38748,.T.);
#55728=ORIENTED_EDGE('',*,*,#38749,.T.);
#55729=ORIENTED_EDGE('',*,*,#38750,.F.);
#55730=ORIENTED_EDGE('',*,*,#38751,.T.);
#55731=ORIENTED_EDGE('',*,*,#38752,.T.);
#55732=ORIENTED_EDGE('',*,*,#38753,.T.);
#55733=ORIENTED_EDGE('',*,*,#38754,.F.);
#55734=ORIENTED_EDGE('',*,*,#38755,.T.);
#55735=ORIENTED_EDGE('',*,*,#38756,.T.);
#55736=ORIENTED_EDGE('',*,*,#38757,.T.);
#55737=ORIENTED_EDGE('',*,*,#38758,.F.);
#55738=ORIENTED_EDGE('',*,*,#38759,.T.);
#55739=ORIENTED_EDGE('',*,*,#38760,.T.);
#55740=ORIENTED_EDGE('',*,*,#38761,.T.);
#55741=ORIENTED_EDGE('',*,*,#38762,.F.);
#55742=ORIENTED_EDGE('',*,*,#38763,.T.);
#55743=ORIENTED_EDGE('',*,*,#38764,.T.);
#55744=ORIENTED_EDGE('',*,*,#38765,.T.);
#55745=ORIENTED_EDGE('',*,*,#38766,.F.);
#55746=ORIENTED_EDGE('',*,*,#38767,.T.);
#55747=ORIENTED_EDGE('',*,*,#38768,.T.);
#55748=ORIENTED_EDGE('',*,*,#38769,.T.);
#55749=ORIENTED_EDGE('',*,*,#38770,.F.);
#55750=ORIENTED_EDGE('',*,*,#38771,.T.);
#55751=ORIENTED_EDGE('',*,*,#38772,.T.);
#55752=ORIENTED_EDGE('',*,*,#38773,.T.);
#55753=ORIENTED_EDGE('',*,*,#38774,.F.);
#55754=ORIENTED_EDGE('',*,*,#38775,.T.);
#55755=ORIENTED_EDGE('',*,*,#38776,.T.);
#55756=ORIENTED_EDGE('',*,*,#38777,.T.);
#55757=ORIENTED_EDGE('',*,*,#38778,.F.);
#55758=ORIENTED_EDGE('',*,*,#38779,.T.);
#55759=ORIENTED_EDGE('',*,*,#38780,.T.);
#55760=ORIENTED_EDGE('',*,*,#38781,.T.);
#55761=ORIENTED_EDGE('',*,*,#38782,.F.);
#55762=ORIENTED_EDGE('',*,*,#38783,.T.);
#55763=ORIENTED_EDGE('',*,*,#38784,.T.);
#55764=ORIENTED_EDGE('',*,*,#38785,.T.);
#55765=ORIENTED_EDGE('',*,*,#38786,.F.);
#55766=ORIENTED_EDGE('',*,*,#38787,.T.);
#55767=ORIENTED_EDGE('',*,*,#38788,.T.);
#55768=ORIENTED_EDGE('',*,*,#38789,.T.);
#55769=ORIENTED_EDGE('',*,*,#38790,.F.);
#55770=ORIENTED_EDGE('',*,*,#38791,.F.);
#55771=ORIENTED_EDGE('',*,*,#38792,.T.);
#55772=ORIENTED_EDGE('',*,*,#38793,.T.);
#55773=ORIENTED_EDGE('',*,*,#38787,.F.);
#55774=ORIENTED_EDGE('',*,*,#38788,.F.);
#55775=ORIENTED_EDGE('',*,*,#38793,.F.);
#55776=ORIENTED_EDGE('',*,*,#38794,.F.);
#55777=ORIENTED_EDGE('',*,*,#38795,.F.);
#55778=ORIENTED_EDGE('',*,*,#38789,.F.);
#55779=ORIENTED_EDGE('',*,*,#38794,.T.);
#55780=ORIENTED_EDGE('',*,*,#38792,.F.);
#55781=ORIENTED_EDGE('',*,*,#38796,.F.);
#55782=ORIENTED_EDGE('',*,*,#38797,.T.);
#55783=ORIENTED_EDGE('',*,*,#38798,.T.);
#55784=ORIENTED_EDGE('',*,*,#38783,.F.);
#55785=ORIENTED_EDGE('',*,*,#38784,.F.);
#55786=ORIENTED_EDGE('',*,*,#38798,.F.);
#55787=ORIENTED_EDGE('',*,*,#38799,.F.);
#55788=ORIENTED_EDGE('',*,*,#38800,.F.);
#55789=ORIENTED_EDGE('',*,*,#38785,.F.);
#55790=ORIENTED_EDGE('',*,*,#38799,.T.);
#55791=ORIENTED_EDGE('',*,*,#38797,.F.);
#55792=ORIENTED_EDGE('',*,*,#38801,.F.);
#55793=ORIENTED_EDGE('',*,*,#38802,.T.);
#55794=ORIENTED_EDGE('',*,*,#38803,.T.);
#55795=ORIENTED_EDGE('',*,*,#38779,.F.);
#55796=ORIENTED_EDGE('',*,*,#38780,.F.);
#55797=ORIENTED_EDGE('',*,*,#38803,.F.);
#55798=ORIENTED_EDGE('',*,*,#38804,.F.);
#55799=ORIENTED_EDGE('',*,*,#38805,.F.);
#55800=ORIENTED_EDGE('',*,*,#38781,.F.);
#55801=ORIENTED_EDGE('',*,*,#38804,.T.);
#55802=ORIENTED_EDGE('',*,*,#38802,.F.);
#55803=ORIENTED_EDGE('',*,*,#38806,.F.);
#55804=ORIENTED_EDGE('',*,*,#38807,.T.);
#55805=ORIENTED_EDGE('',*,*,#38808,.T.);
#55806=ORIENTED_EDGE('',*,*,#38775,.F.);
#55807=ORIENTED_EDGE('',*,*,#38776,.F.);
#55808=ORIENTED_EDGE('',*,*,#38808,.F.);
#55809=ORIENTED_EDGE('',*,*,#38809,.F.);
#55810=ORIENTED_EDGE('',*,*,#38810,.F.);
#55811=ORIENTED_EDGE('',*,*,#38777,.F.);
#55812=ORIENTED_EDGE('',*,*,#38809,.T.);
#55813=ORIENTED_EDGE('',*,*,#38807,.F.);
#55814=ORIENTED_EDGE('',*,*,#38811,.F.);
#55815=ORIENTED_EDGE('',*,*,#38812,.T.);
#55816=ORIENTED_EDGE('',*,*,#38813,.T.);
#55817=ORIENTED_EDGE('',*,*,#38771,.F.);
#55818=ORIENTED_EDGE('',*,*,#38772,.F.);
#55819=ORIENTED_EDGE('',*,*,#38813,.F.);
#55820=ORIENTED_EDGE('',*,*,#38814,.F.);
#55821=ORIENTED_EDGE('',*,*,#38815,.F.);
#55822=ORIENTED_EDGE('',*,*,#38773,.F.);
#55823=ORIENTED_EDGE('',*,*,#38814,.T.);
#55824=ORIENTED_EDGE('',*,*,#38812,.F.);
#55825=ORIENTED_EDGE('',*,*,#38816,.F.);
#55826=ORIENTED_EDGE('',*,*,#38817,.T.);
#55827=ORIENTED_EDGE('',*,*,#38818,.T.);
#55828=ORIENTED_EDGE('',*,*,#38767,.F.);
#55829=ORIENTED_EDGE('',*,*,#38768,.F.);
#55830=ORIENTED_EDGE('',*,*,#38818,.F.);
#55831=ORIENTED_EDGE('',*,*,#38819,.F.);
#55832=ORIENTED_EDGE('',*,*,#38820,.F.);
#55833=ORIENTED_EDGE('',*,*,#38769,.F.);
#55834=ORIENTED_EDGE('',*,*,#38819,.T.);
#55835=ORIENTED_EDGE('',*,*,#38817,.F.);
#55836=ORIENTED_EDGE('',*,*,#38821,.F.);
#55837=ORIENTED_EDGE('',*,*,#38822,.T.);
#55838=ORIENTED_EDGE('',*,*,#38823,.T.);
#55839=ORIENTED_EDGE('',*,*,#38763,.F.);
#55840=ORIENTED_EDGE('',*,*,#38764,.F.);
#55841=ORIENTED_EDGE('',*,*,#38823,.F.);
#55842=ORIENTED_EDGE('',*,*,#38824,.F.);
#55843=ORIENTED_EDGE('',*,*,#38825,.F.);
#55844=ORIENTED_EDGE('',*,*,#38765,.F.);
#55845=ORIENTED_EDGE('',*,*,#38824,.T.);
#55846=ORIENTED_EDGE('',*,*,#38822,.F.);
#55847=ORIENTED_EDGE('',*,*,#38826,.F.);
#55848=ORIENTED_EDGE('',*,*,#38827,.T.);
#55849=ORIENTED_EDGE('',*,*,#38828,.T.);
#55850=ORIENTED_EDGE('',*,*,#38759,.F.);
#55851=ORIENTED_EDGE('',*,*,#38760,.F.);
#55852=ORIENTED_EDGE('',*,*,#38828,.F.);
#55853=ORIENTED_EDGE('',*,*,#38829,.F.);
#55854=ORIENTED_EDGE('',*,*,#38830,.F.);
#55855=ORIENTED_EDGE('',*,*,#38761,.F.);
#55856=ORIENTED_EDGE('',*,*,#38829,.T.);
#55857=ORIENTED_EDGE('',*,*,#38827,.F.);
#55858=ORIENTED_EDGE('',*,*,#38831,.F.);
#55859=ORIENTED_EDGE('',*,*,#38832,.T.);
#55860=ORIENTED_EDGE('',*,*,#38833,.T.);
#55861=ORIENTED_EDGE('',*,*,#38755,.F.);
#55862=ORIENTED_EDGE('',*,*,#38756,.F.);
#55863=ORIENTED_EDGE('',*,*,#38833,.F.);
#55864=ORIENTED_EDGE('',*,*,#38834,.F.);
#55865=ORIENTED_EDGE('',*,*,#38835,.F.);
#55866=ORIENTED_EDGE('',*,*,#38757,.F.);
#55867=ORIENTED_EDGE('',*,*,#38834,.T.);
#55868=ORIENTED_EDGE('',*,*,#38832,.F.);
#55869=ORIENTED_EDGE('',*,*,#38836,.F.);
#55870=ORIENTED_EDGE('',*,*,#38837,.T.);
#55871=ORIENTED_EDGE('',*,*,#38838,.T.);
#55872=ORIENTED_EDGE('',*,*,#38751,.F.);
#55873=ORIENTED_EDGE('',*,*,#38752,.F.);
#55874=ORIENTED_EDGE('',*,*,#38838,.F.);
#55875=ORIENTED_EDGE('',*,*,#38839,.F.);
#55876=ORIENTED_EDGE('',*,*,#38840,.F.);
#55877=ORIENTED_EDGE('',*,*,#38753,.F.);
#55878=ORIENTED_EDGE('',*,*,#38839,.T.);
#55879=ORIENTED_EDGE('',*,*,#38837,.F.);
#55880=ORIENTED_EDGE('',*,*,#38841,.F.);
#55881=ORIENTED_EDGE('',*,*,#38842,.T.);
#55882=ORIENTED_EDGE('',*,*,#38843,.T.);
#55883=ORIENTED_EDGE('',*,*,#38747,.F.);
#55884=ORIENTED_EDGE('',*,*,#38748,.F.);
#55885=ORIENTED_EDGE('',*,*,#38843,.F.);
#55886=ORIENTED_EDGE('',*,*,#38844,.F.);
#55887=ORIENTED_EDGE('',*,*,#38845,.F.);
#55888=ORIENTED_EDGE('',*,*,#38749,.F.);
#55889=ORIENTED_EDGE('',*,*,#38844,.T.);
#55890=ORIENTED_EDGE('',*,*,#38842,.F.);
#55891=ORIENTED_EDGE('',*,*,#38846,.F.);
#55892=ORIENTED_EDGE('',*,*,#38847,.T.);
#55893=ORIENTED_EDGE('',*,*,#38848,.T.);
#55894=ORIENTED_EDGE('',*,*,#38743,.F.);
#55895=ORIENTED_EDGE('',*,*,#38744,.F.);
#55896=ORIENTED_EDGE('',*,*,#38848,.F.);
#55897=ORIENTED_EDGE('',*,*,#38849,.F.);
#55898=ORIENTED_EDGE('',*,*,#38850,.F.);
#55899=ORIENTED_EDGE('',*,*,#38745,.F.);
#55900=ORIENTED_EDGE('',*,*,#38849,.T.);
#55901=ORIENTED_EDGE('',*,*,#38847,.F.);
#55902=ORIENTED_EDGE('',*,*,#38851,.F.);
#55903=ORIENTED_EDGE('',*,*,#38852,.T.);
#55904=ORIENTED_EDGE('',*,*,#38853,.T.);
#55905=ORIENTED_EDGE('',*,*,#38739,.F.);
#55906=ORIENTED_EDGE('',*,*,#38740,.F.);
#55907=ORIENTED_EDGE('',*,*,#38853,.F.);
#55908=ORIENTED_EDGE('',*,*,#38854,.F.);
#55909=ORIENTED_EDGE('',*,*,#38855,.F.);
#55910=ORIENTED_EDGE('',*,*,#38741,.F.);
#55911=ORIENTED_EDGE('',*,*,#38854,.T.);
#55912=ORIENTED_EDGE('',*,*,#38852,.F.);
#55913=ORIENTED_EDGE('',*,*,#38856,.F.);
#55914=ORIENTED_EDGE('',*,*,#38857,.T.);
#55915=ORIENTED_EDGE('',*,*,#38858,.T.);
#55916=ORIENTED_EDGE('',*,*,#38735,.F.);
#55917=ORIENTED_EDGE('',*,*,#38736,.F.);
#55918=ORIENTED_EDGE('',*,*,#38858,.F.);
#55919=ORIENTED_EDGE('',*,*,#38859,.F.);
#55920=ORIENTED_EDGE('',*,*,#38860,.F.);
#55921=ORIENTED_EDGE('',*,*,#38737,.F.);
#55922=ORIENTED_EDGE('',*,*,#38859,.T.);
#55923=ORIENTED_EDGE('',*,*,#38857,.F.);
#55924=ORIENTED_EDGE('',*,*,#38861,.F.);
#55925=ORIENTED_EDGE('',*,*,#38862,.T.);
#55926=ORIENTED_EDGE('',*,*,#38863,.T.);
#55927=ORIENTED_EDGE('',*,*,#38731,.F.);
#55928=ORIENTED_EDGE('',*,*,#38732,.F.);
#55929=ORIENTED_EDGE('',*,*,#38863,.F.);
#55930=ORIENTED_EDGE('',*,*,#38864,.F.);
#55931=ORIENTED_EDGE('',*,*,#38865,.F.);
#55932=ORIENTED_EDGE('',*,*,#38733,.F.);
#55933=ORIENTED_EDGE('',*,*,#38864,.T.);
#55934=ORIENTED_EDGE('',*,*,#38862,.F.);
#55935=ORIENTED_EDGE('',*,*,#38866,.F.);
#55936=ORIENTED_EDGE('',*,*,#38867,.T.);
#55937=ORIENTED_EDGE('',*,*,#38868,.T.);
#55938=ORIENTED_EDGE('',*,*,#38727,.F.);
#55939=ORIENTED_EDGE('',*,*,#38728,.F.);
#55940=ORIENTED_EDGE('',*,*,#38868,.F.);
#55941=ORIENTED_EDGE('',*,*,#38869,.F.);
#55942=ORIENTED_EDGE('',*,*,#38870,.F.);
#55943=ORIENTED_EDGE('',*,*,#38729,.F.);
#55944=ORIENTED_EDGE('',*,*,#38869,.T.);
#55945=ORIENTED_EDGE('',*,*,#38867,.F.);
#55946=ORIENTED_EDGE('',*,*,#38871,.F.);
#55947=ORIENTED_EDGE('',*,*,#38872,.T.);
#55948=ORIENTED_EDGE('',*,*,#38873,.T.);
#55949=ORIENTED_EDGE('',*,*,#38719,.F.);
#55950=ORIENTED_EDGE('',*,*,#38720,.F.);
#55951=ORIENTED_EDGE('',*,*,#38873,.F.);
#55952=ORIENTED_EDGE('',*,*,#38874,.F.);
#55953=ORIENTED_EDGE('',*,*,#38724,.F.);
#55954=ORIENTED_EDGE('',*,*,#38875,.F.);
#55955=ORIENTED_EDGE('',*,*,#38725,.F.);
#55956=ORIENTED_EDGE('',*,*,#38874,.T.);
#55957=ORIENTED_EDGE('',*,*,#38872,.F.);
#55958=ORIENTED_EDGE('',*,*,#38876,.F.);
#55959=ORIENTED_EDGE('',*,*,#38877,.T.);
#55960=ORIENTED_EDGE('',*,*,#38878,.T.);
#55961=ORIENTED_EDGE('',*,*,#38715,.F.);
#55962=ORIENTED_EDGE('',*,*,#38716,.F.);
#55963=ORIENTED_EDGE('',*,*,#38878,.F.);
#55964=ORIENTED_EDGE('',*,*,#38879,.F.);
#55965=ORIENTED_EDGE('',*,*,#38880,.F.);
#55966=ORIENTED_EDGE('',*,*,#38717,.F.);
#55967=ORIENTED_EDGE('',*,*,#38879,.T.);
#55968=ORIENTED_EDGE('',*,*,#38877,.F.);
#55969=ORIENTED_EDGE('',*,*,#38881,.F.);
#55970=ORIENTED_EDGE('',*,*,#38882,.T.);
#55971=ORIENTED_EDGE('',*,*,#38883,.T.);
#55972=ORIENTED_EDGE('',*,*,#38711,.F.);
#55973=ORIENTED_EDGE('',*,*,#38712,.F.);
#55974=ORIENTED_EDGE('',*,*,#38883,.F.);
#55975=ORIENTED_EDGE('',*,*,#38884,.F.);
#55976=ORIENTED_EDGE('',*,*,#38885,.F.);
#55977=ORIENTED_EDGE('',*,*,#38713,.F.);
#55978=ORIENTED_EDGE('',*,*,#38884,.T.);
#55979=ORIENTED_EDGE('',*,*,#38882,.F.);
#55980=ORIENTED_EDGE('',*,*,#38886,.F.);
#55981=ORIENTED_EDGE('',*,*,#38887,.T.);
#55982=ORIENTED_EDGE('',*,*,#38888,.T.);
#55983=ORIENTED_EDGE('',*,*,#38707,.F.);
#55984=ORIENTED_EDGE('',*,*,#38708,.F.);
#55985=ORIENTED_EDGE('',*,*,#38888,.F.);
#55986=ORIENTED_EDGE('',*,*,#38889,.F.);
#55987=ORIENTED_EDGE('',*,*,#38890,.F.);
#55988=ORIENTED_EDGE('',*,*,#38709,.F.);
#55989=ORIENTED_EDGE('',*,*,#38889,.T.);
#55990=ORIENTED_EDGE('',*,*,#38887,.F.);
#55991=ORIENTED_EDGE('',*,*,#38891,.F.);
#55992=ORIENTED_EDGE('',*,*,#38892,.T.);
#55993=ORIENTED_EDGE('',*,*,#38893,.T.);
#55994=ORIENTED_EDGE('',*,*,#38703,.F.);
#55995=ORIENTED_EDGE('',*,*,#38704,.F.);
#55996=ORIENTED_EDGE('',*,*,#38893,.F.);
#55997=ORIENTED_EDGE('',*,*,#38894,.F.);
#55998=ORIENTED_EDGE('',*,*,#38895,.F.);
#55999=ORIENTED_EDGE('',*,*,#38705,.F.);
#56000=ORIENTED_EDGE('',*,*,#38894,.T.);
#56001=ORIENTED_EDGE('',*,*,#38892,.F.);
#56002=ORIENTED_EDGE('',*,*,#38896,.F.);
#56003=ORIENTED_EDGE('',*,*,#38897,.T.);
#56004=ORIENTED_EDGE('',*,*,#38898,.T.);
#56005=ORIENTED_EDGE('',*,*,#38699,.F.);
#56006=ORIENTED_EDGE('',*,*,#38700,.F.);
#56007=ORIENTED_EDGE('',*,*,#38898,.F.);
#56008=ORIENTED_EDGE('',*,*,#38899,.F.);
#56009=ORIENTED_EDGE('',*,*,#38900,.F.);
#56010=ORIENTED_EDGE('',*,*,#38701,.F.);
#56011=ORIENTED_EDGE('',*,*,#38899,.T.);
#56012=ORIENTED_EDGE('',*,*,#38897,.F.);
#56013=ORIENTED_EDGE('',*,*,#38901,.F.);
#56014=ORIENTED_EDGE('',*,*,#38902,.T.);
#56015=ORIENTED_EDGE('',*,*,#38903,.T.);
#56016=ORIENTED_EDGE('',*,*,#38695,.F.);
#56017=ORIENTED_EDGE('',*,*,#38696,.F.);
#56018=ORIENTED_EDGE('',*,*,#38903,.F.);
#56019=ORIENTED_EDGE('',*,*,#38904,.F.);
#56020=ORIENTED_EDGE('',*,*,#38905,.F.);
#56021=ORIENTED_EDGE('',*,*,#38697,.F.);
#56022=ORIENTED_EDGE('',*,*,#38904,.T.);
#56023=ORIENTED_EDGE('',*,*,#38902,.F.);
#56024=ORIENTED_EDGE('',*,*,#38906,.F.);
#56025=ORIENTED_EDGE('',*,*,#38907,.T.);
#56026=ORIENTED_EDGE('',*,*,#38908,.T.);
#56027=ORIENTED_EDGE('',*,*,#38691,.F.);
#56028=ORIENTED_EDGE('',*,*,#38692,.F.);
#56029=ORIENTED_EDGE('',*,*,#38908,.F.);
#56030=ORIENTED_EDGE('',*,*,#38909,.F.);
#56031=ORIENTED_EDGE('',*,*,#38910,.F.);
#56032=ORIENTED_EDGE('',*,*,#38693,.F.);
#56033=ORIENTED_EDGE('',*,*,#38909,.T.);
#56034=ORIENTED_EDGE('',*,*,#38907,.F.);
#56035=ORIENTED_EDGE('',*,*,#38911,.F.);
#56036=ORIENTED_EDGE('',*,*,#38912,.T.);
#56037=ORIENTED_EDGE('',*,*,#38913,.T.);
#56038=ORIENTED_EDGE('',*,*,#38687,.F.);
#56039=ORIENTED_EDGE('',*,*,#38688,.F.);
#56040=ORIENTED_EDGE('',*,*,#38913,.F.);
#56041=ORIENTED_EDGE('',*,*,#38914,.F.);
#56042=ORIENTED_EDGE('',*,*,#38915,.F.);
#56043=ORIENTED_EDGE('',*,*,#38689,.F.);
#56044=ORIENTED_EDGE('',*,*,#38914,.T.);
#56045=ORIENTED_EDGE('',*,*,#38912,.F.);
#56046=ORIENTED_EDGE('',*,*,#38916,.F.);
#56047=ORIENTED_EDGE('',*,*,#38917,.T.);
#56048=ORIENTED_EDGE('',*,*,#38918,.T.);
#56049=ORIENTED_EDGE('',*,*,#38683,.F.);
#56050=ORIENTED_EDGE('',*,*,#38684,.F.);
#56051=ORIENTED_EDGE('',*,*,#38918,.F.);
#56052=ORIENTED_EDGE('',*,*,#38919,.F.);
#56053=ORIENTED_EDGE('',*,*,#38920,.F.);
#56054=ORIENTED_EDGE('',*,*,#38685,.F.);
#56055=ORIENTED_EDGE('',*,*,#38919,.T.);
#56056=ORIENTED_EDGE('',*,*,#38917,.F.);
#56057=ORIENTED_EDGE('',*,*,#38921,.F.);
#56058=ORIENTED_EDGE('',*,*,#38922,.T.);
#56059=ORIENTED_EDGE('',*,*,#38923,.T.);
#56060=ORIENTED_EDGE('',*,*,#38679,.F.);
#56061=ORIENTED_EDGE('',*,*,#38680,.F.);
#56062=ORIENTED_EDGE('',*,*,#38923,.F.);
#56063=ORIENTED_EDGE('',*,*,#38924,.F.);
#56064=ORIENTED_EDGE('',*,*,#38925,.F.);
#56065=ORIENTED_EDGE('',*,*,#38681,.F.);
#56066=ORIENTED_EDGE('',*,*,#38924,.T.);
#56067=ORIENTED_EDGE('',*,*,#38922,.F.);
#56068=ORIENTED_EDGE('',*,*,#38926,.F.);
#56069=ORIENTED_EDGE('',*,*,#38927,.T.);
#56070=ORIENTED_EDGE('',*,*,#38928,.T.);
#56071=ORIENTED_EDGE('',*,*,#38675,.F.);
#56072=ORIENTED_EDGE('',*,*,#38676,.F.);
#56073=ORIENTED_EDGE('',*,*,#38928,.F.);
#56074=ORIENTED_EDGE('',*,*,#38929,.F.);
#56075=ORIENTED_EDGE('',*,*,#38930,.F.);
#56076=ORIENTED_EDGE('',*,*,#38677,.F.);
#56077=ORIENTED_EDGE('',*,*,#38929,.T.);
#56078=ORIENTED_EDGE('',*,*,#38927,.F.);
#56079=ORIENTED_EDGE('',*,*,#38931,.F.);
#56080=ORIENTED_EDGE('',*,*,#38932,.T.);
#56081=ORIENTED_EDGE('',*,*,#38933,.T.);
#56082=ORIENTED_EDGE('',*,*,#38671,.F.);
#56083=ORIENTED_EDGE('',*,*,#38672,.F.);
#56084=ORIENTED_EDGE('',*,*,#38933,.F.);
#56085=ORIENTED_EDGE('',*,*,#38934,.F.);
#56086=ORIENTED_EDGE('',*,*,#38935,.F.);
#56087=ORIENTED_EDGE('',*,*,#38673,.F.);
#56088=ORIENTED_EDGE('',*,*,#38934,.T.);
#56089=ORIENTED_EDGE('',*,*,#38932,.F.);
#56090=ORIENTED_EDGE('',*,*,#38936,.F.);
#56091=ORIENTED_EDGE('',*,*,#38937,.T.);
#56092=ORIENTED_EDGE('',*,*,#38938,.T.);
#56093=ORIENTED_EDGE('',*,*,#38667,.F.);
#56094=ORIENTED_EDGE('',*,*,#38668,.F.);
#56095=ORIENTED_EDGE('',*,*,#38938,.F.);
#56096=ORIENTED_EDGE('',*,*,#38939,.F.);
#56097=ORIENTED_EDGE('',*,*,#38940,.F.);
#56098=ORIENTED_EDGE('',*,*,#38669,.F.);
#56099=ORIENTED_EDGE('',*,*,#38939,.T.);
#56100=ORIENTED_EDGE('',*,*,#38937,.F.);
#56101=ORIENTED_EDGE('',*,*,#38941,.F.);
#56102=ORIENTED_EDGE('',*,*,#38942,.T.);
#56103=ORIENTED_EDGE('',*,*,#38943,.T.);
#56104=ORIENTED_EDGE('',*,*,#38663,.F.);
#56105=ORIENTED_EDGE('',*,*,#38664,.F.);
#56106=ORIENTED_EDGE('',*,*,#38943,.F.);
#56107=ORIENTED_EDGE('',*,*,#38944,.F.);
#56108=ORIENTED_EDGE('',*,*,#38945,.F.);
#56109=ORIENTED_EDGE('',*,*,#38665,.F.);
#56110=ORIENTED_EDGE('',*,*,#38944,.T.);
#56111=ORIENTED_EDGE('',*,*,#38942,.F.);
#56112=ORIENTED_EDGE('',*,*,#38946,.F.);
#56113=ORIENTED_EDGE('',*,*,#38947,.T.);
#56114=ORIENTED_EDGE('',*,*,#38948,.T.);
#56115=ORIENTED_EDGE('',*,*,#38659,.F.);
#56116=ORIENTED_EDGE('',*,*,#38660,.F.);
#56117=ORIENTED_EDGE('',*,*,#38948,.F.);
#56118=ORIENTED_EDGE('',*,*,#38949,.F.);
#56119=ORIENTED_EDGE('',*,*,#38950,.F.);
#56120=ORIENTED_EDGE('',*,*,#38661,.F.);
#56121=ORIENTED_EDGE('',*,*,#38949,.T.);
#56122=ORIENTED_EDGE('',*,*,#38947,.F.);
#56123=ORIENTED_EDGE('',*,*,#38951,.F.);
#56124=ORIENTED_EDGE('',*,*,#38952,.T.);
#56125=ORIENTED_EDGE('',*,*,#38953,.T.);
#56126=ORIENTED_EDGE('',*,*,#38655,.F.);
#56127=ORIENTED_EDGE('',*,*,#38656,.F.);
#56128=ORIENTED_EDGE('',*,*,#38953,.F.);
#56129=ORIENTED_EDGE('',*,*,#38954,.F.);
#56130=ORIENTED_EDGE('',*,*,#38955,.F.);
#56131=ORIENTED_EDGE('',*,*,#38657,.F.);
#56132=ORIENTED_EDGE('',*,*,#38954,.T.);
#56133=ORIENTED_EDGE('',*,*,#38952,.F.);
#56134=ORIENTED_EDGE('',*,*,#38956,.F.);
#56135=ORIENTED_EDGE('',*,*,#38957,.T.);
#56136=ORIENTED_EDGE('',*,*,#38958,.T.);
#56137=ORIENTED_EDGE('',*,*,#38651,.F.);
#56138=ORIENTED_EDGE('',*,*,#38652,.F.);
#56139=ORIENTED_EDGE('',*,*,#38958,.F.);
#56140=ORIENTED_EDGE('',*,*,#38959,.F.);
#56141=ORIENTED_EDGE('',*,*,#38960,.F.);
#56142=ORIENTED_EDGE('',*,*,#38653,.F.);
#56143=ORIENTED_EDGE('',*,*,#38959,.T.);
#56144=ORIENTED_EDGE('',*,*,#38957,.F.);
#56145=ORIENTED_EDGE('',*,*,#38961,.F.);
#56146=ORIENTED_EDGE('',*,*,#38962,.T.);
#56147=ORIENTED_EDGE('',*,*,#38963,.T.);
#56148=ORIENTED_EDGE('',*,*,#38647,.F.);
#56149=ORIENTED_EDGE('',*,*,#38648,.F.);
#56150=ORIENTED_EDGE('',*,*,#38963,.F.);
#56151=ORIENTED_EDGE('',*,*,#38964,.F.);
#56152=ORIENTED_EDGE('',*,*,#38965,.F.);
#56153=ORIENTED_EDGE('',*,*,#38649,.F.);
#56154=ORIENTED_EDGE('',*,*,#38964,.T.);
#56155=ORIENTED_EDGE('',*,*,#38962,.F.);
#56156=ORIENTED_EDGE('',*,*,#38723,.T.);
#56157=ORIENTED_EDGE('',*,*,#38966,.T.);
#56158=ORIENTED_EDGE('',*,*,#38635,.T.);
#56159=ORIENTED_EDGE('',*,*,#38966,.F.);
#56160=ORIENTED_EDGE('',*,*,#38722,.T.);
#56161=ORIENTED_EDGE('',*,*,#38967,.T.);
#56162=ORIENTED_EDGE('',*,*,#38968,.T.);
#56163=ORIENTED_EDGE('',*,*,#38871,.T.);
#56164=ORIENTED_EDGE('',*,*,#38718,.T.);
#56165=ORIENTED_EDGE('',*,*,#38880,.T.);
#56166=ORIENTED_EDGE('',*,*,#38876,.T.);
#56167=ORIENTED_EDGE('',*,*,#38714,.T.);
#56168=ORIENTED_EDGE('',*,*,#38885,.T.);
#56169=ORIENTED_EDGE('',*,*,#38881,.T.);
#56170=ORIENTED_EDGE('',*,*,#38710,.T.);
#56171=ORIENTED_EDGE('',*,*,#38890,.T.);
#56172=ORIENTED_EDGE('',*,*,#38886,.T.);
#56173=ORIENTED_EDGE('',*,*,#38706,.T.);
#56174=ORIENTED_EDGE('',*,*,#38895,.T.);
#56175=ORIENTED_EDGE('',*,*,#38891,.T.);
#56176=ORIENTED_EDGE('',*,*,#38702,.T.);
#56177=ORIENTED_EDGE('',*,*,#38900,.T.);
#56178=ORIENTED_EDGE('',*,*,#38896,.T.);
#56179=ORIENTED_EDGE('',*,*,#38698,.T.);
#56180=ORIENTED_EDGE('',*,*,#38905,.T.);
#56181=ORIENTED_EDGE('',*,*,#38901,.T.);
#56182=ORIENTED_EDGE('',*,*,#38694,.T.);
#56183=ORIENTED_EDGE('',*,*,#38910,.T.);
#56184=ORIENTED_EDGE('',*,*,#38906,.T.);
#56185=ORIENTED_EDGE('',*,*,#38690,.T.);
#56186=ORIENTED_EDGE('',*,*,#38915,.T.);
#56187=ORIENTED_EDGE('',*,*,#38911,.T.);
#56188=ORIENTED_EDGE('',*,*,#38686,.T.);
#56189=ORIENTED_EDGE('',*,*,#38920,.T.);
#56190=ORIENTED_EDGE('',*,*,#38916,.T.);
#56191=ORIENTED_EDGE('',*,*,#38682,.T.);
#56192=ORIENTED_EDGE('',*,*,#38925,.T.);
#56193=ORIENTED_EDGE('',*,*,#38921,.T.);
#56194=ORIENTED_EDGE('',*,*,#38678,.T.);
#56195=ORIENTED_EDGE('',*,*,#38930,.T.);
#56196=ORIENTED_EDGE('',*,*,#38926,.T.);
#56197=ORIENTED_EDGE('',*,*,#38674,.T.);
#56198=ORIENTED_EDGE('',*,*,#38935,.T.);
#56199=ORIENTED_EDGE('',*,*,#38931,.T.);
#56200=ORIENTED_EDGE('',*,*,#38670,.T.);
#56201=ORIENTED_EDGE('',*,*,#38940,.T.);
#56202=ORIENTED_EDGE('',*,*,#38936,.T.);
#56203=ORIENTED_EDGE('',*,*,#38666,.T.);
#56204=ORIENTED_EDGE('',*,*,#38945,.T.);
#56205=ORIENTED_EDGE('',*,*,#38941,.T.);
#56206=ORIENTED_EDGE('',*,*,#38662,.T.);
#56207=ORIENTED_EDGE('',*,*,#38950,.T.);
#56208=ORIENTED_EDGE('',*,*,#38946,.T.);
#56209=ORIENTED_EDGE('',*,*,#38658,.T.);
#56210=ORIENTED_EDGE('',*,*,#38955,.T.);
#56211=ORIENTED_EDGE('',*,*,#38951,.T.);
#56212=ORIENTED_EDGE('',*,*,#38654,.T.);
#56213=ORIENTED_EDGE('',*,*,#38960,.T.);
#56214=ORIENTED_EDGE('',*,*,#38956,.T.);
#56215=ORIENTED_EDGE('',*,*,#38650,.T.);
#56216=ORIENTED_EDGE('',*,*,#38965,.T.);
#56217=ORIENTED_EDGE('',*,*,#38961,.T.);
#56218=ORIENTED_EDGE('',*,*,#38646,.T.);
#56219=ORIENTED_EDGE('',*,*,#38644,.T.);
#56220=ORIENTED_EDGE('',*,*,#38638,.T.);
#56221=ORIENTED_EDGE('',*,*,#38790,.T.);
#56222=ORIENTED_EDGE('',*,*,#38795,.T.);
#56223=ORIENTED_EDGE('',*,*,#38791,.T.);
#56224=ORIENTED_EDGE('',*,*,#38786,.T.);
#56225=ORIENTED_EDGE('',*,*,#38800,.T.);
#56226=ORIENTED_EDGE('',*,*,#38796,.T.);
#56227=ORIENTED_EDGE('',*,*,#38782,.T.);
#56228=ORIENTED_EDGE('',*,*,#38805,.T.);
#56229=ORIENTED_EDGE('',*,*,#38801,.T.);
#56230=ORIENTED_EDGE('',*,*,#38778,.T.);
#56231=ORIENTED_EDGE('',*,*,#38810,.T.);
#56232=ORIENTED_EDGE('',*,*,#38806,.T.);
#56233=ORIENTED_EDGE('',*,*,#38774,.T.);
#56234=ORIENTED_EDGE('',*,*,#38815,.T.);
#56235=ORIENTED_EDGE('',*,*,#38811,.T.);
#56236=ORIENTED_EDGE('',*,*,#38770,.T.);
#56237=ORIENTED_EDGE('',*,*,#38820,.T.);
#56238=ORIENTED_EDGE('',*,*,#38816,.T.);
#56239=ORIENTED_EDGE('',*,*,#38766,.T.);
#56240=ORIENTED_EDGE('',*,*,#38825,.T.);
#56241=ORIENTED_EDGE('',*,*,#38821,.T.);
#56242=ORIENTED_EDGE('',*,*,#38762,.T.);
#56243=ORIENTED_EDGE('',*,*,#38830,.T.);
#56244=ORIENTED_EDGE('',*,*,#38826,.T.);
#56245=ORIENTED_EDGE('',*,*,#38758,.T.);
#56246=ORIENTED_EDGE('',*,*,#38835,.T.);
#56247=ORIENTED_EDGE('',*,*,#38831,.T.);
#56248=ORIENTED_EDGE('',*,*,#38754,.T.);
#56249=ORIENTED_EDGE('',*,*,#38840,.T.);
#56250=ORIENTED_EDGE('',*,*,#38836,.T.);
#56251=ORIENTED_EDGE('',*,*,#38750,.T.);
#56252=ORIENTED_EDGE('',*,*,#38845,.T.);
#56253=ORIENTED_EDGE('',*,*,#38841,.T.);
#56254=ORIENTED_EDGE('',*,*,#38746,.T.);
#56255=ORIENTED_EDGE('',*,*,#38850,.T.);
#56256=ORIENTED_EDGE('',*,*,#38846,.T.);
#56257=ORIENTED_EDGE('',*,*,#38742,.T.);
#56258=ORIENTED_EDGE('',*,*,#38855,.T.);
#56259=ORIENTED_EDGE('',*,*,#38851,.T.);
#56260=ORIENTED_EDGE('',*,*,#38738,.T.);
#56261=ORIENTED_EDGE('',*,*,#38860,.T.);
#56262=ORIENTED_EDGE('',*,*,#38856,.T.);
#56263=ORIENTED_EDGE('',*,*,#38734,.T.);
#56264=ORIENTED_EDGE('',*,*,#38865,.T.);
#56265=ORIENTED_EDGE('',*,*,#38861,.T.);
#56266=ORIENTED_EDGE('',*,*,#38730,.T.);
#56267=ORIENTED_EDGE('',*,*,#38870,.T.);
#56268=ORIENTED_EDGE('',*,*,#38866,.T.);
#56269=ORIENTED_EDGE('',*,*,#38726,.T.);
#56270=ORIENTED_EDGE('',*,*,#38875,.T.);
#56271=ORIENTED_EDGE('',*,*,#38968,.F.);
#56272=ORIENTED_EDGE('',*,*,#38967,.F.);
#56273=ORIENTED_EDGE('',*,*,#38969,.T.);
#56274=ORIENTED_EDGE('',*,*,#38969,.F.);
#56275=ORIENTED_EDGE('',*,*,#38970,.T.);
#56276=ORIENTED_EDGE('',*,*,#38971,.F.);
#56277=ORIENTED_EDGE('',*,*,#38972,.T.);
#56278=ORIENTED_EDGE('',*,*,#38973,.F.);
#56279=ORIENTED_EDGE('',*,*,#38974,.F.);
#56280=ORIENTED_EDGE('',*,*,#38975,.T.);
#56281=ORIENTED_EDGE('',*,*,#38976,.F.);
#56282=ORIENTED_EDGE('',*,*,#38977,.F.);
#56283=ORIENTED_EDGE('',*,*,#38978,.T.);
#56284=ORIENTED_EDGE('',*,*,#38979,.F.);
#56285=ORIENTED_EDGE('',*,*,#38980,.F.);
#56286=ORIENTED_EDGE('',*,*,#38981,.T.);
#56287=ORIENTED_EDGE('',*,*,#38982,.F.);
#56288=ORIENTED_EDGE('',*,*,#38983,.F.);
#56289=ORIENTED_EDGE('',*,*,#38984,.T.);
#56290=ORIENTED_EDGE('',*,*,#38985,.F.);
#56291=ORIENTED_EDGE('',*,*,#38986,.F.);
#56292=ORIENTED_EDGE('',*,*,#38987,.T.);
#56293=ORIENTED_EDGE('',*,*,#38988,.F.);
#56294=ORIENTED_EDGE('',*,*,#38970,.F.);
#56295=ORIENTED_EDGE('',*,*,#38989,.F.);
#56296=ORIENTED_EDGE('',*,*,#38975,.F.);
#56297=ORIENTED_EDGE('',*,*,#38990,.F.);
#56298=ORIENTED_EDGE('',*,*,#38991,.F.);
#56299=ORIENTED_EDGE('',*,*,#38992,.F.);
#56300=ORIENTED_EDGE('',*,*,#38978,.F.);
#56301=ORIENTED_EDGE('',*,*,#38993,.F.);
#56302=ORIENTED_EDGE('',*,*,#38994,.F.);
#56303=ORIENTED_EDGE('',*,*,#38995,.F.);
#56304=ORIENTED_EDGE('',*,*,#38996,.F.);
#56305=ORIENTED_EDGE('',*,*,#38997,.F.);
#56306=ORIENTED_EDGE('',*,*,#38972,.F.);
#56307=ORIENTED_EDGE('',*,*,#38998,.F.);
#56308=ORIENTED_EDGE('',*,*,#38981,.F.);
#56309=ORIENTED_EDGE('',*,*,#38999,.F.);
#56310=ORIENTED_EDGE('',*,*,#39000,.F.);
#56311=ORIENTED_EDGE('',*,*,#39001,.F.);
#56312=ORIENTED_EDGE('',*,*,#39002,.F.);
#56313=ORIENTED_EDGE('',*,*,#39003,.F.);
#56314=ORIENTED_EDGE('',*,*,#38987,.F.);
#56315=ORIENTED_EDGE('',*,*,#39004,.F.);
#56316=ORIENTED_EDGE('',*,*,#39005,.F.);
#56317=ORIENTED_EDGE('',*,*,#39006,.F.);
#56318=ORIENTED_EDGE('',*,*,#38984,.F.);
#56319=ORIENTED_EDGE('',*,*,#38982,.T.);
#56320=ORIENTED_EDGE('',*,*,#38998,.T.);
#56321=ORIENTED_EDGE('',*,*,#39007,.F.);
#56322=ORIENTED_EDGE('',*,*,#38999,.T.);
#56323=ORIENTED_EDGE('',*,*,#38980,.T.);
#56324=ORIENTED_EDGE('',*,*,#39008,.T.);
#56325=ORIENTED_EDGE('',*,*,#39009,.T.);
#56326=ORIENTED_EDGE('',*,*,#39010,.F.);
#56327=ORIENTED_EDGE('',*,*,#38979,.T.);
#56328=ORIENTED_EDGE('',*,*,#38992,.T.);
#56329=ORIENTED_EDGE('',*,*,#39011,.F.);
#56330=ORIENTED_EDGE('',*,*,#38993,.T.);
#56331=ORIENTED_EDGE('',*,*,#38977,.T.);
#56332=ORIENTED_EDGE('',*,*,#39012,.T.);
#56333=ORIENTED_EDGE('',*,*,#39013,.T.);
#56334=ORIENTED_EDGE('',*,*,#39008,.F.);
#56335=ORIENTED_EDGE('',*,*,#38976,.T.);
#56336=ORIENTED_EDGE('',*,*,#38989,.T.);
#56337=ORIENTED_EDGE('',*,*,#39014,.F.);
#56338=ORIENTED_EDGE('',*,*,#38990,.T.);
#56339=ORIENTED_EDGE('',*,*,#38974,.T.);
#56340=ORIENTED_EDGE('',*,*,#39015,.T.);
#56341=ORIENTED_EDGE('',*,*,#39016,.T.);
#56342=ORIENTED_EDGE('',*,*,#39012,.F.);
#56343=ORIENTED_EDGE('',*,*,#38991,.T.);
#56344=ORIENTED_EDGE('',*,*,#39014,.T.);
#56345=ORIENTED_EDGE('',*,*,#38994,.T.);
#56346=ORIENTED_EDGE('',*,*,#39011,.T.);
#56347=ORIENTED_EDGE('',*,*,#38996,.T.);
#56348=ORIENTED_EDGE('',*,*,#39017,.T.);
#56349=ORIENTED_EDGE('',*,*,#39000,.T.);
#56350=ORIENTED_EDGE('',*,*,#39007,.T.);
#56351=ORIENTED_EDGE('',*,*,#39002,.T.);
#56352=ORIENTED_EDGE('',*,*,#39018,.T.);
#56353=ORIENTED_EDGE('',*,*,#39005,.T.);
#56354=ORIENTED_EDGE('',*,*,#39019,.T.);
#56355=ORIENTED_EDGE('',*,*,#39020,.F.);
#56356=ORIENTED_EDGE('',*,*,#39021,.T.);
#56357=ORIENTED_EDGE('',*,*,#39016,.F.);
#56358=ORIENTED_EDGE('',*,*,#39022,.T.);
#56359=ORIENTED_EDGE('',*,*,#39013,.F.);
#56360=ORIENTED_EDGE('',*,*,#39023,.T.);
#56361=ORIENTED_EDGE('',*,*,#39009,.F.);
#56362=ORIENTED_EDGE('',*,*,#39024,.T.);
#56363=ORIENTED_EDGE('',*,*,#39025,.F.);
#56364=ORIENTED_EDGE('',*,*,#39026,.T.);
#56365=ORIENTED_EDGE('',*,*,#39027,.F.);
#56366=ORIENTED_EDGE('',*,*,#39028,.T.);
#56367=ORIENTED_EDGE('',*,*,#39024,.F.);
#56368=ORIENTED_EDGE('',*,*,#39023,.F.);
#56369=ORIENTED_EDGE('',*,*,#39022,.F.);
#56370=ORIENTED_EDGE('',*,*,#39021,.F.);
#56371=ORIENTED_EDGE('',*,*,#39029,.T.);
#56372=ORIENTED_EDGE('',*,*,#39029,.F.);
#56373=ORIENTED_EDGE('',*,*,#39028,.F.);
#56374=ORIENTED_EDGE('',*,*,#39026,.F.);
#56375=ORIENTED_EDGE('',*,*,#38971,.T.);
#56376=ORIENTED_EDGE('',*,*,#39030,.T.);
#56377=ORIENTED_EDGE('',*,*,#39020,.T.);
#56378=ORIENTED_EDGE('',*,*,#39015,.F.);
#56379=ORIENTED_EDGE('',*,*,#38973,.T.);
#56380=ORIENTED_EDGE('',*,*,#38997,.T.);
#56381=ORIENTED_EDGE('',*,*,#39017,.F.);
#56382=ORIENTED_EDGE('',*,*,#38995,.T.);
#56383=ORIENTED_EDGE('',*,*,#38986,.T.);
#56384=ORIENTED_EDGE('',*,*,#39031,.T.);
#56385=ORIENTED_EDGE('',*,*,#39027,.T.);
#56386=ORIENTED_EDGE('',*,*,#39030,.F.);
#56387=ORIENTED_EDGE('',*,*,#38988,.T.);
#56388=ORIENTED_EDGE('',*,*,#39003,.T.);
#56389=ORIENTED_EDGE('',*,*,#39018,.F.);
#56390=ORIENTED_EDGE('',*,*,#39001,.T.);
#56391=ORIENTED_EDGE('',*,*,#38983,.T.);
#56392=ORIENTED_EDGE('',*,*,#39010,.T.);
#56393=ORIENTED_EDGE('',*,*,#39025,.T.);
#56394=ORIENTED_EDGE('',*,*,#39031,.F.);
#56395=ORIENTED_EDGE('',*,*,#38985,.T.);
#56396=ORIENTED_EDGE('',*,*,#39006,.T.);
#56397=ORIENTED_EDGE('',*,*,#39019,.F.);
#56398=ORIENTED_EDGE('',*,*,#39004,.T.);
#57123=B_SPLINE_SURFACE_WITH_KNOTS('',3,3,((#112068,#112069,#112070,#112071,
#112072,#112073,#112074,#112075,#112076,#112077,#112078,#112079,#112080,
#112081,#112082,#112083,#112084,#112085,#112086,#112087,#112088,#112089,
#112090,#112091,#112092,#112093,#112094,#112095,#112096,#112097,#112098,
#112099,#112100,#112101,#112102,#112103,#112104,#112105,#112106,#112107,
#112108,#112109,#112110,#112111,#112112,#112113,#112114,#112115,#112116,
#112117,#112118,#112119,#112120,#112121,#112122,#112123,#112124,#112125,
#112126,#112127,#112128,#112129,#112130,#112131,#112132,#112133,#112134,
#112135,#112136,#112137,#112138,#112139,#112140,#112141,#112142,#112143,
#112144,#112145,#112146,#112147,#112148,#112149,#112150),(#112151,#112152,
#112153,#112154,#112155,#112156,#112157,#112158,#112159,#112160,#112161,
#112162,#112163,#112164,#112165,#112166,#112167,#112168,#112169,#112170,
#112171,#112172,#112173,#112174,#112175,#112176,#112177,#112178,#112179,
#112180,#112181,#112182,#112183,#112184,#112185,#112186,#112187,#112188,
#112189,#112190,#112191,#112192,#112193,#112194,#112195,#112196,#112197,
#112198,#112199,#112200,#112201,#112202,#112203,#112204,#112205,#112206,
#112207,#112208,#112209,#112210,#112211,#112212,#112213,#112214,#112215,
#112216,#112217,#112218,#112219,#112220,#112221,#112222,#112223,#112224,
#112225,#112226,#112227,#112228,#112229,#112230,#112231,#112232,#112233),
(#112234,#112235,#112236,#112237,#112238,#112239,#112240,#112241,#112242,
#112243,#112244,#112245,#112246,#112247,#112248,#112249,#112250,#112251,
#112252,#112253,#112254,#112255,#112256,#112257,#112258,#112259,#112260,
#112261,#112262,#112263,#112264,#112265,#112266,#112267,#112268,#112269,
#112270,#112271,#112272,#112273,#112274,#112275,#112276,#112277,#112278,
#112279,#112280,#112281,#112282,#112283,#112284,#112285,#112286,#112287,
#112288,#112289,#112290,#112291,#112292,#112293,#112294,#112295,#112296,
#112297,#112298,#112299,#112300,#112301,#112302,#112303,#112304,#112305,
#112306,#112307,#112308,#112309,#112310,#112311,#112312,#112313,#112314,
#112315,#112316),(#112317,#112318,#112319,#112320,#112321,#112322,#112323,
#112324,#112325,#112326,#112327,#112328,#112329,#112330,#112331,#112332,
#112333,#112334,#112335,#112336,#112337,#112338,#112339,#112340,#112341,
#112342,#112343,#112344,#112345,#112346,#112347,#112348,#112349,#112350,
#112351,#112352,#112353,#112354,#112355,#112356,#112357,#112358,#112359,
#112360,#112361,#112362,#112363,#112364,#112365,#112366,#112367,#112368,
#112369,#112370,#112371,#112372,#112373,#112374,#112375,#112376,#112377,
#112378,#112379,#112380,#112381,#112382,#112383,#112384,#112385,#112386,
#112387,#112388,#112389,#112390,#112391,#112392,#112393,#112394,#112395,
#112396,#112397,#112398,#112399)),.UNSPECIFIED.,.F.,.F.,.F.,(4,4),(4,1,
1,1,1,1,1,1,1,1,1,1,1,1,1,1,1,1,1,1,1,1,1,1,1,1,1,1,1,1,1,1,1,1,1,1,1,1,
1,1,1,1,1,1,1,1,1,1,1,1,1,1,1,1,1,1,1,1,1,1,1,1,1,1,1,1,1,1,1,1,1,1,1,1,
1,1,1,1,1,1,4),(0.,0.0296469363228873),(8.30626835282486,9.30079792027989,
10.2953274877349,11.2898570551899,12.284386622645,13.2789161901,14.273445757555,
15.26797532501,16.2625048924651,17.2570344599201,18.2515640273751,19.2460935948302,
20.2406231622852,21.2351527297402,22.2296822971952,23.2242118646503,24.2187414321053,
25.2132709995603,26.2078005670153,27.2023301344704,28.1968597019254,29.1913892693804,
30.1859188368355,31.1804484042905,32.1749779717455,33.1695075392005,34.1640371066556,
35.1585666741106,36.1530962415656,37.1476258090206,38.1421553764757,39.1366849439307,
40.1312145113857,41.1257440788408,42.1202736462958,43.1148032137508,44.1093327812058,
45.1038623486609,46.0983919161159,47.0929214835709,48.0874510510259,49.081980618481,
50.076510185936,51.071039753391,52.0655693208461,53.0600988883011,54.0546284557561,
55.0491580232111,56.0436875906662,57.0382171581212,58.0327467255762,59.0272762930312,
60.0218058604863,61.0163354279413,62.0108649953963,63.0053945628514,63.9999241303064,
64.9944536977614,65.9889832652164,66.9835128326715,67.9780424001265,68.9725719675815,
69.9671015350365,70.9616311024916,71.9561606699466,72.9506902374016,73.9452198048566,
74.9397493723117,75.9342789397667,76.9288085072217,77.9233380746768,78.9178676421318,
79.9123972095868,80.9069267770418,81.9014563444969,82.8959859119519,83.8905154794069,
84.8850450468619,85.879574614317,86.874104181772,87.868633749227),
 .UNSPECIFIED.);
#57124=B_SPLINE_SURFACE_WITH_KNOTS('',3,3,((#112596,#112597,#112598,#112599,
#112600,#112601,#112602,#112603,#112604,#112605,#112606,#112607,#112608,
#112609,#112610,#112611,#112612,#112613,#112614,#112615,#112616,#112617,
#112618,#112619,#112620,#112621,#112622,#112623,#112624,#112625,#112626,
#112627,#112628,#112629,#112630,#112631,#112632,#112633,#112634,#112635,
#112636,#112637,#112638,#112639,#112640,#112641,#112642,#112643,#112644,
#112645,#112646,#112647,#112648,#112649,#112650,#112651,#112652,#112653,
#112654,#112655,#112656,#112657,#112658,#112659,#112660,#112661,#112662,
#112663,#112664,#112665,#112666,#112667,#112668,#112669,#112670,#112671,
#112672,#112673,#112674,#112675,#112676,#112677,#112678),(#112679,#112680,
#112681,#112682,#112683,#112684,#112685,#112686,#112687,#112688,#112689,
#112690,#112691,#112692,#112693,#112694,#112695,#112696,#112697,#112698,
#112699,#112700,#112701,#112702,#112703,#112704,#112705,#112706,#112707,
#112708,#112709,#112710,#112711,#112712,#112713,#112714,#112715,#112716,
#112717,#112718,#112719,#112720,#112721,#112722,#112723,#112724,#112725,
#112726,#112727,#112728,#112729,#112730,#112731,#112732,#112733,#112734,
#112735,#112736,#112737,#112738,#112739,#112740,#112741,#112742,#112743,
#112744,#112745,#112746,#112747,#112748,#112749,#112750,#112751,#112752,
#112753,#112754,#112755,#112756,#112757,#112758,#112759,#112760,#112761),
(#112762,#112763,#112764,#112765,#112766,#112767,#112768,#112769,#112770,
#112771,#112772,#112773,#112774,#112775,#112776,#112777,#112778,#112779,
#112780,#112781,#112782,#112783,#112784,#112785,#112786,#112787,#112788,
#112789,#112790,#112791,#112792,#112793,#112794,#112795,#112796,#112797,
#112798,#112799,#112800,#112801,#112802,#112803,#112804,#112805,#112806,
#112807,#112808,#112809,#112810,#112811,#112812,#112813,#112814,#112815,
#112816,#112817,#112818,#112819,#112820,#112821,#112822,#112823,#112824,
#112825,#112826,#112827,#112828,#112829,#112830,#112831,#112832,#112833,
#112834,#112835,#112836,#112837,#112838,#112839,#112840,#112841,#112842,
#112843,#112844),(#112845,#112846,#112847,#112848,#112849,#112850,#112851,
#112852,#112853,#112854,#112855,#112856,#112857,#112858,#112859,#112860,
#112861,#112862,#112863,#112864,#112865,#112866,#112867,#112868,#112869,
#112870,#112871,#112872,#112873,#112874,#112875,#112876,#112877,#112878,
#112879,#112880,#112881,#112882,#112883,#112884,#112885,#112886,#112887,
#112888,#112889,#112890,#112891,#112892,#112893,#112894,#112895,#112896,
#112897,#112898,#112899,#112900,#112901,#112902,#112903,#112904,#112905,
#112906,#112907,#112908,#112909,#112910,#112911,#112912,#112913,#112914,
#112915,#112916,#112917,#112918,#112919,#112920,#112921,#112922,#112923,
#112924,#112925,#112926,#112927)),.UNSPECIFIED.,.F.,.F.,.F.,(4,4),(4,1,
1,1,1,1,1,1,1,1,1,1,1,1,1,1,1,1,1,1,1,1,1,1,1,1,1,1,1,1,1,1,1,1,1,1,1,1,
1,1,1,1,1,1,1,1,1,1,1,1,1,1,1,1,1,1,1,1,1,1,1,1,1,1,1,1,1,1,1,1,1,1,1,1,
1,1,1,1,1,1,4),(0.,0.0296469363228873),(11.6151336144496,12.6096631819046,
13.6041927493596,14.5987223168147,15.5932518842697,16.5877814517247,17.5823110191797,
18.5768405866348,19.5713701540898,20.5658997215448,21.5604292889998,22.5549588564549,
23.5494884239099,24.5440179913649,25.53854755882,26.533077126275,27.52760669373,
28.522136261185,29.5166658286401,30.5111953960951,31.5057249635501,32.5002545310051,
33.4947840984602,34.4893136659152,35.4838432333702,36.4783728008253,37.4729023682803,
38.4674319357353,39.4619615031903,40.4564910706454,41.4510206381004,42.4455502055554,
43.4400797730104,44.4346093404655,45.4291389079205,46.4236684753755,47.4181980428306,
48.4127276102856,49.4072571777406,50.4017867451956,51.3963163126507,52.3908458801057,
53.3853754475607,54.3799050150157,55.3744345824708,56.3689641499258,57.3634937173808,
58.3580232848359,59.3525528522909,60.3470824197459,61.3416119872009,62.336141554656,
63.330671122111,64.325200689566,65.319730257021,66.3142598244761,67.3087893919311,
68.3033189593861,69.2978485268412,70.2923780942962,71.2869076617512,72.2814372292062,
73.2759667966613,74.2704963641163,75.2650259315713,76.2595554990263,77.2540850664814,
78.2486146339364,79.2431442013914,80.2376737688465,81.2322033363015,82.2267329037565,
83.2212624712115,84.2157920386666,85.2103216061216,86.2048511735766,87.1993807410316,
88.1939103084867,89.1884398759417,90.1829694433967,91.1774990108518),
 .UNSPECIFIED.);
#60214=ADVANCED_FACE('',(#7114),#840,.T.);
#60215=ADVANCED_FACE('',(#7115),#841,.T.);
#60216=ADVANCED_FACE('',(#7116),#842,.T.);
#60217=ADVANCED_FACE('',(#7117),#843,.T.);
#60218=ADVANCED_FACE('',(#7118),#844,.T.);
#60219=ADVANCED_FACE('',(#7119),#845,.T.);
#60220=ADVANCED_FACE('',(#7120),#846,.T.);
#60221=ADVANCED_FACE('',(#7121),#847,.T.);
#60222=ADVANCED_FACE('',(#7122),#848,.T.);
#60223=ADVANCED_FACE('',(#7123),#849,.T.);
#60224=ADVANCED_FACE('',(#7124),#850,.T.);
#60225=ADVANCED_FACE('',(#7125),#851,.T.);
#60226=ADVANCED_FACE('',(#7126),#852,.T.);
#60227=ADVANCED_FACE('',(#7127),#853,.T.);
#60228=ADVANCED_FACE('',(#7128),#854,.T.);
#60229=ADVANCED_FACE('',(#7129),#855,.T.);
#60230=ADVANCED_FACE('',(#7130),#856,.T.);
#60231=ADVANCED_FACE('',(#7131),#857,.T.);
#60232=ADVANCED_FACE('',(#7132),#858,.T.);
#60233=ADVANCED_FACE('',(#7133),#859,.T.);
#60234=ADVANCED_FACE('',(#7134),#860,.T.);
#60235=ADVANCED_FACE('',(#7135),#861,.T.);
#60236=ADVANCED_FACE('',(#7136),#862,.T.);
#60237=ADVANCED_FACE('',(#7137),#863,.T.);
#60238=ADVANCED_FACE('',(#7138),#864,.T.);
#60239=ADVANCED_FACE('',(#7139),#3892,.T.);
#60240=ADVANCED_FACE('',(#7140),#57123,.F.);
#60241=ADVANCED_FACE('',(#7141),#3893,.F.);
#60242=ADVANCED_FACE('',(#7142),#865,.T.);
#60243=ADVANCED_FACE('',(#7143),#57124,.F.);
#60244=ADVANCED_FACE('',(#7144),#108,.F.);
#60245=ADVANCED_FACE('',(#7145),#866,.T.);
#60246=ADVANCED_FACE('',(#7146,#1857),#3894,.F.);
#60247=ADVANCED_FACE('',(#7147),#951,.T.);
#60248=ADVANCED_FACE('',(#7148),#3895,.F.);
#60249=ADVANCED_FACE('',(#7149),#3896,.F.);
#60250=ADVANCED_FACE('',(#7150),#3897,.F.);
#60251=ADVANCED_FACE('',(#7151),#3898,.F.);
#60252=ADVANCED_FACE('',(#7152),#867,.T.);
#60253=ADVANCED_FACE('',(#7153),#3899,.F.);
#60254=ADVANCED_FACE('',(#7154),#3900,.F.);
#60255=ADVANCED_FACE('',(#7155),#3901,.F.);
#60256=ADVANCED_FACE('',(#7156),#3902,.F.);
#60257=ADVANCED_FACE('',(#7157),#3903,.F.);
#60258=ADVANCED_FACE('',(#7158),#3904,.F.);
#60259=ADVANCED_FACE('',(#7159),#3905,.F.);
#60260=ADVANCED_FACE('',(#7160),#3906,.F.);
#60261=ADVANCED_FACE('',(#7161),#3907,.F.);
#60262=ADVANCED_FACE('',(#7162),#3908,.F.);
#60263=ADVANCED_FACE('',(#7163),#3909,.F.);
#60264=ADVANCED_FACE('',(#7164),#3910,.F.);
#60265=ADVANCED_FACE('',(#7165),#3911,.F.);
#60266=ADVANCED_FACE('',(#7166),#3912,.F.);
#60267=ADVANCED_FACE('',(#7167),#3913,.F.);
#60268=ADVANCED_FACE('',(#7168),#3914,.F.);
#60269=ADVANCED_FACE('',(#7169),#3915,.F.);
#60270=ADVANCED_FACE('',(#7170),#3916,.F.);
#60271=ADVANCED_FACE('',(#7171),#3917,.F.);
#60272=ADVANCED_FACE('',(#7172),#3918,.F.);
#60273=ADVANCED_FACE('',(#7173),#3919,.F.);
#60274=ADVANCED_FACE('',(#7174),#3920,.F.);
#60275=ADVANCED_FACE('',(#7175),#3921,.F.);
#60276=ADVANCED_FACE('',(#7176),#3922,.F.);
#60277=ADVANCED_FACE('',(#7177),#3923,.F.);
#60278=ADVANCED_FACE('',(#7178),#3924,.F.);
#60279=ADVANCED_FACE('',(#7179),#3925,.F.);
#60280=ADVANCED_FACE('',(#7180),#3926,.F.);
#60281=ADVANCED_FACE('',(#7181),#3927,.F.);
#60282=ADVANCED_FACE('',(#7182),#3928,.F.);
#60283=ADVANCED_FACE('',(#7183),#3929,.F.);
#60284=ADVANCED_FACE('',(#7184),#3930,.F.);
#60285=ADVANCED_FACE('',(#7185),#3931,.F.);
#60286=ADVANCED_FACE('',(#7186),#3932,.F.);
#60287=ADVANCED_FACE('',(#7187),#3933,.F.);
#60288=ADVANCED_FACE('',(#7188),#3934,.F.);
#60289=ADVANCED_FACE('',(#7189),#3935,.F.);
#60290=ADVANCED_FACE('',(#7190),#3936,.F.);
#60291=ADVANCED_FACE('',(#7191),#3937,.F.);
#60292=ADVANCED_FACE('',(#7192),#3938,.F.);
#60293=ADVANCED_FACE('',(#7193),#3939,.F.);
#60294=ADVANCED_FACE('',(#7194),#3940,.F.);
#60295=ADVANCED_FACE('',(#7195),#3941,.F.);
#60296=ADVANCED_FACE('',(#7196),#3942,.F.);
#60297=ADVANCED_FACE('',(#7197),#3943,.F.);
#60298=ADVANCED_FACE('',(#7198),#3944,.F.);
#60299=ADVANCED_FACE('',(#7199),#3945,.F.);
#60300=ADVANCED_FACE('',(#7200),#3946,.F.);
#60301=ADVANCED_FACE('',(#7201),#3947,.F.);
#60302=ADVANCED_FACE('',(#7202),#3948,.F.);
#60303=ADVANCED_FACE('',(#7203),#3949,.F.);
#60304=ADVANCED_FACE('',(#7204),#3950,.F.);
#60305=ADVANCED_FACE('',(#7205),#3951,.F.);
#60306=ADVANCED_FACE('',(#7206),#3952,.F.);
#60307=ADVANCED_FACE('',(#7207),#3953,.F.);
#60308=ADVANCED_FACE('',(#7208),#3954,.F.);
#60309=ADVANCED_FACE('',(#7209),#3955,.F.);
#60310=ADVANCED_FACE('',(#7210),#3956,.F.);
#60311=ADVANCED_FACE('',(#7211),#3957,.F.);
#60312=ADVANCED_FACE('',(#7212),#3958,.F.);
#60313=ADVANCED_FACE('',(#7213),#3959,.F.);
#60314=ADVANCED_FACE('',(#7214),#3960,.F.);
#60315=ADVANCED_FACE('',(#7215),#3961,.F.);
#60316=ADVANCED_FACE('',(#7216),#3962,.F.);
#60317=ADVANCED_FACE('',(#7217),#3963,.F.);
#60318=ADVANCED_FACE('',(#7218),#3964,.F.);
#60319=ADVANCED_FACE('',(#7219),#3965,.F.);
#60320=ADVANCED_FACE('',(#7220),#3966,.F.);
#60321=ADVANCED_FACE('',(#7221),#3967,.F.);
#60322=ADVANCED_FACE('',(#7222),#3968,.F.);
#60323=ADVANCED_FACE('',(#7223),#3969,.F.);
#60324=ADVANCED_FACE('',(#7224),#3970,.F.);
#60325=ADVANCED_FACE('',(#7225),#3971,.F.);
#60326=ADVANCED_FACE('',(#7226),#3972,.F.);
#60327=ADVANCED_FACE('',(#7227),#3973,.F.);
#60328=ADVANCED_FACE('',(#7228),#3974,.F.);
#60329=ADVANCED_FACE('',(#7229),#3975,.F.);
#60330=ADVANCED_FACE('',(#7230),#3976,.F.);
#60331=ADVANCED_FACE('',(#7231),#3977,.F.);
#60332=ADVANCED_FACE('',(#7232),#3978,.F.);
#60333=ADVANCED_FACE('',(#7233),#3979,.F.);
#60334=ADVANCED_FACE('',(#7234),#3980,.F.);
#60335=ADVANCED_FACE('',(#7235),#3981,.F.);
#60336=ADVANCED_FACE('',(#7236),#3982,.F.);
#60337=ADVANCED_FACE('',(#7237),#3983,.F.);
#60338=ADVANCED_FACE('',(#7238),#3984,.F.);
#60339=ADVANCED_FACE('',(#7239),#3985,.F.);
#60340=ADVANCED_FACE('',(#7240),#3986,.F.);
#60341=ADVANCED_FACE('',(#7241),#3987,.F.);
#60342=ADVANCED_FACE('',(#7242),#3988,.F.);
#60343=ADVANCED_FACE('',(#7243),#3989,.F.);
#60344=ADVANCED_FACE('',(#7244),#3990,.F.);
#60345=ADVANCED_FACE('',(#7245),#3991,.F.);
#60346=ADVANCED_FACE('',(#7246),#3992,.F.);
#60347=ADVANCED_FACE('',(#7247),#3993,.F.);
#60348=ADVANCED_FACE('',(#7248),#3994,.F.);
#60349=ADVANCED_FACE('',(#7249),#3995,.F.);
#60350=ADVANCED_FACE('',(#7250),#3996,.F.);
#60351=ADVANCED_FACE('',(#7251),#3997,.F.);
#60352=ADVANCED_FACE('',(#7252),#3998,.F.);
#60353=ADVANCED_FACE('',(#7253),#3999,.F.);
#60354=ADVANCED_FACE('',(#7254),#4000,.F.);
#60355=ADVANCED_FACE('',(#7255),#4001,.F.);
#60356=ADVANCED_FACE('',(#7256),#4002,.F.);
#60357=ADVANCED_FACE('',(#7257),#4003,.F.);
#60358=ADVANCED_FACE('',(#7258),#109,.T.);
#60359=ADVANCED_FACE('',(#7259),#952,.T.);
#60360=ADVANCED_FACE('',(#7260,#1858),#4004,.T.);
#60361=ADVANCED_FACE('',(#7261),#953,.F.);
#60362=ADVANCED_FACE('',(#7262),#868,.T.);
#60363=ADVANCED_FACE('',(#7263),#869,.T.);
#60364=ADVANCED_FACE('',(#7264),#870,.T.);
#60365=ADVANCED_FACE('',(#7265),#871,.T.);
#60366=ADVANCED_FACE('',(#7266),#872,.T.);
#60367=ADVANCED_FACE('',(#7267),#873,.T.);
#60368=ADVANCED_FACE('',(#7268),#4005,.F.);
#60369=ADVANCED_FACE('',(#7269),#4006,.F.);
#60370=ADVANCED_FACE('',(#7270),#4007,.F.);
#60371=ADVANCED_FACE('',(#7271),#4008,.T.);
#60372=ADVANCED_FACE('',(#7272),#4009,.T.);
#60373=ADVANCED_FACE('',(#7273),#4010,.T.);
#60374=ADVANCED_FACE('',(#7274),#4011,.T.);
#60375=ADVANCED_FACE('',(#7275),#4012,.T.);
#60376=ADVANCED_FACE('',(#7276),#4013,.T.);
#60377=ADVANCED_FACE('',(#7277),#4014,.F.);
#60378=ADVANCED_FACE('',(#7278),#4015,.F.);
#60379=ADVANCED_FACE('',(#7279),#4016,.F.);
#60380=ADVANCED_FACE('',(#7280),#4017,.F.);
#60381=ADVANCED_FACE('',(#7281),#4018,.F.);
#60382=ADVANCED_FACE('',(#7282),#4019,.F.);
#60383=ADVANCED_FACE('',(#7283),#954,.F.);
#60384=ADVANCED_FACE('',(#7284),#4020,.F.);
#60385=ADVANCED_FACE('',(#7285),#4021,.F.);
#60386=ADVANCED_FACE('',(#7286),#4022,.F.);
#60408=CLOSED_SHELL('',(#60214,#60215,#60216,#60217,#60218,#60219,#60220,
#60221,#60222,#60223,#60224,#60225,#60226,#60227,#60228,#60229,#60230,#60231,
#60232,#60233,#60234,#60235,#60236,#60237,#60238,#60239,#60240,#60241,#60242,
#60243,#60244,#60245,#60246,#60247,#60248,#60249,#60250,#60251,#60252,#60253,
#60254,#60255,#60256,#60257,#60258,#60259,#60260,#60261,#60262,#60263,#60264,
#60265,#60266,#60267,#60268,#60269,#60270,#60271,#60272,#60273,#60274,#60275,
#60276,#60277,#60278,#60279,#60280,#60281,#60282,#60283,#60284,#60285,#60286,
#60287,#60288,#60289,#60290,#60291,#60292,#60293,#60294,#60295,#60296,#60297,
#60298,#60299,#60300,#60301,#60302,#60303,#60304,#60305,#60306,#60307,#60308,
#60309,#60310,#60311,#60312,#60313,#60314,#60315,#60316,#60317,#60318,#60319,
#60320,#60321,#60322,#60323,#60324,#60325,#60326,#60327,#60328,#60329,#60330,
#60331,#60332,#60333,#60334,#60335,#60336,#60337,#60338,#60339,#60340,#60341,
#60342,#60343,#60344,#60345,#60346,#60347,#60348,#60349,#60350,#60351,#60352,
#60353,#60354,#60355,#60356,#60357,#60358,#60359,#60360,#60361,#60362,#60363,
#60364,#60365,#60366,#60367,#60368,#60369,#60370,#60371,#60372,#60373,#60374,
#60375,#60376,#60377,#60378,#60379,#60380,#60381,#60382,#60383,#60384,#60385,
#60386));
#63462=AXIS2_PLACEMENT_3D('',#110987,#75273,#75274);
#63463=AXIS2_PLACEMENT_3D('',#110988,#75275,#75276);
#63464=AXIS2_PLACEMENT_3D('',#111004,#75278,#75279);
#63465=AXIS2_PLACEMENT_3D('',#111012,#75280,#75281);
#63466=AXIS2_PLACEMENT_3D('',#111060,#75283,#75284);
#63467=AXIS2_PLACEMENT_3D('',#111108,#75286,#75287);
#63468=AXIS2_PLACEMENT_3D('',#111162,#75289,#75290);
#63469=AXIS2_PLACEMENT_3D('',#111210,#75292,#75293);
#63470=AXIS2_PLACEMENT_3D('',#111258,#75295,#75296);
#63471=AXIS2_PLACEMENT_3D('',#111312,#75298,#75299);
#63472=AXIS2_PLACEMENT_3D('',#111360,#75301,#75302);
#63473=AXIS2_PLACEMENT_3D('',#111408,#75304,#75305);
#63474=AXIS2_PLACEMENT_3D('',#111456,#75307,#75308);
#63475=AXIS2_PLACEMENT_3D('',#111510,#75310,#75311);
#63476=AXIS2_PLACEMENT_3D('',#111558,#75313,#75314);
#63477=AXIS2_PLACEMENT_3D('',#111606,#75316,#75317);
#63478=AXIS2_PLACEMENT_3D('',#111620,#75319,#75320);
#63479=AXIS2_PLACEMENT_3D('',#111628,#75321,#75322);
#63480=AXIS2_PLACEMENT_3D('',#111652,#75324,#75325);
#63481=AXIS2_PLACEMENT_3D('',#111677,#75327,#75328);
#63482=AXIS2_PLACEMENT_3D('',#111702,#75330,#75331);
#63483=AXIS2_PLACEMENT_3D('',#111726,#75333,#75334);
#63484=AXIS2_PLACEMENT_3D('',#111750,#75336,#75337);
#63485=AXIS2_PLACEMENT_3D('',#111775,#75339,#75340);
#63486=AXIS2_PLACEMENT_3D('',#111800,#75342,#75343);
#63487=AXIS2_PLACEMENT_3D('',#111824,#75345,#75346);
#63488=AXIS2_PLACEMENT_3D('',#111849,#75348,#75349);
#63489=AXIS2_PLACEMENT_3D('',#111874,#75351,#75352);
#63490=AXIS2_PLACEMENT_3D('',#111898,#75354,#75355);
#63491=AXIS2_PLACEMENT_3D('',#111983,#75356,#75357);
#63492=AXIS2_PLACEMENT_3D('',#111985,#75358,#75359);
#63493=AXIS2_PLACEMENT_3D('',#112499,#75360,#75361);
#63494=AXIS2_PLACEMENT_3D('',#112501,#75362,#75363);
#63495=AXIS2_PLACEMENT_3D('',#112585,#75364,#75365);
#63496=AXIS2_PLACEMENT_3D('',#112586,#75366,#75367);
#63497=AXIS2_PLACEMENT_3D('',#112587,#75368,#75369);
#63498=AXIS2_PLACEMENT_3D('',#112932,#75370,#75371);
#63499=AXIS2_PLACEMENT_3D('',#112934,#75372,#75373);
#63500=AXIS2_PLACEMENT_3D('',#112935,#75374,#75375);
#63501=AXIS2_PLACEMENT_3D('',#112936,#75376,#75377);
#63502=AXIS2_PLACEMENT_3D('',#112937,#75378,#75379);
#63503=AXIS2_PLACEMENT_3D('',#112938,#75380,#75381);
#63504=AXIS2_PLACEMENT_3D('',#112940,#75382,#75383);
#63505=AXIS2_PLACEMENT_3D('',#112941,#75384,#75385);
#63506=AXIS2_PLACEMENT_3D('',#112944,#75387,#75388);
#63507=AXIS2_PLACEMENT_3D('',#112945,#75389,#75390);
#63508=AXIS2_PLACEMENT_3D('',#112946,#75391,#75392);
#63509=AXIS2_PLACEMENT_3D('',#112957,#75396,#75397);
#63510=AXIS2_PLACEMENT_3D('',#112959,#75398,#75399);
#63511=AXIS2_PLACEMENT_3D('',#112961,#75401,#75402);
#63512=AXIS2_PLACEMENT_3D('',#112967,#75404,#75405);
#63513=AXIS2_PLACEMENT_3D('',#112969,#75406,#75407);
#63514=AXIS2_PLACEMENT_3D('',#112973,#75409,#75410);
#63515=AXIS2_PLACEMENT_3D('',#112977,#75412,#75413);
#63516=AXIS2_PLACEMENT_3D('',#112981,#75415,#75416);
#63517=AXIS2_PLACEMENT_3D('',#112985,#75418,#75419);
#63518=AXIS2_PLACEMENT_3D('',#112989,#75421,#75422);
#63519=AXIS2_PLACEMENT_3D('',#112993,#75424,#75425);
#63520=AXIS2_PLACEMENT_3D('',#112997,#75427,#75428);
#63521=AXIS2_PLACEMENT_3D('',#113001,#75430,#75431);
#63522=AXIS2_PLACEMENT_3D('',#113005,#75433,#75434);
#63523=AXIS2_PLACEMENT_3D('',#113009,#75436,#75437);
#63524=AXIS2_PLACEMENT_3D('',#113013,#75439,#75440);
#63525=AXIS2_PLACEMENT_3D('',#113017,#75442,#75443);
#63526=AXIS2_PLACEMENT_3D('',#113021,#75445,#75446);
#63527=AXIS2_PLACEMENT_3D('',#113025,#75448,#75449);
#63528=AXIS2_PLACEMENT_3D('',#113029,#75451,#75452);
#63529=AXIS2_PLACEMENT_3D('',#113033,#75454,#75455);
#63530=AXIS2_PLACEMENT_3D('',#113037,#75457,#75458);
#63531=AXIS2_PLACEMENT_3D('',#113041,#75460,#75461);
#63532=AXIS2_PLACEMENT_3D('',#113045,#75463,#75464);
#63533=AXIS2_PLACEMENT_3D('',#113049,#75466,#75467);
#63534=AXIS2_PLACEMENT_3D('',#113053,#75469,#75470);
#63535=AXIS2_PLACEMENT_3D('',#113057,#75472,#75473);
#63536=AXIS2_PLACEMENT_3D('',#113061,#75475,#75476);
#63537=AXIS2_PLACEMENT_3D('',#113065,#75478,#75479);
#63538=AXIS2_PLACEMENT_3D('',#113069,#75481,#75482);
#63539=AXIS2_PLACEMENT_3D('',#113073,#75484,#75485);
#63540=AXIS2_PLACEMENT_3D('',#113077,#75487,#75488);
#63541=AXIS2_PLACEMENT_3D('',#113081,#75490,#75491);
#63542=AXIS2_PLACEMENT_3D('',#113085,#75493,#75494);
#63543=AXIS2_PLACEMENT_3D('',#113089,#75496,#75497);
#63544=AXIS2_PLACEMENT_3D('',#113093,#75499,#75500);
#63545=AXIS2_PLACEMENT_3D('',#113097,#75502,#75503);
#63546=AXIS2_PLACEMENT_3D('',#113101,#75505,#75506);
#63547=AXIS2_PLACEMENT_3D('',#113105,#75508,#75509);
#63548=AXIS2_PLACEMENT_3D('',#113109,#75511,#75512);
#63549=AXIS2_PLACEMENT_3D('',#113113,#75514,#75515);
#63550=AXIS2_PLACEMENT_3D('',#113117,#75517,#75518);
#63551=AXIS2_PLACEMENT_3D('',#113121,#75520,#75521);
#63552=AXIS2_PLACEMENT_3D('',#113122,#75522,#75523);
#63553=AXIS2_PLACEMENT_3D('',#113124,#75524,#75525);
#63554=AXIS2_PLACEMENT_3D('',#113128,#75527,#75528);
#63555=AXIS2_PLACEMENT_3D('',#113132,#75530,#75531);
#63556=AXIS2_PLACEMENT_3D('',#113136,#75533,#75534);
#63557=AXIS2_PLACEMENT_3D('',#113140,#75536,#75537);
#63558=AXIS2_PLACEMENT_3D('',#113144,#75539,#75540);
#63559=AXIS2_PLACEMENT_3D('',#113148,#75542,#75543);
#63560=AXIS2_PLACEMENT_3D('',#113152,#75545,#75546);
#63561=AXIS2_PLACEMENT_3D('',#113156,#75548,#75549);
#63562=AXIS2_PLACEMENT_3D('',#113160,#75551,#75552);
#63563=AXIS2_PLACEMENT_3D('',#113164,#75554,#75555);
#63564=AXIS2_PLACEMENT_3D('',#113168,#75557,#75558);
#63565=AXIS2_PLACEMENT_3D('',#113172,#75560,#75561);
#63566=AXIS2_PLACEMENT_3D('',#113176,#75563,#75564);
#63567=AXIS2_PLACEMENT_3D('',#113180,#75566,#75567);
#63568=AXIS2_PLACEMENT_3D('',#113184,#75569,#75570);
#63569=AXIS2_PLACEMENT_3D('',#113188,#75572,#75573);
#63570=AXIS2_PLACEMENT_3D('',#113192,#75575,#75576);
#63571=AXIS2_PLACEMENT_3D('',#113196,#75578,#75579);
#63572=AXIS2_PLACEMENT_3D('',#113200,#75581,#75582);
#63573=AXIS2_PLACEMENT_3D('',#113204,#75584,#75585);
#63574=AXIS2_PLACEMENT_3D('',#113208,#75587,#75588);
#63575=AXIS2_PLACEMENT_3D('',#113212,#75590,#75591);
#63576=AXIS2_PLACEMENT_3D('',#113216,#75593,#75594);
#63577=AXIS2_PLACEMENT_3D('',#113220,#75596,#75597);
#63578=AXIS2_PLACEMENT_3D('',#113224,#75599,#75600);
#63579=AXIS2_PLACEMENT_3D('',#113228,#75602,#75603);
#63580=AXIS2_PLACEMENT_3D('',#113232,#75605,#75606);
#63581=AXIS2_PLACEMENT_3D('',#113236,#75608,#75609);
#63582=AXIS2_PLACEMENT_3D('',#113240,#75611,#75612);
#63583=AXIS2_PLACEMENT_3D('',#113244,#75614,#75615);
#63584=AXIS2_PLACEMENT_3D('',#113248,#75617,#75618);
#63585=AXIS2_PLACEMENT_3D('',#113252,#75620,#75621);
#63586=AXIS2_PLACEMENT_3D('',#113255,#75623,#75624);
#63587=AXIS2_PLACEMENT_3D('',#113256,#75625,#75626);
#63588=AXIS2_PLACEMENT_3D('',#113264,#75629,#75630);
#63589=AXIS2_PLACEMENT_3D('',#113266,#75632,#75633);
#63590=AXIS2_PLACEMENT_3D('',#113270,#75634,#75635);
#63591=AXIS2_PLACEMENT_3D('',#113278,#75638,#75639);
#63592=AXIS2_PLACEMENT_3D('',#113280,#75641,#75642);
#63593=AXIS2_PLACEMENT_3D('',#113284,#75643,#75644);
#63594=AXIS2_PLACEMENT_3D('',#113292,#75647,#75648);
#63595=AXIS2_PLACEMENT_3D('',#113294,#75650,#75651);
#63596=AXIS2_PLACEMENT_3D('',#113298,#75652,#75653);
#63597=AXIS2_PLACEMENT_3D('',#113306,#75656,#75657);
#63598=AXIS2_PLACEMENT_3D('',#113308,#75659,#75660);
#63599=AXIS2_PLACEMENT_3D('',#113312,#75661,#75662);
#63600=AXIS2_PLACEMENT_3D('',#113320,#75665,#75666);
#63601=AXIS2_PLACEMENT_3D('',#113322,#75668,#75669);
#63602=AXIS2_PLACEMENT_3D('',#113326,#75670,#75671);
#63603=AXIS2_PLACEMENT_3D('',#113334,#75674,#75675);
#63604=AXIS2_PLACEMENT_3D('',#113336,#75677,#75678);
#63605=AXIS2_PLACEMENT_3D('',#113340,#75679,#75680);
#63606=AXIS2_PLACEMENT_3D('',#113348,#75683,#75684);
#63607=AXIS2_PLACEMENT_3D('',#113350,#75686,#75687);
#63608=AXIS2_PLACEMENT_3D('',#113354,#75688,#75689);
#63609=AXIS2_PLACEMENT_3D('',#113362,#75692,#75693);
#63610=AXIS2_PLACEMENT_3D('',#113364,#75695,#75696);
#63611=AXIS2_PLACEMENT_3D('',#113368,#75697,#75698);
#63612=AXIS2_PLACEMENT_3D('',#113376,#75701,#75702);
#63613=AXIS2_PLACEMENT_3D('',#113378,#75704,#75705);
#63614=AXIS2_PLACEMENT_3D('',#113382,#75706,#75707);
#63615=AXIS2_PLACEMENT_3D('',#113390,#75710,#75711);
#63616=AXIS2_PLACEMENT_3D('',#113392,#75713,#75714);
#63617=AXIS2_PLACEMENT_3D('',#113396,#75715,#75716);
#63618=AXIS2_PLACEMENT_3D('',#113404,#75719,#75720);
#63619=AXIS2_PLACEMENT_3D('',#113406,#75722,#75723);
#63620=AXIS2_PLACEMENT_3D('',#113410,#75724,#75725);
#63621=AXIS2_PLACEMENT_3D('',#113418,#75728,#75729);
#63622=AXIS2_PLACEMENT_3D('',#113420,#75731,#75732);
#63623=AXIS2_PLACEMENT_3D('',#113424,#75733,#75734);
#63624=AXIS2_PLACEMENT_3D('',#113432,#75737,#75738);
#63625=AXIS2_PLACEMENT_3D('',#113434,#75740,#75741);
#63626=AXIS2_PLACEMENT_3D('',#113438,#75742,#75743);
#63627=AXIS2_PLACEMENT_3D('',#113446,#75746,#75747);
#63628=AXIS2_PLACEMENT_3D('',#113448,#75749,#75750);
#63629=AXIS2_PLACEMENT_3D('',#113452,#75751,#75752);
#63630=AXIS2_PLACEMENT_3D('',#113460,#75755,#75756);
#63631=AXIS2_PLACEMENT_3D('',#113462,#75758,#75759);
#63632=AXIS2_PLACEMENT_3D('',#113466,#75760,#75761);
#63633=AXIS2_PLACEMENT_3D('',#113474,#75764,#75765);
#63634=AXIS2_PLACEMENT_3D('',#113476,#75767,#75768);
#63635=AXIS2_PLACEMENT_3D('',#113480,#75769,#75770);
#63636=AXIS2_PLACEMENT_3D('',#113488,#75773,#75774);
#63637=AXIS2_PLACEMENT_3D('',#113490,#75776,#75777);
#63638=AXIS2_PLACEMENT_3D('',#113494,#75778,#75779);
#63639=AXIS2_PLACEMENT_3D('',#113502,#75782,#75783);
#63640=AXIS2_PLACEMENT_3D('',#113504,#75785,#75786);
#63641=AXIS2_PLACEMENT_3D('',#113508,#75787,#75788);
#63642=AXIS2_PLACEMENT_3D('',#113516,#75791,#75792);
#63643=AXIS2_PLACEMENT_3D('',#113518,#75794,#75795);
#63644=AXIS2_PLACEMENT_3D('',#113522,#75796,#75797);
#63645=AXIS2_PLACEMENT_3D('',#113530,#75800,#75801);
#63646=AXIS2_PLACEMENT_3D('',#113532,#75803,#75804);
#63647=AXIS2_PLACEMENT_3D('',#113536,#75805,#75806);
#63648=AXIS2_PLACEMENT_3D('',#113544,#75809,#75810);
#63649=AXIS2_PLACEMENT_3D('',#113546,#75812,#75813);
#63650=AXIS2_PLACEMENT_3D('',#113550,#75814,#75815);
#63651=AXIS2_PLACEMENT_3D('',#113558,#75818,#75819);
#63652=AXIS2_PLACEMENT_3D('',#113560,#75821,#75822);
#63653=AXIS2_PLACEMENT_3D('',#113564,#75823,#75824);
#63654=AXIS2_PLACEMENT_3D('',#113572,#75827,#75828);
#63655=AXIS2_PLACEMENT_3D('',#113574,#75830,#75831);
#63656=AXIS2_PLACEMENT_3D('',#113578,#75832,#75833);
#63657=AXIS2_PLACEMENT_3D('',#113586,#75836,#75837);
#63658=AXIS2_PLACEMENT_3D('',#113588,#75839,#75840);
#63659=AXIS2_PLACEMENT_3D('',#113592,#75841,#75842);
#63660=AXIS2_PLACEMENT_3D('',#113600,#75845,#75846);
#63661=AXIS2_PLACEMENT_3D('',#113602,#75848,#75849);
#63662=AXIS2_PLACEMENT_3D('',#113606,#75850,#75851);
#63663=AXIS2_PLACEMENT_3D('',#113614,#75854,#75855);
#63664=AXIS2_PLACEMENT_3D('',#113616,#75857,#75858);
#63665=AXIS2_PLACEMENT_3D('',#113620,#75859,#75860);
#63666=AXIS2_PLACEMENT_3D('',#113628,#75863,#75864);
#63667=AXIS2_PLACEMENT_3D('',#113630,#75866,#75867);
#63668=AXIS2_PLACEMENT_3D('',#113634,#75868,#75869);
#63669=AXIS2_PLACEMENT_3D('',#113642,#75872,#75873);
#63670=AXIS2_PLACEMENT_3D('',#113644,#75875,#75876);
#63671=AXIS2_PLACEMENT_3D('',#113648,#75877,#75878);
#63672=AXIS2_PLACEMENT_3D('',#113656,#75881,#75882);
#63673=AXIS2_PLACEMENT_3D('',#113658,#75884,#75885);
#63674=AXIS2_PLACEMENT_3D('',#113662,#75886,#75887);
#63675=AXIS2_PLACEMENT_3D('',#113670,#75890,#75891);
#63676=AXIS2_PLACEMENT_3D('',#113672,#75893,#75894);
#63677=AXIS2_PLACEMENT_3D('',#113676,#75895,#75896);
#63678=AXIS2_PLACEMENT_3D('',#113684,#75899,#75900);
#63679=AXIS2_PLACEMENT_3D('',#113686,#75902,#75903);
#63680=AXIS2_PLACEMENT_3D('',#113690,#75904,#75905);
#63681=AXIS2_PLACEMENT_3D('',#113698,#75908,#75909);
#63682=AXIS2_PLACEMENT_3D('',#113700,#75911,#75912);
#63683=AXIS2_PLACEMENT_3D('',#113704,#75913,#75914);
#63684=AXIS2_PLACEMENT_3D('',#113712,#75917,#75918);
#63685=AXIS2_PLACEMENT_3D('',#113714,#75920,#75921);
#63686=AXIS2_PLACEMENT_3D('',#113718,#75922,#75923);
#63687=AXIS2_PLACEMENT_3D('',#113726,#75926,#75927);
#63688=AXIS2_PLACEMENT_3D('',#113728,#75929,#75930);
#63689=AXIS2_PLACEMENT_3D('',#113732,#75931,#75932);
#63690=AXIS2_PLACEMENT_3D('',#113740,#75935,#75936);
#63691=AXIS2_PLACEMENT_3D('',#113742,#75938,#75939);
#63692=AXIS2_PLACEMENT_3D('',#113746,#75940,#75941);
#63693=AXIS2_PLACEMENT_3D('',#113747,#75942,#75943);
#63694=AXIS2_PLACEMENT_3D('',#113748,#75944,#75945);
#63695=AXIS2_PLACEMENT_3D('',#113750,#75946,#75947);
#63696=AXIS2_PLACEMENT_3D('',#113752,#75949,#75950);
#63697=AXIS2_PLACEMENT_3D('',#113754,#75951,#75952);
#63698=AXIS2_PLACEMENT_3D('',#113755,#75953,#75954);
#63699=AXIS2_PLACEMENT_3D('',#113763,#75956,#75957);
#63700=AXIS2_PLACEMENT_3D('',#113773,#75958,#75959);
#63701=AXIS2_PLACEMENT_3D('',#113783,#75960,#75961);
#63702=AXIS2_PLACEMENT_3D('',#113793,#75962,#75963);
#63703=AXIS2_PLACEMENT_3D('',#113803,#75964,#75965);
#63704=AXIS2_PLACEMENT_3D('',#113813,#75966,#75967);
#63705=AXIS2_PLACEMENT_3D('',#113817,#75968,#75969);
#63706=AXIS2_PLACEMENT_3D('',#113822,#75972,#75973);
#63707=AXIS2_PLACEMENT_3D('',#113823,#75974,#75975);
#63708=AXIS2_PLACEMENT_3D('',#113828,#75978,#75979);
#63709=AXIS2_PLACEMENT_3D('',#113829,#75980,#75981);
#63710=AXIS2_PLACEMENT_3D('',#113833,#75983,#75984);
#63711=AXIS2_PLACEMENT_3D('',#113835,#75986,#75987);
#63712=AXIS2_PLACEMENT_3D('',#113840,#75990,#75991);
#63713=AXIS2_PLACEMENT_3D('',#113841,#75992,#75993);
#63714=AXIS2_PLACEMENT_3D('',#113845,#75995,#75996);
#63715=AXIS2_PLACEMENT_3D('',#113847,#75998,#75999);
#63716=AXIS2_PLACEMENT_3D('',#113851,#76001,#76002);
#63717=AXIS2_PLACEMENT_3D('',#113853,#76004,#76005);
#63718=AXIS2_PLACEMENT_3D('',#113860,#76010,#76011);
#63719=AXIS2_PLACEMENT_3D('',#113865,#76015,#76016);
#63720=AXIS2_PLACEMENT_3D('',#113870,#76020,#76021);
#63721=AXIS2_PLACEMENT_3D('',#113871,#76022,#76023);
#63722=AXIS2_PLACEMENT_3D('',#113872,#76024,#76025);
#63723=AXIS2_PLACEMENT_3D('',#113874,#76027,#76028);
#63724=AXIS2_PLACEMENT_3D('',#113875,#76029,#76030);
#63725=AXIS2_PLACEMENT_3D('',#113877,#76032,#76033);
#63726=AXIS2_PLACEMENT_3D('',#113879,#76035,#76036);
#63727=AXIS2_PLACEMENT_3D('',#113882,#76038,#76039);
#63728=AXIS2_PLACEMENT_3D('',#113883,#76040,#76041);
#63729=AXIS2_PLACEMENT_3D('',#113884,#76042,#76043);
#63730=AXIS2_PLACEMENT_3D('',#113885,#76044,#76045);
#63731=AXIS2_PLACEMENT_3D('',#113886,#76046,#76047);
#63732=AXIS2_PLACEMENT_3D('',#113887,#76048,#76049);
#63733=AXIS2_PLACEMENT_3D('',#113888,#76050,#76051);
#63734=AXIS2_PLACEMENT_3D('',#113889,#76052,#76053);
#63735=AXIS2_PLACEMENT_3D('',#113892,#76055,#76056);
#63736=AXIS2_PLACEMENT_3D('',#113893,#76057,#76058);
#63737=AXIS2_PLACEMENT_3D('',#113895,#76060,#76061);
#63738=AXIS2_PLACEMENT_3D('',#113896,#76062,#76063);
#63739=AXIS2_PLACEMENT_3D('',#113899,#76065,#76066);
#63740=AXIS2_PLACEMENT_3D('',#113901,#76068,#76069);
#63741=AXIS2_PLACEMENT_3D('',#113903,#76071,#76072);
#75273=DIRECTION('axis',(0.,0.,1.));
#75274=DIRECTION('refdir',(1.,0.,0.));
#75275=DIRECTION('center_axis',(0.,-1.,0.));
#75276=DIRECTION('ref_axis',(1.,0.,0.));
#75277=DIRECTION('',(0.,1.,0.));
#75278=DIRECTION('center_axis',(0.,1.,0.));
#75279=DIRECTION('ref_axis',(1.,0.,0.));
#75280=DIRECTION('center_axis',(0.,-1.,0.));
#75281=DIRECTION('ref_axis',(1.,0.,0.));
#75282=DIRECTION('',(0.,1.,0.));
#75283=DIRECTION('center_axis',(0.,-1.,0.));
#75284=DIRECTION('ref_axis',(1.,0.,0.));
#75285=DIRECTION('',(0.,1.,0.));
#75286=DIRECTION('center_axis',(0.,-1.,0.));
#75287=DIRECTION('ref_axis',(1.,0.,0.));
#75288=DIRECTION('',(0.,1.,0.));
#75289=DIRECTION('center_axis',(0.,-1.,0.));
#75290=DIRECTION('ref_axis',(1.,0.,0.));
#75291=DIRECTION('',(0.,1.,0.));
#75292=DIRECTION('center_axis',(0.,-1.,0.));
#75293=DIRECTION('ref_axis',(1.,0.,0.));
#75294=DIRECTION('',(0.,1.,0.));
#75295=DIRECTION('center_axis',(0.,-1.,0.));
#75296=DIRECTION('ref_axis',(1.,0.,0.));
#75297=DIRECTION('',(0.,1.,0.));
#75298=DIRECTION('center_axis',(0.,-1.,0.));
#75299=DIRECTION('ref_axis',(1.,0.,0.));
#75300=DIRECTION('',(0.,1.,0.));
#75301=DIRECTION('center_axis',(0.,-1.,0.));
#75302=DIRECTION('ref_axis',(1.,0.,0.));
#75303=DIRECTION('',(0.,1.,0.));
#75304=DIRECTION('center_axis',(0.,-1.,0.));
#75305=DIRECTION('ref_axis',(1.,0.,0.));
#75306=DIRECTION('',(0.,1.,0.));
#75307=DIRECTION('center_axis',(0.,-1.,0.));
#75308=DIRECTION('ref_axis',(1.,0.,0.));
#75309=DIRECTION('',(0.,1.,0.));
#75310=DIRECTION('center_axis',(0.,-1.,0.));
#75311=DIRECTION('ref_axis',(1.,0.,0.));
#75312=DIRECTION('',(0.,1.,0.));
#75313=DIRECTION('center_axis',(0.,-1.,0.));
#75314=DIRECTION('ref_axis',(1.,0.,0.));
#75315=DIRECTION('',(0.,1.,0.));
#75316=DIRECTION('center_axis',(0.,-1.,0.));
#75317=DIRECTION('ref_axis',(1.,0.,8.34187923537817E-14));
#75318=DIRECTION('',(0.,-1.,0.));
#75319=DIRECTION('center_axis',(0.,-1.,0.));
#75320=DIRECTION('ref_axis',(1.,0.,8.34187923537817E-14));
#75321=DIRECTION('center_axis',(0.,-1.,0.));
#75322=DIRECTION('ref_axis',(1.,0.,8.34187923537817E-14));
#75323=DIRECTION('',(0.,-1.,0.));
#75324=DIRECTION('center_axis',(0.,-1.,0.));
#75325=DIRECTION('ref_axis',(1.,0.,8.34187923537817E-14));
#75326=DIRECTION('',(0.,-1.,0.));
#75327=DIRECTION('center_axis',(0.,-1.,0.));
#75328=DIRECTION('ref_axis',(1.,0.,8.34187923537817E-14));
#75329=DIRECTION('',(0.,-1.,0.));
#75330=DIRECTION('center_axis',(0.,-1.,0.));
#75331=DIRECTION('ref_axis',(1.,0.,8.34187923537817E-14));
#75332=DIRECTION('',(0.,-1.,0.));
#75333=DIRECTION('center_axis',(0.,-1.,0.));
#75334=DIRECTION('ref_axis',(1.,0.,8.34187923537817E-14));
#75335=DIRECTION('',(0.,-1.,0.));
#75336=DIRECTION('center_axis',(0.,-1.,0.));
#75337=DIRECTION('ref_axis',(1.,0.,8.34187923537817E-14));
#75338=DIRECTION('',(0.,-1.,0.));
#75339=DIRECTION('center_axis',(0.,-1.,0.));
#75340=DIRECTION('ref_axis',(1.,0.,8.34187923537817E-14));
#75341=DIRECTION('',(0.,-1.,0.));
#75342=DIRECTION('center_axis',(0.,-1.,0.));
#75343=DIRECTION('ref_axis',(1.,0.,8.34187923537817E-14));
#75344=DIRECTION('',(0.,-1.,0.));
#75345=DIRECTION('center_axis',(0.,-1.,0.));
#75346=DIRECTION('ref_axis',(1.,0.,8.34187923537817E-14));
#75347=DIRECTION('',(0.,-1.,0.));
#75348=DIRECTION('center_axis',(0.,-1.,0.));
#75349=DIRECTION('ref_axis',(1.,0.,8.34187923537817E-14));
#75350=DIRECTION('',(0.,-1.,0.));
#75351=DIRECTION('center_axis',(0.,-1.,0.));
#75352=DIRECTION('ref_axis',(1.,0.,8.34187923537817E-14));
#75353=DIRECTION('',(0.,-1.,0.));
#75354=DIRECTION('center_axis',(0.,1.,0.));
#75355=DIRECTION('ref_axis',(0.,0.,1.));
#75356=DIRECTION('center_axis',(0.,-1.,0.));
#75357=DIRECTION('ref_axis',(1.,0.,0.));
#75358=DIRECTION('center_axis',(0.,-1.,0.));
#75359=DIRECTION('ref_axis',(1.,0.,0.));
#75360=DIRECTION('center_axis',(0.,1.,0.));
#75361=DIRECTION('ref_axis',(0.,0.,1.));
#75362=DIRECTION('center_axis',(0.,1.,0.));
#75363=DIRECTION('ref_axis',(1.,0.,0.));
#75364=DIRECTION('center_axis',(0.,1.,0.));
#75365=DIRECTION('ref_axis',(1.,0.,8.34187923537817E-14));
#75366=DIRECTION('center_axis',(0.,1.,0.));
#75367=DIRECTION('ref_axis',(1.,0.,0.));
#75368=DIRECTION('center_axis',(0.,-1.,0.));
#75369=DIRECTION('ref_axis',(1.,0.,8.34187923537817E-14));
#75370=DIRECTION('center_axis',(0.,1.,0.));
#75371=DIRECTION('ref_axis',(0.,0.,1.));
#75372=DIRECTION('center_axis',(-1.,0.,0.));
#75373=DIRECTION('ref_axis',(0.,0.,-1.));
#75374=DIRECTION('center_axis',(0.,-1.,0.));
#75375=DIRECTION('ref_axis',(1.,0.,0.));
#75376=DIRECTION('center_axis',(0.,-1.,0.));
#75377=DIRECTION('ref_axis',(1.,0.,0.));
#75378=DIRECTION('center_axis',(0.,-1.,0.));
#75379=DIRECTION('ref_axis',(1.,0.,0.));
#75380=DIRECTION('center_axis',(0.,1.,0.));
#75381=DIRECTION('ref_axis',(1.,0.,0.));
#75382=DIRECTION('center_axis',(0.,1.,0.));
#75383=DIRECTION('ref_axis',(1.,0.,0.));
#75384=DIRECTION('center_axis',(0.,1.,0.));
#75385=DIRECTION('ref_axis',(1.,0.,0.));
#75386=DIRECTION('',(0.707106781186548,-0.707106781186548,-8.65956056235493E-17));
#75387=DIRECTION('center_axis',(0.,1.,0.));
#75388=DIRECTION('ref_axis',(1.,0.,0.));
#75389=DIRECTION('center_axis',(0.,1.,0.));
#75390=DIRECTION('ref_axis',(1.,0.,0.));
#75391=DIRECTION('center_axis',(-0.493533981978479,0.,-0.869726513699833));
#75392=DIRECTION('ref_axis',(0.869726513699833,0.,-0.493533981978479));
#75393=DIRECTION('',(0.,-1.,0.));
#75394=DIRECTION('',(0.869726513699833,0.,-0.493533981978479));
#75395=DIRECTION('',(0.,-1.,0.));
#75396=DIRECTION('center_axis',(0.,-1.,0.));
#75397=DIRECTION('ref_axis',(-0.17364817766693,0.,-0.984807753012208));
#75398=DIRECTION('center_axis',(0.,-1.,0.));
#75399=DIRECTION('ref_axis',(1.,0.,0.));
#75400=DIRECTION('',(-0.986074150277955,0.,-0.166306254102511));
#75401=DIRECTION('center_axis',(-0.166306254102511,0.,0.986074150277955));
#75402=DIRECTION('ref_axis',(-0.986074150277955,0.,-0.166306254102511));
#75403=DIRECTION('',(0.,1.,0.));
#75404=DIRECTION('center_axis',(0.,1.,0.));
#75405=DIRECTION('ref_axis',(1.,0.,0.));
#75406=DIRECTION('center_axis',(0.,1.,0.));
#75407=DIRECTION('ref_axis',(1.,0.,0.));
#75408=DIRECTION('',(0.,-1.,0.));
#75409=DIRECTION('center_axis',(0.,-1.,0.));
#75410=DIRECTION('ref_axis',(1.,0.,0.));
#75411=DIRECTION('',(0.,1.,0.));
#75412=DIRECTION('center_axis',(0.,1.,0.));
#75413=DIRECTION('ref_axis',(1.,0.,0.));
#75414=DIRECTION('',(0.,-1.,0.));
#75415=DIRECTION('center_axis',(0.,-1.,0.));
#75416=DIRECTION('ref_axis',(1.,0.,0.));
#75417=DIRECTION('',(0.,1.,0.));
#75418=DIRECTION('center_axis',(0.,1.,0.));
#75419=DIRECTION('ref_axis',(1.,0.,0.));
#75420=DIRECTION('',(0.,-1.,0.));
#75421=DIRECTION('center_axis',(0.,-1.,0.));
#75422=DIRECTION('ref_axis',(1.,0.,0.));
#75423=DIRECTION('',(0.,1.,0.));
#75424=DIRECTION('center_axis',(0.,1.,0.));
#75425=DIRECTION('ref_axis',(1.,0.,0.));
#75426=DIRECTION('',(0.,-1.,0.));
#75427=DIRECTION('center_axis',(0.,-1.,0.));
#75428=DIRECTION('ref_axis',(1.,0.,0.));
#75429=DIRECTION('',(0.,1.,0.));
#75430=DIRECTION('center_axis',(0.,1.,0.));
#75431=DIRECTION('ref_axis',(1.,0.,0.));
#75432=DIRECTION('',(0.,-1.,0.));
#75433=DIRECTION('center_axis',(0.,-1.,0.));
#75434=DIRECTION('ref_axis',(1.,0.,0.));
#75435=DIRECTION('',(0.,1.,0.));
#75436=DIRECTION('center_axis',(0.,1.,0.));
#75437=DIRECTION('ref_axis',(1.,0.,0.));
#75438=DIRECTION('',(0.,-1.,0.));
#75439=DIRECTION('center_axis',(0.,-1.,0.));
#75440=DIRECTION('ref_axis',(1.,0.,0.));
#75441=DIRECTION('',(0.,1.,0.));
#75442=DIRECTION('center_axis',(0.,1.,0.));
#75443=DIRECTION('ref_axis',(1.,0.,0.));
#75444=DIRECTION('',(0.,-1.,0.));
#75445=DIRECTION('center_axis',(0.,-1.,0.));
#75446=DIRECTION('ref_axis',(1.,0.,0.));
#75447=DIRECTION('',(0.,1.,0.));
#75448=DIRECTION('center_axis',(0.,1.,0.));
#75449=DIRECTION('ref_axis',(1.,0.,0.));
#75450=DIRECTION('',(0.,-1.,0.));
#75451=DIRECTION('center_axis',(0.,-1.,0.));
#75452=DIRECTION('ref_axis',(1.,0.,0.));
#75453=DIRECTION('',(0.,1.,0.));
#75454=DIRECTION('center_axis',(0.,1.,0.));
#75455=DIRECTION('ref_axis',(1.,0.,0.));
#75456=DIRECTION('',(0.,-1.,0.));
#75457=DIRECTION('center_axis',(0.,-1.,0.));
#75458=DIRECTION('ref_axis',(1.,0.,0.));
#75459=DIRECTION('',(0.,1.,0.));
#75460=DIRECTION('center_axis',(0.,1.,0.));
#75461=DIRECTION('ref_axis',(1.,0.,0.));
#75462=DIRECTION('',(0.,-1.,0.));
#75463=DIRECTION('center_axis',(0.,-1.,0.));
#75464=DIRECTION('ref_axis',(1.,0.,0.));
#75465=DIRECTION('',(0.,1.,0.));
#75466=DIRECTION('center_axis',(0.,1.,0.));
#75467=DIRECTION('ref_axis',(1.,0.,0.));
#75468=DIRECTION('',(0.,-1.,0.));
#75469=DIRECTION('center_axis',(0.,-1.,0.));
#75470=DIRECTION('ref_axis',(1.,0.,0.));
#75471=DIRECTION('',(0.,1.,0.));
#75472=DIRECTION('center_axis',(0.,1.,0.));
#75473=DIRECTION('ref_axis',(1.,0.,0.));
#75474=DIRECTION('',(0.,-1.,0.));
#75475=DIRECTION('center_axis',(0.,-1.,0.));
#75476=DIRECTION('ref_axis',(1.,0.,0.));
#75477=DIRECTION('',(0.,1.,0.));
#75478=DIRECTION('center_axis',(0.,1.,0.));
#75479=DIRECTION('ref_axis',(1.,0.,0.));
#75480=DIRECTION('',(0.,-1.,0.));
#75481=DIRECTION('center_axis',(0.,-1.,0.));
#75482=DIRECTION('ref_axis',(1.,0.,0.));
#75483=DIRECTION('',(0.,1.,0.));
#75484=DIRECTION('center_axis',(0.,1.,0.));
#75485=DIRECTION('ref_axis',(1.,0.,0.));
#75486=DIRECTION('',(0.,-1.,0.));
#75487=DIRECTION('center_axis',(0.,-1.,0.));
#75488=DIRECTION('ref_axis',(1.,0.,0.));
#75489=DIRECTION('',(0.,1.,0.));
#75490=DIRECTION('center_axis',(0.,1.,0.));
#75491=DIRECTION('ref_axis',(1.,0.,0.));
#75492=DIRECTION('',(0.,-1.,0.));
#75493=DIRECTION('center_axis',(0.,-1.,0.));
#75494=DIRECTION('ref_axis',(1.,0.,0.));
#75495=DIRECTION('',(0.,1.,0.));
#75496=DIRECTION('center_axis',(0.,1.,0.));
#75497=DIRECTION('ref_axis',(1.,0.,0.));
#75498=DIRECTION('',(0.,-1.,0.));
#75499=DIRECTION('center_axis',(0.,-1.,0.));
#75500=DIRECTION('ref_axis',(1.,0.,0.));
#75501=DIRECTION('',(0.,1.,0.));
#75502=DIRECTION('center_axis',(0.,1.,0.));
#75503=DIRECTION('ref_axis',(1.,0.,0.));
#75504=DIRECTION('',(0.,-1.,0.));
#75505=DIRECTION('center_axis',(0.,-1.,0.));
#75506=DIRECTION('ref_axis',(1.,0.,0.));
#75507=DIRECTION('',(0.,1.,0.));
#75508=DIRECTION('center_axis',(0.,1.,0.));
#75509=DIRECTION('ref_axis',(1.,0.,0.));
#75510=DIRECTION('',(0.,-1.,0.));
#75511=DIRECTION('center_axis',(0.,-1.,0.));
#75512=DIRECTION('ref_axis',(1.,0.,0.));
#75513=DIRECTION('',(0.,1.,0.));
#75514=DIRECTION('center_axis',(0.,1.,0.));
#75515=DIRECTION('ref_axis',(1.,0.,0.));
#75516=DIRECTION('',(0.,-1.,0.));
#75517=DIRECTION('center_axis',(0.,-1.,0.));
#75518=DIRECTION('ref_axis',(1.,0.,0.));
#75519=DIRECTION('',(0.,-1.,0.));
#75520=DIRECTION('center_axis',(0.,-1.,0.));
#75521=DIRECTION('ref_axis',(1.,0.,0.));
#75522=DIRECTION('center_axis',(0.,-1.,0.));
#75523=DIRECTION('ref_axis',(1.,0.,0.));
#75524=DIRECTION('center_axis',(0.,-1.,0.));
#75525=DIRECTION('ref_axis',(1.,0.,0.));
#75526=DIRECTION('',(0.,1.,0.));
#75527=DIRECTION('center_axis',(0.,1.,0.));
#75528=DIRECTION('ref_axis',(1.,0.,0.));
#75529=DIRECTION('',(0.,-1.,0.));
#75530=DIRECTION('center_axis',(0.,-1.,0.));
#75531=DIRECTION('ref_axis',(1.,0.,0.));
#75532=DIRECTION('',(0.,1.,0.));
#75533=DIRECTION('center_axis',(0.,1.,0.));
#75534=DIRECTION('ref_axis',(1.,0.,0.));
#75535=DIRECTION('',(0.,-1.,0.));
#75536=DIRECTION('center_axis',(0.,-1.,0.));
#75537=DIRECTION('ref_axis',(1.,0.,0.));
#75538=DIRECTION('',(0.,1.,0.));
#75539=DIRECTION('center_axis',(0.,1.,0.));
#75540=DIRECTION('ref_axis',(1.,0.,0.));
#75541=DIRECTION('',(0.,-1.,0.));
#75542=DIRECTION('center_axis',(0.,-1.,0.));
#75543=DIRECTION('ref_axis',(1.,0.,0.));
#75544=DIRECTION('',(0.,1.,0.));
#75545=DIRECTION('center_axis',(0.,1.,0.));
#75546=DIRECTION('ref_axis',(1.,0.,0.));
#75547=DIRECTION('',(0.,-1.,0.));
#75548=DIRECTION('center_axis',(0.,-1.,0.));
#75549=DIRECTION('ref_axis',(1.,0.,0.));
#75550=DIRECTION('',(0.,1.,0.));
#75551=DIRECTION('center_axis',(0.,1.,0.));
#75552=DIRECTION('ref_axis',(1.,0.,0.));
#75553=DIRECTION('',(0.,-1.,0.));
#75554=DIRECTION('center_axis',(0.,-1.,0.));
#75555=DIRECTION('ref_axis',(1.,0.,0.));
#75556=DIRECTION('',(0.,1.,0.));
#75557=DIRECTION('center_axis',(0.,1.,0.));
#75558=DIRECTION('ref_axis',(1.,0.,0.));
#75559=DIRECTION('',(0.,-1.,0.));
#75560=DIRECTION('center_axis',(0.,-1.,0.));
#75561=DIRECTION('ref_axis',(1.,0.,0.));
#75562=DIRECTION('',(0.,1.,0.));
#75563=DIRECTION('center_axis',(0.,1.,0.));
#75564=DIRECTION('ref_axis',(1.,0.,0.));
#75565=DIRECTION('',(0.,-1.,0.));
#75566=DIRECTION('center_axis',(0.,-1.,0.));
#75567=DIRECTION('ref_axis',(1.,0.,0.));
#75568=DIRECTION('',(0.,1.,0.));
#75569=DIRECTION('center_axis',(0.,1.,0.));
#75570=DIRECTION('ref_axis',(1.,0.,0.));
#75571=DIRECTION('',(0.,-1.,0.));
#75572=DIRECTION('center_axis',(0.,-1.,0.));
#75573=DIRECTION('ref_axis',(1.,0.,0.));
#75574=DIRECTION('',(0.,1.,0.));
#75575=DIRECTION('center_axis',(0.,1.,0.));
#75576=DIRECTION('ref_axis',(1.,0.,0.));
#75577=DIRECTION('',(0.,-1.,0.));
#75578=DIRECTION('center_axis',(0.,-1.,0.));
#75579=DIRECTION('ref_axis',(1.,0.,0.));
#75580=DIRECTION('',(0.,1.,0.));
#75581=DIRECTION('center_axis',(0.,1.,0.));
#75582=DIRECTION('ref_axis',(1.,0.,0.));
#75583=DIRECTION('',(0.,-1.,0.));
#75584=DIRECTION('center_axis',(0.,-1.,0.));
#75585=DIRECTION('ref_axis',(1.,0.,0.));
#75586=DIRECTION('',(0.,1.,0.));
#75587=DIRECTION('center_axis',(0.,1.,0.));
#75588=DIRECTION('ref_axis',(1.,0.,0.));
#75589=DIRECTION('',(0.,-1.,0.));
#75590=DIRECTION('center_axis',(0.,-1.,0.));
#75591=DIRECTION('ref_axis',(1.,0.,0.));
#75592=DIRECTION('',(0.,1.,0.));
#75593=DIRECTION('center_axis',(0.,1.,0.));
#75594=DIRECTION('ref_axis',(1.,0.,0.));
#75595=DIRECTION('',(0.,-1.,0.));
#75596=DIRECTION('center_axis',(0.,-1.,0.));
#75597=DIRECTION('ref_axis',(1.,0.,0.));
#75598=DIRECTION('',(0.,1.,0.));
#75599=DIRECTION('center_axis',(0.,1.,0.));
#75600=DIRECTION('ref_axis',(1.,0.,0.));
#75601=DIRECTION('',(0.,-1.,0.));
#75602=DIRECTION('center_axis',(0.,-1.,0.));
#75603=DIRECTION('ref_axis',(1.,0.,0.));
#75604=DIRECTION('',(0.,1.,0.));
#75605=DIRECTION('center_axis',(0.,1.,0.));
#75606=DIRECTION('ref_axis',(1.,0.,0.));
#75607=DIRECTION('',(0.,-1.,0.));
#75608=DIRECTION('center_axis',(0.,-1.,0.));
#75609=DIRECTION('ref_axis',(1.,0.,0.));
#75610=DIRECTION('',(0.,1.,0.));
#75611=DIRECTION('center_axis',(0.,1.,0.));
#75612=DIRECTION('ref_axis',(1.,0.,0.));
#75613=DIRECTION('',(0.,-1.,0.));
#75614=DIRECTION('center_axis',(0.,-1.,0.));
#75615=DIRECTION('ref_axis',(1.,0.,0.));
#75616=DIRECTION('',(0.,1.,0.));
#75617=DIRECTION('center_axis',(0.,1.,0.));
#75618=DIRECTION('ref_axis',(1.,0.,0.));
#75619=DIRECTION('',(0.,-1.,0.));
#75620=DIRECTION('center_axis',(0.,-1.,0.));
#75621=DIRECTION('ref_axis',(1.,0.,0.));
#75622=DIRECTION('',(0.,1.,0.));
#75623=DIRECTION('center_axis',(0.,1.,0.));
#75624=DIRECTION('ref_axis',(1.,0.,0.));
#75625=DIRECTION('center_axis',(-0.637062515999983,0.,-0.770812137104607));
#75626=DIRECTION('ref_axis',(0.770812137104607,0.,-0.637062515999983));
#75627=DIRECTION('',(0.,-1.,0.));
#75628=DIRECTION('',(0.770812137104607,0.,-0.637062515999983));
#75629=DIRECTION('center_axis',(0.,-1.,0.));
#75630=DIRECTION('ref_axis',(-0.342020143325669,0.,-0.939692620785908));
#75631=DIRECTION('',(-0.99997224619817,0.,0.0074502908256634));
#75632=DIRECTION('center_axis',(0.00745029082566334,0.,0.99997224619817));
#75633=DIRECTION('ref_axis',(-0.99997224619817,0.,0.00745029082566334));
#75634=DIRECTION('center_axis',(-0.761234227842014,0.,-0.64847702377322));
#75635=DIRECTION('ref_axis',(0.64847702377322,0.,-0.761234227842014));
#75636=DIRECTION('',(0.,-1.,0.));
#75637=DIRECTION('',(0.64847702377322,0.,-0.761234227842014));
#75638=DIRECTION('center_axis',(0.,-1.,0.));
#75639=DIRECTION('ref_axis',(-0.5,0.,-0.866025403784438));
#75640=DIRECTION('',(-0.983486691428025,0.,0.180980462437128));
#75641=DIRECTION('center_axis',(0.180980462437128,0.,0.983486691428025));
#75642=DIRECTION('ref_axis',(-0.983486691428025,0.,0.180980462437128));
#75643=DIRECTION('center_axis',(-0.862276222874171,0.,-0.506438264219691));
#75644=DIRECTION('ref_axis',(0.506438264219691,0.,-0.862276222874171));
#75645=DIRECTION('',(0.,-1.,0.));
#75646=DIRECTION('',(0.506438264219691,0.,-0.862276222874171));
#75647=DIRECTION('center_axis',(0.,-1.,0.));
#75648=DIRECTION('ref_axis',(-0.64278760968654,0.,-0.766044443118978));
#75649=DIRECTION('',(-0.937118391207119,0.,0.349011634277973));
#75650=DIRECTION('center_axis',(0.349011634277973,0.,0.937118391207119));
#75651=DIRECTION('ref_axis',(-0.937118391207118,0.,0.349011634277973));
#75652=DIRECTION('center_axis',(-0.937118391207119,0.,-0.349011634277973));
#75653=DIRECTION('ref_axis',(0.349011634277973,0.,-0.937118391207119));
#75654=DIRECTION('',(0.,-1.,0.));
#75655=DIRECTION('',(0.349011634277973,0.,-0.937118391207119));
#75656=DIRECTION('center_axis',(0.,-1.,0.));
#75657=DIRECTION('ref_axis',(-0.766044443118978,0.,-0.642787609686539));
#75658=DIRECTION('',(-0.862276222874171,0.,0.506438264219691));
#75659=DIRECTION('center_axis',(0.506438264219691,0.,0.862276222874171));
#75660=DIRECTION('ref_axis',(-0.862276222874171,0.,0.506438264219691));
#75661=DIRECTION('center_axis',(-0.983486691428025,0.,-0.180980462437128));
#75662=DIRECTION('ref_axis',(0.180980462437128,0.,-0.983486691428025));
#75663=DIRECTION('',(0.,-1.,0.));
#75664=DIRECTION('',(0.180980462437128,0.,-0.983486691428025));
#75665=DIRECTION('center_axis',(0.,-1.,0.));
#75666=DIRECTION('ref_axis',(-0.866025403784439,0.,-0.5));
#75667=DIRECTION('',(-0.761234227842013,0.,0.64847702377322));
#75668=DIRECTION('center_axis',(0.64847702377322,0.,0.761234227842013));
#75669=DIRECTION('ref_axis',(-0.761234227842013,0.,0.64847702377322));
#75670=DIRECTION('center_axis',(-0.99997224619817,0.,-0.00745029082566206));
#75671=DIRECTION('ref_axis',(0.00745029082566206,0.,-0.99997224619817));
#75672=DIRECTION('',(0.,-1.,0.));
#75673=DIRECTION('',(0.00745029082566206,0.,-0.99997224619817));
#75674=DIRECTION('center_axis',(0.,-1.,0.));
#75675=DIRECTION('ref_axis',(-0.939692620785909,0.,-0.342020143325668));
#75676=DIRECTION('',(-0.637062515999982,0.,0.770812137104608));
#75677=DIRECTION('center_axis',(0.770812137104608,0.,0.637062515999982));
#75678=DIRECTION('ref_axis',(-0.637062515999982,0.,0.770812137104608));
#75679=DIRECTION('center_axis',(-0.986074150277955,0.,0.166306254102511));
#75680=DIRECTION('ref_axis',(-0.166306254102511,0.,-0.986074150277955));
#75681=DIRECTION('',(0.,-1.,0.));
#75682=DIRECTION('',(-0.166306254102511,0.,-0.986074150277955));
#75683=DIRECTION('center_axis',(0.,-1.,0.));
#75684=DIRECTION('ref_axis',(-0.984807753012208,0.,-0.17364817766693));
#75685=DIRECTION('',(-0.493533981978478,0.,0.869726513699834));
#75686=DIRECTION('center_axis',(0.869726513699834,0.,0.493533981978479));
#75687=DIRECTION('ref_axis',(-0.493533981978479,0.,0.869726513699834));
#75688=DIRECTION('center_axis',(-0.942214690279141,0.,0.335009667654805));
#75689=DIRECTION('ref_axis',(-0.335009667654805,0.,-0.942214690279141));
#75690=DIRECTION('',(0.,-1.,0.));
#75691=DIRECTION('',(-0.335009667654805,0.,-0.942214690279141));
#75692=DIRECTION('center_axis',(0.,-1.,0.));
#75693=DIRECTION('ref_axis',(-1.,0.,1.83697019872103E-16));
#75694=DIRECTION('',(-0.335009667654805,0.,0.942214690279141));
#75695=DIRECTION('center_axis',(0.942214690279141,0.,0.335009667654805));
#75696=DIRECTION('ref_axis',(-0.335009667654805,0.,0.942214690279141));
#75697=DIRECTION('center_axis',(-0.869726513699833,0.,0.493533981978479));
#75698=DIRECTION('ref_axis',(-0.493533981978479,0.,-0.869726513699833));
#75699=DIRECTION('',(0.,-1.,0.));
#75700=DIRECTION('',(-0.493533981978479,0.,-0.869726513699833));
#75701=DIRECTION('center_axis',(0.,-1.,0.));
#75702=DIRECTION('ref_axis',(-0.984807753012208,0.,0.17364817766693));
#75703=DIRECTION('',(-0.166306254102511,0.,0.986074150277955));
#75704=DIRECTION('center_axis',(0.986074150277955,0.,0.166306254102511));
#75705=DIRECTION('ref_axis',(-0.166306254102511,0.,0.986074150277955));
#75706=DIRECTION('center_axis',(-0.770812137104607,0.,0.637062515999983));
#75707=DIRECTION('ref_axis',(-0.637062515999983,0.,-0.770812137104607));
#75708=DIRECTION('',(0.,-1.,0.));
#75709=DIRECTION('',(-0.637062515999983,0.,-0.770812137104607));
#75710=DIRECTION('center_axis',(0.,-1.,0.));
#75711=DIRECTION('ref_axis',(-0.939692620785908,0.,0.342020143325669));
#75712=DIRECTION('',(0.00745029082566329,0.,0.99997224619817));
#75713=DIRECTION('center_axis',(0.99997224619817,0.,-0.00745029082566323));
#75714=DIRECTION('ref_axis',(0.00745029082566323,0.,0.99997224619817));
#75715=DIRECTION('center_axis',(-0.64847702377322,0.,0.761234227842014));
#75716=DIRECTION('ref_axis',(-0.761234227842014,0.,-0.64847702377322));
#75717=DIRECTION('',(0.,-1.,0.));
#75718=DIRECTION('',(-0.761234227842014,0.,-0.64847702377322));
#75719=DIRECTION('center_axis',(0.,-1.,0.));
#75720=DIRECTION('ref_axis',(-0.866025403784438,0.,0.5));
#75721=DIRECTION('',(0.180980462437128,0.,0.983486691428025));
#75722=DIRECTION('center_axis',(0.983486691428025,0.,-0.180980462437128));
#75723=DIRECTION('ref_axis',(0.180980462437128,0.,0.983486691428025));
#75724=DIRECTION('center_axis',(-0.506438264219691,0.,0.862276222874171));
#75725=DIRECTION('ref_axis',(-0.862276222874171,0.,-0.506438264219691));
#75726=DIRECTION('',(0.,-1.,0.));
#75727=DIRECTION('',(-0.862276222874171,0.,-0.506438264219691));
#75728=DIRECTION('center_axis',(0.,-1.,0.));
#75729=DIRECTION('ref_axis',(-0.766044443118978,0.,0.642787609686539));
#75730=DIRECTION('',(0.349011634277973,0.,0.937118391207119));
#75731=DIRECTION('center_axis',(0.937118391207119,0.,-0.349011634277973));
#75732=DIRECTION('ref_axis',(0.349011634277973,0.,0.937118391207118));
#75733=DIRECTION('center_axis',(-0.349011634277973,0.,0.937118391207119));
#75734=DIRECTION('ref_axis',(-0.937118391207119,0.,-0.349011634277973));
#75735=DIRECTION('',(0.,-1.,0.));
#75736=DIRECTION('',(-0.937118391207119,0.,-0.349011634277973));
#75737=DIRECTION('center_axis',(0.,-1.,0.));
#75738=DIRECTION('ref_axis',(-0.642787609686539,0.,0.766044443118978));
#75739=DIRECTION('',(0.506438264219691,0.,0.862276222874171));
#75740=DIRECTION('center_axis',(0.862276222874171,0.,-0.506438264219691));
#75741=DIRECTION('ref_axis',(0.506438264219691,0.,0.862276222874171));
#75742=DIRECTION('center_axis',(-0.180980462437127,0.,0.983486691428025));
#75743=DIRECTION('ref_axis',(-0.983486691428025,0.,-0.180980462437127));
#75744=DIRECTION('',(0.,-1.,0.));
#75745=DIRECTION('',(-0.983486691428025,0.,-0.180980462437127));
#75746=DIRECTION('center_axis',(0.,-1.,0.));
#75747=DIRECTION('ref_axis',(-0.5,0.,0.866025403784439));
#75748=DIRECTION('',(0.648477023773221,0.,0.761234227842013));
#75749=DIRECTION('center_axis',(0.761234227842013,0.,-0.648477023773221));
#75750=DIRECTION('ref_axis',(0.648477023773221,0.,0.761234227842013));
#75751=DIRECTION('center_axis',(-0.00745029082566251,0.,0.99997224619817));
#75752=DIRECTION('ref_axis',(-0.99997224619817,0.,-0.00745029082566251));
#75753=DIRECTION('',(0.,-1.,0.));
#75754=DIRECTION('',(-0.99997224619817,0.,-0.00745029082566251));
#75755=DIRECTION('center_axis',(0.,-1.,0.));
#75756=DIRECTION('ref_axis',(-0.342020143325669,0.,0.939692620785909));
#75757=DIRECTION('',(0.770812137104608,0.,0.637062515999982));
#75758=DIRECTION('center_axis',(0.637062515999982,0.,-0.770812137104608));
#75759=DIRECTION('ref_axis',(0.770812137104608,0.,0.637062515999982));
#75760=DIRECTION('center_axis',(0.166306254102511,0.,0.986074150277955));
#75761=DIRECTION('ref_axis',(-0.986074150277955,0.,0.166306254102511));
#75762=DIRECTION('',(0.,-1.,0.));
#75763=DIRECTION('',(-0.986074150277955,0.,0.166306254102511));
#75764=DIRECTION('center_axis',(0.,-1.,0.));
#75765=DIRECTION('ref_axis',(-0.17364817766693,0.,0.984807753012208));
#75766=DIRECTION('',(0.869726513699833,0.,0.493533981978479));
#75767=DIRECTION('center_axis',(0.493533981978479,0.,-0.869726513699834));
#75768=DIRECTION('ref_axis',(0.869726513699834,0.,0.493533981978479));
#75769=DIRECTION('center_axis',(0.335009667654805,0.,0.942214690279141));
#75770=DIRECTION('ref_axis',(-0.942214690279141,0.,0.335009667654805));
#75771=DIRECTION('',(0.,-1.,0.));
#75772=DIRECTION('',(-0.942214690279141,0.,0.335009667654805));
#75773=DIRECTION('center_axis',(0.,-1.,0.));
#75774=DIRECTION('ref_axis',(1.22464679914735E-16,0.,1.));
#75775=DIRECTION('',(0.942214690279141,0.,0.335009667654805));
#75776=DIRECTION('center_axis',(0.335009667654805,0.,-0.942214690279141));
#75777=DIRECTION('ref_axis',(0.942214690279141,0.,0.335009667654805));
#75778=DIRECTION('center_axis',(0.493533981978479,0.,0.869726513699833));
#75779=DIRECTION('ref_axis',(-0.869726513699833,0.,0.493533981978479));
#75780=DIRECTION('',(0.,-1.,0.));
#75781=DIRECTION('',(-0.869726513699833,0.,0.493533981978479));
#75782=DIRECTION('center_axis',(0.,-1.,0.));
#75783=DIRECTION('ref_axis',(0.173648177666931,0.,0.984807753012208));
#75784=DIRECTION('',(0.986074150277955,0.,0.166306254102511));
#75785=DIRECTION('center_axis',(0.166306254102511,0.,-0.986074150277955));
#75786=DIRECTION('ref_axis',(0.986074150277955,0.,0.166306254102511));
#75787=DIRECTION('center_axis',(0.637062515999982,0.,0.770812137104607));
#75788=DIRECTION('ref_axis',(-0.770812137104608,0.,0.637062515999982));
#75789=DIRECTION('',(0.,-1.,0.));
#75790=DIRECTION('',(-0.770812137104608,0.,0.637062515999982));
#75791=DIRECTION('center_axis',(0.,-1.,0.));
#75792=DIRECTION('ref_axis',(0.342020143325669,0.,0.939692620785908));
#75793=DIRECTION('',(0.99997224619817,0.,-0.00745029082566279));
#75794=DIRECTION('center_axis',(-0.00745029082566278,0.,-0.99997224619817));
#75795=DIRECTION('ref_axis',(0.99997224619817,0.,-0.00745029082566278));
#75796=DIRECTION('center_axis',(0.761234227842013,0.,0.64847702377322));
#75797=DIRECTION('ref_axis',(-0.64847702377322,0.,0.761234227842013));
#75798=DIRECTION('',(0.,-1.,0.));
#75799=DIRECTION('',(-0.64847702377322,0.,0.761234227842013));
#75800=DIRECTION('center_axis',(0.,-1.,0.));
#75801=DIRECTION('ref_axis',(0.5,0.,0.866025403784439));
#75802=DIRECTION('',(0.983486691428025,0.,-0.180980462437127));
#75803=DIRECTION('center_axis',(-0.180980462437127,0.,-0.983486691428025));
#75804=DIRECTION('ref_axis',(0.983486691428025,0.,-0.180980462437127));
#75805=DIRECTION('center_axis',(0.862276222874171,0.,0.506438264219691));
#75806=DIRECTION('ref_axis',(-0.506438264219691,0.,0.862276222874171));
#75807=DIRECTION('',(0.,-1.,0.));
#75808=DIRECTION('',(-0.506438264219691,0.,0.862276222874171));
#75809=DIRECTION('center_axis',(0.,-1.,0.));
#75810=DIRECTION('ref_axis',(0.642787609686539,0.,0.766044443118978));
#75811=DIRECTION('',(0.937118391207119,0.,-0.349011634277973));
#75812=DIRECTION('center_axis',(-0.349011634277973,0.,-0.937118391207119));
#75813=DIRECTION('ref_axis',(0.937118391207118,0.,-0.349011634277973));
#75814=DIRECTION('center_axis',(0.937118391207119,0.,0.349011634277973));
#75815=DIRECTION('ref_axis',(-0.349011634277973,0.,0.937118391207119));
#75816=DIRECTION('',(0.,-1.,0.));
#75817=DIRECTION('',(-0.349011634277973,0.,0.937118391207119));
#75818=DIRECTION('center_axis',(0.,-1.,0.));
#75819=DIRECTION('ref_axis',(0.766044443118978,0.,0.642787609686539));
#75820=DIRECTION('',(0.862276222874171,0.,-0.506438264219691));
#75821=DIRECTION('center_axis',(-0.506438264219691,0.,-0.862276222874171));
#75822=DIRECTION('ref_axis',(0.862276222874171,0.,-0.506438264219691));
#75823=DIRECTION('center_axis',(0.983486691428025,0.,0.180980462437127));
#75824=DIRECTION('ref_axis',(-0.180980462437127,0.,0.983486691428025));
#75825=DIRECTION('',(0.,-1.,0.));
#75826=DIRECTION('',(-0.180980462437127,0.,0.983486691428025));
#75827=DIRECTION('center_axis',(0.,-1.,0.));
#75828=DIRECTION('ref_axis',(0.866025403784439,0.,0.5));
#75829=DIRECTION('',(0.761234227842013,0.,-0.64847702377322));
#75830=DIRECTION('center_axis',(-0.648477023773221,0.,-0.761234227842013));
#75831=DIRECTION('ref_axis',(0.761234227842013,0.,-0.648477023773221));
#75832=DIRECTION('center_axis',(0.99997224619817,0.,0.00745029082566256));
#75833=DIRECTION('ref_axis',(-0.00745029082566256,0.,0.99997224619817));
#75834=DIRECTION('',(0.,-1.,0.));
#75835=DIRECTION('',(-0.00745029082566256,0.,0.99997224619817));
#75836=DIRECTION('center_axis',(0.,-1.,0.));
#75837=DIRECTION('ref_axis',(0.939692620785908,0.,0.342020143325669));
#75838=DIRECTION('',(0.637062515999982,0.,-0.770812137104608));
#75839=DIRECTION('center_axis',(-0.770812137104608,0.,-0.637062515999982));
#75840=DIRECTION('ref_axis',(0.637062515999982,0.,-0.770812137104608));
#75841=DIRECTION('center_axis',(0.986074150277955,0.,-0.166306254102511));
#75842=DIRECTION('ref_axis',(0.166306254102511,0.,0.986074150277955));
#75843=DIRECTION('',(0.,-1.,0.));
#75844=DIRECTION('',(0.166306254102511,0.,0.986074150277955));
#75845=DIRECTION('center_axis',(0.,-1.,0.));
#75846=DIRECTION('ref_axis',(0.984807753012208,0.,0.17364817766693));
#75847=DIRECTION('',(0.493533981978479,0.,-0.869726513699833));
#75848=DIRECTION('center_axis',(-0.869726513699833,0.,-0.493533981978479));
#75849=DIRECTION('ref_axis',(0.493533981978479,0.,-0.869726513699833));
#75850=DIRECTION('center_axis',(0.942214690279141,0.,-0.335009667654805));
#75851=DIRECTION('ref_axis',(0.335009667654805,0.,0.942214690279141));
#75852=DIRECTION('',(0.,-1.,0.));
#75853=DIRECTION('',(0.335009667654805,0.,0.942214690279141));
#75854=DIRECTION('center_axis',(0.,-1.,0.));
#75855=DIRECTION('ref_axis',(1.,0.,-6.12323399573677E-17));
#75856=DIRECTION('',(0.335009667654805,0.,-0.942214690279141));
#75857=DIRECTION('center_axis',(-0.942214690279141,0.,-0.335009667654805));
#75858=DIRECTION('ref_axis',(0.335009667654805,0.,-0.942214690279141));
#75859=DIRECTION('center_axis',(0.869726513699833,0.,-0.493533981978479));
#75860=DIRECTION('ref_axis',(0.493533981978479,0.,0.869726513699833));
#75861=DIRECTION('',(0.,-1.,0.));
#75862=DIRECTION('',(0.493533981978479,0.,0.869726513699833));
#75863=DIRECTION('center_axis',(0.,-1.,0.));
#75864=DIRECTION('ref_axis',(0.984807753012208,0.,-0.17364817766693));
#75865=DIRECTION('',(0.166306254102511,0.,-0.986074150277955));
#75866=DIRECTION('center_axis',(-0.986074150277955,0.,-0.166306254102511));
#75867=DIRECTION('ref_axis',(0.166306254102511,0.,-0.986074150277955));
#75868=DIRECTION('center_axis',(0.770812137104608,0.,-0.637062515999982));
#75869=DIRECTION('ref_axis',(0.637062515999982,0.,0.770812137104608));
#75870=DIRECTION('',(0.,-1.,0.));
#75871=DIRECTION('',(0.637062515999982,0.,0.770812137104608));
#75872=DIRECTION('center_axis',(0.,-1.,0.));
#75873=DIRECTION('ref_axis',(0.939692620785908,0.,-0.342020143325669));
#75874=DIRECTION('',(-0.00745029082566273,0.,-0.99997224619817));
#75875=DIRECTION('center_axis',(-0.99997224619817,0.,0.00745029082566273));
#75876=DIRECTION('ref_axis',(-0.00745029082566273,0.,-0.99997224619817));
#75877=DIRECTION('center_axis',(0.64847702377322,0.,-0.761234227842013));
#75878=DIRECTION('ref_axis',(0.761234227842013,0.,0.64847702377322));
#75879=DIRECTION('',(0.,-1.,0.));
#75880=DIRECTION('',(0.761234227842013,0.,0.64847702377322));
#75881=DIRECTION('center_axis',(0.,-1.,0.));
#75882=DIRECTION('ref_axis',(0.866025403784439,0.,-0.5));
#75883=DIRECTION('',(-0.180980462437128,0.,-0.983486691428025));
#75884=DIRECTION('center_axis',(-0.983486691428025,0.,0.180980462437128));
#75885=DIRECTION('ref_axis',(-0.180980462437128,0.,-0.983486691428025));
#75886=DIRECTION('center_axis',(0.506438264219691,0.,-0.862276222874171));
#75887=DIRECTION('ref_axis',(0.862276222874171,0.,0.506438264219691));
#75888=DIRECTION('',(0.,-1.,0.));
#75889=DIRECTION('',(0.862276222874171,0.,0.506438264219691));
#75890=DIRECTION('center_axis',(0.,-1.,0.));
#75891=DIRECTION('ref_axis',(0.766044443118978,0.,-0.642787609686539));
#75892=DIRECTION('',(-0.349011634277973,0.,-0.937118391207119));
#75893=DIRECTION('center_axis',(-0.937118391207119,0.,0.349011634277973));
#75894=DIRECTION('ref_axis',(-0.349011634277973,0.,-0.937118391207119));
#75895=DIRECTION('center_axis',(0.349011634277973,0.,-0.937118391207119));
#75896=DIRECTION('ref_axis',(0.937118391207119,0.,0.349011634277973));
#75897=DIRECTION('',(0.,-1.,0.));
#75898=DIRECTION('',(0.937118391207119,0.,0.349011634277973));
#75899=DIRECTION('center_axis',(0.,-1.,0.));
#75900=DIRECTION('ref_axis',(0.642787609686539,0.,-0.766044443118978));
#75901=DIRECTION('',(-0.506438264219691,0.,-0.862276222874171));
#75902=DIRECTION('center_axis',(-0.862276222874171,0.,0.506438264219691));
#75903=DIRECTION('ref_axis',(-0.506438264219691,0.,-0.862276222874171));
#75904=DIRECTION('center_axis',(0.180980462437127,0.,-0.983486691428025));
#75905=DIRECTION('ref_axis',(0.983486691428025,0.,0.180980462437127));
#75906=DIRECTION('',(0.,-1.,0.));
#75907=DIRECTION('',(0.983486691428025,0.,0.180980462437127));
#75908=DIRECTION('center_axis',(0.,-1.,0.));
#75909=DIRECTION('ref_axis',(0.5,0.,-0.866025403784439));
#75910=DIRECTION('',(-0.64847702377322,0.,-0.761234227842013));
#75911=DIRECTION('center_axis',(-0.761234227842013,0.,0.64847702377322));
#75912=DIRECTION('ref_axis',(-0.64847702377322,0.,-0.761234227842013));
#75913=DIRECTION('center_axis',(0.00745029082566256,0.,-0.99997224619817));
#75914=DIRECTION('ref_axis',(0.99997224619817,0.,0.00745029082566256));
#75915=DIRECTION('',(0.,-1.,0.));
#75916=DIRECTION('',(0.99997224619817,0.,0.00745029082566256));
#75917=DIRECTION('center_axis',(0.,-1.,0.));
#75918=DIRECTION('ref_axis',(0.342020143325669,0.,-0.939692620785908));
#75919=DIRECTION('',(-0.770812137104608,0.,-0.637062515999982));
#75920=DIRECTION('center_axis',(-0.637062515999982,0.,0.770812137104608));
#75921=DIRECTION('ref_axis',(-0.770812137104608,0.,-0.637062515999982));
#75922=DIRECTION('center_axis',(-0.166306254102511,0.,-0.986074150277955));
#75923=DIRECTION('ref_axis',(0.986074150277955,0.,-0.166306254102511));
#75924=DIRECTION('',(0.,-1.,0.));
#75925=DIRECTION('',(0.986074150277955,0.,-0.166306254102511));
#75926=DIRECTION('center_axis',(0.,-1.,0.));
#75927=DIRECTION('ref_axis',(0.17364817766693,0.,-0.984807753012208));
#75928=DIRECTION('',(-0.869726513699833,0.,-0.493533981978479));
#75929=DIRECTION('center_axis',(-0.493533981978479,0.,0.869726513699833));
#75930=DIRECTION('ref_axis',(-0.869726513699833,0.,-0.493533981978479));
#75931=DIRECTION('center_axis',(-0.335009667654805,0.,-0.942214690279141));
#75932=DIRECTION('ref_axis',(0.942214690279141,0.,-0.335009667654805));
#75933=DIRECTION('',(0.,-1.,0.));
#75934=DIRECTION('',(0.942214690279141,0.,-0.335009667654805));
#75935=DIRECTION('center_axis',(0.,-1.,0.));
#75936=DIRECTION('ref_axis',(0.,0.,-1.));
#75937=DIRECTION('',(-0.942214690279141,0.,-0.335009667654805));
#75938=DIRECTION('center_axis',(-0.335009667654805,0.,0.942214690279141));
#75939=DIRECTION('ref_axis',(-0.942214690279141,0.,-0.335009667654805));
#75940=DIRECTION('center_axis',(0.,1.,0.));
#75941=DIRECTION('ref_axis',(0.,0.,1.));
#75942=DIRECTION('center_axis',(-1.,0.,0.));
#75943=DIRECTION('ref_axis',(0.,0.,-1.));
#75944=DIRECTION('center_axis',(0.,-1.,0.));
#75945=DIRECTION('ref_axis',(1.,0.,0.));
#75946=DIRECTION('center_axis',(0.,-1.,0.));
#75947=DIRECTION('ref_axis',(1.,0.,0.));
#75948=DIRECTION('',(-0.707106781186547,-0.707106781186547,8.65956056235493E-17));
#75949=DIRECTION('center_axis',(0.,1.,0.));
#75950=DIRECTION('ref_axis',(1.,0.,0.));
#75951=DIRECTION('center_axis',(0.,-1.,0.));
#75952=DIRECTION('ref_axis',(1.,0.,0.));
#75953=DIRECTION('center_axis',(0.,1.,0.));
#75954=DIRECTION('ref_axis',(1.,0.,0.));
#75955=DIRECTION('',(0.707106781186551,-0.707106781186544,8.65956056235498E-17));
#75956=DIRECTION('center_axis',(0.,-1.,0.));
#75957=DIRECTION('ref_axis',(1.,0.,0.));
#75958=DIRECTION('center_axis',(0.,-1.,0.));
#75959=DIRECTION('ref_axis',(1.,0.,0.));
#75960=DIRECTION('center_axis',(0.,-1.,0.));
#75961=DIRECTION('ref_axis',(1.,0.,0.));
#75962=DIRECTION('center_axis',(0.,-1.,0.));
#75963=DIRECTION('ref_axis',(1.,0.,0.));
#75964=DIRECTION('center_axis',(0.,-1.,0.));
#75965=DIRECTION('ref_axis',(1.,0.,0.));
#75966=DIRECTION('center_axis',(0.,-1.,0.));
#75967=DIRECTION('ref_axis',(1.,0.,0.));
#75968=DIRECTION('center_axis',(0.,-1.,0.));
#75969=DIRECTION('ref_axis',(1.,0.,0.));
#75970=DIRECTION('',(0.,1.,0.));
#75971=DIRECTION('',(0.,-1.,0.));
#75972=DIRECTION('center_axis',(0.,1.,0.));
#75973=DIRECTION('ref_axis',(1.,0.,0.));
#75974=DIRECTION('center_axis',(0.,-1.,0.));
#75975=DIRECTION('ref_axis',(1.,0.,0.));
#75976=DIRECTION('',(0.,1.,0.));
#75977=DIRECTION('',(0.,-1.,0.));
#75978=DIRECTION('center_axis',(0.,1.,0.));
#75979=DIRECTION('ref_axis',(1.,0.,0.));
#75980=DIRECTION('center_axis',(0.,-1.,0.));
#75981=DIRECTION('ref_axis',(1.,0.,0.));
#75982=DIRECTION('',(0.,-1.,0.));
#75983=DIRECTION('center_axis',(0.,1.,0.));
#75984=DIRECTION('ref_axis',(1.,0.,0.));
#75985=DIRECTION('',(0.,1.,0.));
#75986=DIRECTION('center_axis',(0.,-1.,0.));
#75987=DIRECTION('ref_axis',(1.,0.,0.));
#75988=DIRECTION('',(0.,1.,0.));
#75989=DIRECTION('',(0.,-1.,0.));
#75990=DIRECTION('center_axis',(0.,1.,0.));
#75991=DIRECTION('ref_axis',(1.,0.,0.));
#75992=DIRECTION('center_axis',(0.,-1.,0.));
#75993=DIRECTION('ref_axis',(1.,0.,0.));
#75994=DIRECTION('',(0.,-1.,0.));
#75995=DIRECTION('center_axis',(0.,1.,0.));
#75996=DIRECTION('ref_axis',(1.,0.,0.));
#75997=DIRECTION('',(0.,1.,0.));
#75998=DIRECTION('center_axis',(0.,-1.,0.));
#75999=DIRECTION('ref_axis',(1.,0.,0.));
#76000=DIRECTION('',(0.,-1.,0.));
#76001=DIRECTION('center_axis',(0.,1.,0.));
#76002=DIRECTION('ref_axis',(1.,0.,0.));
#76003=DIRECTION('',(0.,1.,0.));
#76004=DIRECTION('center_axis',(0.866025403784439,0.,0.5));
#76005=DIRECTION('ref_axis',(-0.5,0.,0.866025403784439));
#76006=DIRECTION('',(-0.5,0.,0.866025403784439));
#76007=DIRECTION('',(0.,-1.,0.));
#76008=DIRECTION('',(-0.5,0.,0.866025403784439));
#76009=DIRECTION('',(0.,-1.,0.));
#76010=DIRECTION('center_axis',(0.866025403784439,0.,-0.5));
#76011=DIRECTION('ref_axis',(0.5,0.,0.866025403784439));
#76012=DIRECTION('',(0.5,0.,0.866025403784439));
#76013=DIRECTION('',(0.,-1.,0.));
#76014=DIRECTION('',(0.5,0.,0.866025403784439));
#76015=DIRECTION('center_axis',(0.,0.,-1.));
#76016=DIRECTION('ref_axis',(1.,0.,0.));
#76017=DIRECTION('',(1.,0.,0.));
#76018=DIRECTION('',(0.,-1.,0.));
#76019=DIRECTION('',(1.,0.,0.));
#76020=DIRECTION('center_axis',(0.,1.,0.));
#76021=DIRECTION('ref_axis',(1.,0.,0.));
#76022=DIRECTION('center_axis',(0.,1.,0.));
#76023=DIRECTION('ref_axis',(1.,0.,0.));
#76024=DIRECTION('center_axis',(0.,1.,0.));
#76025=DIRECTION('ref_axis',(1.,0.,0.));
#76026=DIRECTION('',(0.499999999999999,0.,-0.866025403784439));
#76027=DIRECTION('center_axis',(0.,1.,0.));
#76028=DIRECTION('ref_axis',(1.,0.,0.));
#76029=DIRECTION('center_axis',(0.,1.,0.));
#76030=DIRECTION('ref_axis',(1.,0.,0.));
#76031=DIRECTION('',(-0.5,0.,-0.866025403784439));
#76032=DIRECTION('center_axis',(0.,1.,0.));
#76033=DIRECTION('ref_axis',(1.,0.,0.));
#76034=DIRECTION('',(-1.,0.,0.));
#76035=DIRECTION('center_axis',(0.,1.,0.));
#76036=DIRECTION('ref_axis',(0.,0.,1.));
#76037=DIRECTION('',(0.499999999999999,0.,-0.866025403784439));
#76038=DIRECTION('center_axis',(0.,-1.,0.));
#76039=DIRECTION('ref_axis',(1.,0.,0.));
#76040=DIRECTION('center_axis',(0.,1.,0.));
#76041=DIRECTION('ref_axis',(0.,0.,1.));
#76042=DIRECTION('center_axis',(0.,-1.,0.));
#76043=DIRECTION('ref_axis',(1.,0.,0.));
#76044=DIRECTION('center_axis',(0.,1.,0.));
#76045=DIRECTION('ref_axis',(0.,0.,1.));
#76046=DIRECTION('center_axis',(0.,-1.,0.));
#76047=DIRECTION('ref_axis',(1.,0.,0.));
#76048=DIRECTION('center_axis',(0.,1.,0.));
#76049=DIRECTION('ref_axis',(0.,0.,1.));
#76050=DIRECTION('center_axis',(0.,-1.,0.));
#76051=DIRECTION('ref_axis',(1.,0.,0.));
#76052=DIRECTION('center_axis',(0.,1.,0.));
#76053=DIRECTION('ref_axis',(0.,0.,1.));
#76054=DIRECTION('',(-1.,0.,0.));
#76055=DIRECTION('center_axis',(0.,-1.,0.));
#76056=DIRECTION('ref_axis',(1.,0.,0.));
#76057=DIRECTION('center_axis',(0.,1.,0.));
#76058=DIRECTION('ref_axis',(0.,0.,1.));
#76059=DIRECTION('',(-0.5,0.,-0.866025403784439));
#76060=DIRECTION('center_axis',(0.,-1.,0.));
#76061=DIRECTION('ref_axis',(1.,0.,0.));
#76062=DIRECTION('center_axis',(0.,1.,0.));
#76063=DIRECTION('ref_axis',(1.,0.,0.));
#76064=DIRECTION('',(0.857167300702113,-0.515038074910054,1.04972719113862E-16));
#76065=DIRECTION('center_axis',(-0.866025403784439,0.,-0.499999999999999));
#76066=DIRECTION('ref_axis',(0.499999999999999,0.,-0.866025403784439));
#76067=DIRECTION('',(0.,-1.,0.));
#76068=DIRECTION('center_axis',(-0.866025403784439,0.,0.5));
#76069=DIRECTION('ref_axis',(-0.5,0.,-0.866025403784439));
#76070=DIRECTION('',(0.,-1.,0.));
#76071=DIRECTION('center_axis',(0.,0.,1.));
#76072=DIRECTION('ref_axis',(-1.,0.,0.));
#110987=CARTESIAN_POINT('',(0.,0.,0.));
#110988=CARTESIAN_POINT('Origin',(6.,11.5,28.5));
#110989=CARTESIAN_POINT('',(4.78367053658047,11.2551073498501,28.5008333383868));
#110990=CARTESIAN_POINT('',(4.78395933369915,11.3198926501499,28.50124080222));
#110991=CARTESIAN_POINT('',(4.785,11.5,28.5));
#110992=CARTESIAN_POINT('',(6.5316301394983,11.4,29.5935755465205));
#110993=CARTESIAN_POINT('Ctrl Pts',(4.78367053658047,11.2551073498501,28.5008333383868));
#110994=CARTESIAN_POINT('Ctrl Pts',(4.78333000604768,11.2578458824113,28.5471435748903));
#110995=CARTESIAN_POINT('Ctrl Pts',(4.7857463752668,11.2605844149725,28.5934160710629));
#110996=CARTESIAN_POINT('Ctrl Pts',(4.79103847843843,11.2633229475337,28.6393548443288));
#110997=CARTESIAN_POINT('Ctrl Pts',(4.83692017656987,11.2870655920405,29.0376367483577));
#110998=CARTESIAN_POINT('Ctrl Pts',(5.09895975195116,11.3108082365472,29.4108339831172));
#110999=CARTESIAN_POINT('Ctrl Pts',(5.45800228421852,11.3345508810539,29.5895156282118));
#111000=CARTESIAN_POINT('Ctrl Pts',(5.78791523044235,11.3563672540359,29.7537005998278));
#111001=CARTESIAN_POINT('Ctrl Pts',(6.19972968361632,11.378183627018,29.7536522281492));
#111002=CARTESIAN_POINT('Ctrl Pts',(6.53227676969646,11.4,29.5943192153712));
#111003=CARTESIAN_POINT('',(5.46901649069986,11.4,29.5928318776698));
#111004=CARTESIAN_POINT('Origin',(6.,11.4,28.5));
#111005=CARTESIAN_POINT('Ctrl Pts',(5.46901649069988,11.4,29.5928318776698));
#111006=CARTESIAN_POINT('Ctrl Pts',(5.10673195249988,11.3762573554933,29.4168056110598));
#111007=CARTESIAN_POINT('Ctrl Pts',(4.84192918259107,11.3525147109866,29.0480006432466));
#111008=CARTESIAN_POINT('Ctrl Pts',(4.79253458702825,11.3287720664798,28.6507530872812));
#111009=CARTESIAN_POINT('Ctrl Pts',(4.78637695817715,11.3258122610365,28.6012314142364));
#111010=CARTESIAN_POINT('Ctrl Pts',(4.78356690442832,11.3228524555932,28.5512677259328));
#111011=CARTESIAN_POINT('Ctrl Pts',(4.78395933369915,11.3198926501499,28.50124080222));
#111012=CARTESIAN_POINT('Origin',(6.,11.5,28.5));
#111013=CARTESIAN_POINT('',(4.78681310871935,10.8051073498501,28.5004280789557));
#111014=CARTESIAN_POINT('',(4.78685314888988,10.8698926501499,28.5003771245331));
#111015=CARTESIAN_POINT('',(4.785,11.5,28.5));
#111016=CARTESIAN_POINT('Ctrl Pts',(4.78681310871935,10.8051073498501,28.5004280789557));
#111017=CARTESIAN_POINT('Ctrl Pts',(4.78625720576908,10.8153900153709,28.675482357614));
#111018=CARTESIAN_POINT('Ctrl Pts',(4.82167149629011,10.8256726808918,28.8503220275809));
#111019=CARTESIAN_POINT('Ctrl Pts',(4.89417743280821,10.8359553464126,29.0081177215779));
#111020=CARTESIAN_POINT('Ctrl Pts',(5.06159342741432,10.8596979909194,29.3724675158664));
#111021=CARTESIAN_POINT('Ctrl Pts',(5.42676232515714,10.8834406354261,29.6459479071283));
#111022=CARTESIAN_POINT('Ctrl Pts',(5.82349664722961,10.9071832799328,29.7041047455662));
#111023=CARTESIAN_POINT('Ctrl Pts',(6.22023096930208,10.9309259244395,29.762261584004));
#111024=CARTESIAN_POINT('Ctrl Pts',(6.64853071570421,10.9546685689463,29.6050948696179));
#111025=CARTESIAN_POINT('Ctrl Pts',(6.91347199143402,10.978411213453,29.3041169995649));
#111026=CARTESIAN_POINT('Ctrl Pts',(7.17841326716384,11.0021538579597,29.0031391295119));
#111027=CARTESIAN_POINT('Ctrl Pts',(7.27999607222133,11.0258965024664,28.558350103792));
#111028=CARTESIAN_POINT('Ctrl Pts',(7.17199676483148,11.0496391469732,28.1722029684367));
#111029=CARTESIAN_POINT('Ctrl Pts',(7.06399745744163,11.0733817914799,27.7860558330813));
#111030=CARTESIAN_POINT('Ctrl Pts',(6.74641603760442,11.0971244359866,27.4585505880904));
#111031=CARTESIAN_POINT('Ctrl Pts',(6.36377108114857,11.1208670804934,27.338680374029));
#111032=CARTESIAN_POINT('Ctrl Pts',(5.98112612469273,11.1446097250001,27.2188101599676));
#111033=CARTESIAN_POINT('Ctrl Pts',(5.53341763161827,11.1683523695068,27.3065749768356));
#111034=CARTESIAN_POINT('Ctrl Pts',(5.22442529552183,11.1920950140135,27.5621406719187));
#111035=CARTESIAN_POINT('Ctrl Pts',(4.95107286353664,11.213099125959,27.788228817552));
#111036=CARTESIAN_POINT('Ctrl Pts',(4.78628235194937,11.2341032379046,28.1456411432977));
#111037=CARTESIAN_POINT('Ctrl Pts',(4.78367053658047,11.2551073498501,28.5008333383868));
#111038=CARTESIAN_POINT('Ctrl Pts',(4.78395933369915,11.3198926501499,28.50124080222));
#111039=CARTESIAN_POINT('Ctrl Pts',(4.7867148507545,11.2991098110865,28.149967205262));
#111040=CARTESIAN_POINT('Ctrl Pts',(4.94736605064105,11.2783269720231,27.795575840609));
#111041=CARTESIAN_POINT('Ctrl Pts',(5.21568227798337,11.2575441329596,27.5691997084345));
#111042=CARTESIAN_POINT('Ctrl Pts',(5.52221098571815,11.2338014884529,27.3105840296708));
#111043=CARTESIAN_POINT('Ctrl Pts',(5.96925482240456,11.2100588439462,27.219042816261));
#111044=CARTESIAN_POINT('Ctrl Pts',(6.35303532139312,11.1863161994395,27.335452288796));
#111045=CARTESIAN_POINT('Ctrl Pts',(6.73681582038168,11.1625735549327,27.451861761331));
#111046=CARTESIAN_POINT('Ctrl Pts',(7.05733298167239,11.138830910426,27.7762219198108));
#111047=CARTESIAN_POINT('Ctrl Pts',(7.16888570291544,11.1150882659193,28.1613057291473));
#111048=CARTESIAN_POINT('Ctrl Pts',(7.2804384241585,11.0913456214126,28.5463895384839));
#111049=CARTESIAN_POINT('Ctrl Pts',(7.1830267053539,11.0676029769058,28.992196998677));
#111050=CARTESIAN_POINT('Ctrl Pts',(6.92089719776952,11.0438603323991,29.2956409119842));
#111051=CARTESIAN_POINT('Ctrl Pts',(6.65876769018514,11.0201176878924,29.5990848252914));
#111052=CARTESIAN_POINT('Ctrl Pts',(6.23192039382099,10.9963750433856,29.7601651917126));
#111053=CARTESIAN_POINT('Ctrl Pts',(5.83465859429877,10.9726323988789,29.7056760033484));
#111054=CARTESIAN_POINT('Ctrl Pts',(5.43739679477654,10.9488897543722,29.6511868149842));
#111055=CARTESIAN_POINT('Ctrl Pts',(5.06972049209625,10.9251471098655,29.3811280718347));
#111056=CARTESIAN_POINT('Ctrl Pts',(4.89893754845613,10.9014044653587,29.0183518086313));
#111057=CARTESIAN_POINT('Ctrl Pts',(4.8233817897133,10.8909005269558,28.8578566488922));
#111058=CARTESIAN_POINT('Ctrl Pts',(4.78636297044207,10.8803965885529,28.6792143587691));
#111059=CARTESIAN_POINT('Ctrl Pts',(4.78685314888988,10.8698926501499,28.5003771245331));
#111060=CARTESIAN_POINT('Origin',(6.,11.5,28.5));
#111061=CARTESIAN_POINT('',(4.78518722151686,10.3551073498501,28.4989078916254));
#111062=CARTESIAN_POINT('',(4.78507578420029,10.4198926501499,28.4989065979813));
#111063=CARTESIAN_POINT('',(4.785,11.5,28.5));
#111064=CARTESIAN_POINT('Ctrl Pts',(4.78518722151686,10.3551073498501,28.4989078916254));
#111065=CARTESIAN_POINT('Ctrl Pts',(4.78789665453853,10.3729341483306,28.8013698915326));
#111066=CARTESIAN_POINT('Ctrl Pts',(4.90234790879614,10.3907609468111,29.1056620640487));
#111067=CARTESIAN_POINT('Ctrl Pts',(5.10684325164102,10.4085877452916,29.3266182276633));
#111068=CARTESIAN_POINT('Ctrl Pts',(5.37920063727921,10.4323303897983,29.6208989786355));
#111069=CARTESIAN_POINT('Ctrl Pts',(5.81128073514232,10.456073034305,29.7673559959613));
#111070=CARTESIAN_POINT('Ctrl Pts',(6.20644280658897,10.4798156788117,29.6993364484615));
#111071=CARTESIAN_POINT('Ctrl Pts',(6.60160487803562,10.5035583233185,29.6313169009617));
#111072=CARTESIAN_POINT('Ctrl Pts',(6.95984892306582,10.5273009678252,29.3488207886363));
#111073=CARTESIAN_POINT('Ctrl Pts',(7.11813708317254,10.5510436123319,28.9804125574957));
#111074=CARTESIAN_POINT('Ctrl Pts',(7.27642524327927,10.5747862568386,28.6120043263552));
#111075=CARTESIAN_POINT('Ctrl Pts',(7.23475751846253,10.5985289013454,28.1576839763995));
#111076=CARTESIAN_POINT('Ctrl Pts',(7.01209712549708,10.6222715458521,27.8242143957805));
#111077=CARTESIAN_POINT('Ctrl Pts',(6.78943673253163,10.6460141903588,27.4907448151614));
#111078=CARTESIAN_POINT('Ctrl Pts',(6.38578367141748,10.6697568348655,27.2781260038789));
#111079=CARTESIAN_POINT('Ctrl Pts',(5.98484124835373,10.6934994793723,27.2831203215813));
#111080=CARTESIAN_POINT('Ctrl Pts',(5.58389882528997,10.717242123879,27.2881146392838));
#111081=CARTESIAN_POINT('Ctrl Pts',(5.18566704027662,10.7409847683857,27.5107220859713));
#111082=CARTESIAN_POINT('Ctrl Pts',(4.97138269350465,10.7647274128924,27.8496354079726));
#111083=CARTESIAN_POINT('Ctrl Pts',(4.84990242605869,10.7781873918783,28.0417692787753));
#111084=CARTESIAN_POINT('Ctrl Pts',(4.7875407840496,10.7916473708642,28.2712825419986));
#111085=CARTESIAN_POINT('Ctrl Pts',(4.78681310871935,10.8051073498501,28.5004280789557));
#111086=CARTESIAN_POINT('Ctrl Pts',(4.78685314888988,10.8698926501499,28.5003771245331));
#111087=CARTESIAN_POINT('Ctrl Pts',(4.78747094843896,10.8566539440461,28.2749784698909));
#111088=CARTESIAN_POINT('Ctrl Pts',(4.84767172642457,10.8434152379423,28.0492701468604));
#111089=CARTESIAN_POINT('Ctrl Pts',(4.96539746739741,10.8301765318386,27.8591937606951));
#111090=CARTESIAN_POINT('Ctrl Pts',(5.17652991457877,10.8064338873318,27.5183057592197));
#111091=CARTESIAN_POINT('Ctrl Pts',(5.57268439354146,10.7826912428251,27.292023539526));
#111092=CARTESIAN_POINT('Ctrl Pts',(5.97356402380349,10.7589485983184,27.2833149153006));
#111093=CARTESIAN_POINT('Ctrl Pts',(6.37444365406551,10.7352059538117,27.2746062910752));
#111094=CARTESIAN_POINT('Ctrl Pts',(6.78004843562688,10.7114633093049,27.483471262318));
#111095=CARTESIAN_POINT('Ctrl Pts',(7.0057896364173,10.6877206647982,27.8148619299256));
#111096=CARTESIAN_POINT('Ctrl Pts',(7.23153083720772,10.6639780202915,28.1462525975332));
#111097=CARTESIAN_POINT('Ctrl Pts',(7.27740845722719,10.6402353757847,28.6001689615056));
#111098=CARTESIAN_POINT('Ctrl Pts',(7.12254190425398,10.616492731278,28.9700288680826));
#111099=CARTESIAN_POINT('Ctrl Pts',(6.96767535128077,10.5927500867713,29.3398887746596));
#111100=CARTESIAN_POINT('Ctrl Pts',(6.61206462531487,10.5690074422646,29.6256922238413));
#111101=CARTESIAN_POINT('Ctrl Pts',(6.21754989447942,10.5452647977578,29.697371194261));
#111102=CARTESIAN_POINT('Ctrl Pts',(5.82303516364397,10.5215221532511,29.7690501646807));
#111103=CARTESIAN_POINT('Ctrl Pts',(5.38961642793897,10.4977795087444,29.6266046563385));
#111104=CARTESIAN_POINT('Ctrl Pts',(5.11454326365905,10.4740368642377,29.33486102967));
#111105=CARTESIAN_POINT('Ctrl Pts',(4.90544523763903,10.4559887928751,29.1130908813533));
#111106=CARTESIAN_POINT('Ctrl Pts',(4.78784473538313,10.4379407215125,28.8050511392199));
#111107=CARTESIAN_POINT('Ctrl Pts',(4.78507578420029,10.4198926501499,28.4989065979813));
#111108=CARTESIAN_POINT('Origin',(6.,11.5,28.5));
#111109=CARTESIAN_POINT('',(4.78326855736707,9.90510734985006,28.5004863587445));
#111110=CARTESIAN_POINT('',(4.78333364803414,9.96989265014994,28.5005459760334));
#111111=CARTESIAN_POINT('',(4.785,11.5,28.5));
#111112=CARTESIAN_POINT('Ctrl Pts',(4.78326855736707,9.90510734985006,28.5004863587445));
#111113=CARTESIAN_POINT('Ctrl Pts',(4.78312813994714,9.90673563678347,28.5280000759249));
#111114=CARTESIAN_POINT('Ctrl Pts',(4.78398106663306,9.90836392371688,28.5555049348603));
#111115=CARTESIAN_POINT('Ctrl Pts',(4.78585519896961,9.90999221065029,28.5829400337243));
#111116=CARTESIAN_POINT('Ctrl Pts',(4.81318260479242,9.93373485515702,28.9829811972126));
#111117=CARTESIAN_POINT('Ctrl Pts',(5.05763485169036,9.95747749966375,29.3681902410136));
#111118=CARTESIAN_POINT('Ctrl Pts',(5.40796108834759,9.98122014417047,29.5632575298335));
#111119=CARTESIAN_POINT('Ctrl Pts',(5.75828732500482,10.0049627886772,29.7583248186535));
#111120=CARTESIAN_POINT('Ctrl Pts',(6.21448755142135,10.0287054331839,29.7632503524923));
#111121=CARTESIAN_POINT('Ctrl Pts',(6.56894386303769,10.0524480776906,29.5757925106412));
#111122=CARTESIAN_POINT('Ctrl Pts',(6.92340017465404,10.0761907221974,29.38833466879));
#111123=CARTESIAN_POINT('Ctrl Pts',(7.17611257147019,10.0999333667041,29.0084934512488));
#111124=CARTESIAN_POINT('Ctrl Pts',(7.21207098565849,10.1236760112108,28.6091355755066));
#111125=CARTESIAN_POINT('Ctrl Pts',(7.2480293998468,10.1474186557176,28.2097776997644));
#111126=CARTESIAN_POINT('Ctrl Pts',(7.06723383140724,10.1711613002243,27.7909031658212));
#111127=CARTESIAN_POINT('Ctrl Pts',(6.75196481435131,10.194903944731,27.5431428689897));
#111128=CARTESIAN_POINT('Ctrl Pts',(6.43669579729538,10.2186465892377,27.2953825721582));
#111129=CARTESIAN_POINT('Ctrl Pts',(5.98695333162308,10.2423892337445,27.2187365124384));
#111130=CARTESIAN_POINT('Ctrl Pts',(5.6074163743245,10.2661318782512,27.348086491701));
#111131=CARTESIAN_POINT('Ctrl Pts',(5.22787941702593,10.2898745227579,27.4774364709637));
#111132=CARTESIAN_POINT('Ctrl Pts',(4.91854796810108,10.3136171672646,27.8127824892088));
#111133=CARTESIAN_POINT('Ctrl Pts',(4.82019958034531,10.3373598117714,28.2015077406407));
#111134=CARTESIAN_POINT('Ctrl Pts',(4.79569456285552,10.3432756577976,28.2983646317645));
#111135=CARTESIAN_POINT('Ctrl Pts',(4.78428809268046,10.3491915038238,28.3985354875622));
#111136=CARTESIAN_POINT('Ctrl Pts',(4.78518722151686,10.3551073498501,28.4989078916254));
#111137=CARTESIAN_POINT('Ctrl Pts',(4.78507578420029,10.4198926501499,28.4989065979813));
#111138=CARTESIAN_POINT('Ctrl Pts',(4.78420211771668,10.4141980770058,28.4023110976785));
#111139=CARTESIAN_POINT('Ctrl Pts',(4.79476044511274,10.4085035038616,28.3059042730909));
#111140=CARTESIAN_POINT('Ctrl Pts',(4.81748372732635,10.4028089307175,28.2124555283066));
#111141=CARTESIAN_POINT('Ctrl Pts',(4.91222494812837,10.3790662862107,27.8228353986066));
#111142=CARTESIAN_POINT('Ctrl Pts',(5.21843498258722,10.355323641704,27.4846368842013));
#111143=CARTESIAN_POINT('Ctrl Pts',(5.59675674158146,10.3315809971973,27.3517747524404));
#111144=CARTESIAN_POINT('Ctrl Pts',(5.9750785005757,10.3078383526906,27.2189126206795));
#111145=CARTESIAN_POINT('Ctrl Pts',(6.42551198410532,10.2840957081838,27.291386871563));
#111146=CARTESIAN_POINT('Ctrl Pts',(6.74306380257482,10.2603530636771,27.5362144155618));
#111147=CARTESIAN_POINT('Ctrl Pts',(7.06061562104432,10.2366104191704,27.7810419595606));
#111148=CARTESIAN_POINT('Ctrl Pts',(7.2452857744537,10.2128677746637,28.1982227966747));
#111149=CARTESIAN_POINT('Ctrl Pts',(7.21303036873607,10.1891251301569,28.5978967802481));
#111150=CARTESIAN_POINT('Ctrl Pts',(7.18077496301845,10.1653824856502,28.9975707638215));
#111151=CARTESIAN_POINT('Ctrl Pts',(6.93159399817384,10.1416398411435,29.3797378938541));
#111152=CARTESIAN_POINT('Ctrl Pts',(6.57889039174064,10.1178971966368,29.5704729534016));
#111153=CARTESIAN_POINT('Ctrl Pts',(6.22618678530745,10.09415455213,29.7612080129492));
#111154=CARTESIAN_POINT('Ctrl Pts',(5.76996053728566,10.0704119076233,29.7605110020117));
#111155=CARTESIAN_POINT('Ctrl Pts',(5.41784138777708,10.0466692631166,29.5686991145014));
#111156=CARTESIAN_POINT('Ctrl Pts',(5.0657222382685,10.0229266186098,29.3768872269911));
#111157=CARTESIAN_POINT('Ctrl Pts',(4.81771018727311,9.99918397410312,28.993960462908));
#111158=CARTESIAN_POINT('Ctrl Pts',(4.78667616574802,9.97544132959639,28.594189793868));
#111159=CARTESIAN_POINT('Ctrl Pts',(4.78425860526484,9.97359176978091,28.5630475272744));
#111160=CARTESIAN_POINT('Ctrl Pts',(4.78315776754325,9.97174220996543,28.5318030440965));
#111161=CARTESIAN_POINT('Ctrl Pts',(4.78333364803414,9.96989265014994,28.5005459760334));
#111162=CARTESIAN_POINT('Origin',(6.,11.5,28.5));
#111163=CARTESIAN_POINT('',(4.78654814450966,9.45510734985006,28.5006898848044));
#111164=CARTESIAN_POINT('',(4.78661099114014,9.51989265014995,28.5006411245624));
#111165=CARTESIAN_POINT('',(4.785,11.5,28.5));
#111166=CARTESIAN_POINT('Ctrl Pts',(4.78654814450966,9.45510734985006,28.5006898848044));
#111167=CARTESIAN_POINT('Ctrl Pts',(4.78573643973839,9.46427976974311,28.6567574803934));
#111168=CARTESIAN_POINT('Ctrl Pts',(4.81368718036296,9.47345218963616,28.8125454468369));
#111169=CARTESIAN_POINT('Ctrl Pts',(4.87175089853111,9.48262460952921,28.9561585382471));
#111170=CARTESIAN_POINT('Ctrl Pts',(5.02204779240205,9.50636725403594,29.327898451555));
#111171=CARTESIAN_POINT('Ctrl Pts',(5.37410884694187,9.53010989854266,29.6180637866337));
#111172=CARTESIAN_POINT('Ctrl Pts',(5.76771016394421,9.55385254304938,29.6945995475735));
#111173=CARTESIAN_POINT('Ctrl Pts',(6.16131148094654,9.57759518755611,29.7711353085133));
#111174=CARTESIAN_POINT('Ctrl Pts',(6.59645306041139,9.60133783206284,29.634041495314));
#111175=CARTESIAN_POINT('Ctrl Pts',(6.87510084197326,9.62508047656957,29.3457098576534));
#111176=CARTESIAN_POINT('Ctrl Pts',(7.15374862353513,9.6488231210763,29.0573782199929));
#111177=CARTESIAN_POINT('Ctrl Pts',(7.27590260719402,9.67256576558302,28.6178087578709));
#111178=CARTESIAN_POINT('Ctrl Pts',(7.18597019843295,9.69630841008975,28.2270506724461));
#111179=CARTESIAN_POINT('Ctrl Pts',(7.09603778967188,9.72005105459647,27.8362925870213));
#111180=CARTESIAN_POINT('Ctrl Pts',(6.79401898849085,9.7437936991032,27.4943458782936));
#111181=CARTESIAN_POINT('Ctrl Pts',(6.41736333395727,9.76753634360992,27.3568313796495));
#111182=CARTESIAN_POINT('Ctrl Pts',(6.04070767942368,9.79127898811665,27.2193168810055));
#111183=CARTESIAN_POINT('Ctrl Pts',(5.58941517153755,9.81502163262338,27.2862345924451));
#111184=CARTESIAN_POINT('Ctrl Pts',(5.26887019996833,9.83876427713011,27.5271300897527));
#111185=CARTESIAN_POINT('Ctrl Pts',(4.97030842359998,9.86087863470343,27.7515048077313));
#111186=CARTESIAN_POINT('Ctrl Pts',(4.7851756174621,9.88299299227674,28.1268125501468));
#111187=CARTESIAN_POINT('Ctrl Pts',(4.78326855736707,9.90510734985006,28.5004863587445));
#111188=CARTESIAN_POINT('Ctrl Pts',(4.78333364803414,9.96989265014994,28.5005459760334));
#111189=CARTESIAN_POINT('Ctrl Pts',(4.7854155306801,9.9479995654587,28.1305586782034));
#111190=CARTESIAN_POINT('Ctrl Pts',(4.96638170498052,9.92610648076746,27.7588080795541));
#111191=CARTESIAN_POINT('Ctrl Pts',(5.25988458774409,9.90421339607621,27.533948439426));
#111192=CARTESIAN_POINT('Ctrl Pts',(5.57818302332005,9.88047075156948,27.2900923280207));
#111193=CARTESIAN_POINT('Ctrl Pts',(6.02883588652676,9.85672810706275,27.2189946792071));
#111194=CARTESIAN_POINT('Ctrl Pts',(6.40674989258746,9.83298546255602,27.3530122195701));
#111195=CARTESIAN_POINT('Ctrl Pts',(6.78466389864815,9.8092428180493,27.4870297599331));
#111196=CARTESIAN_POINT('Ctrl Pts',(7.08983904756283,9.78550017354258,27.8261624894727));
#111197=CARTESIAN_POINT('Ctrl Pts',(7.18338933774817,9.76175752903585,28.2160702229757));
#111198=CARTESIAN_POINT('Ctrl Pts',(7.2769396279335,9.73801488452913,28.6059779564786));
#111199=CARTESIAN_POINT('Ctrl Pts',(7.15886505938949,9.7142722400224,29.046660693945));
#111200=CARTESIAN_POINT('Ctrl Pts',(6.88290167449175,9.69052959551567,29.3375625802597));
#111201=CARTESIAN_POINT('Ctrl Pts',(6.606938289594,9.66678695100894,29.6284644665744));
#111202=CARTESIAN_POINT('Ctrl Pts',(6.17308608834251,9.64304430650222,29.7695855017375));
#111203=CARTESIAN_POINT('Ctrl Pts',(5.77879233160934,9.61930166199549,29.6967011366441));
#111204=CARTESIAN_POINT('Ctrl Pts',(5.38449857487616,9.59555901748876,29.6238167715508));
#111205=CARTESIAN_POINT('Ctrl Pts',(5.0297632626613,9.57181637298203,29.3369270062008));
#111206=CARTESIAN_POINT('Ctrl Pts',(4.87602735483413,9.54807372847531,28.9665961163745));
#111207=CARTESIAN_POINT('Ctrl Pts',(4.81520229020312,9.53868003570019,28.820076018195));
#111208=CARTESIAN_POINT('Ctrl Pts',(4.78584088953869,9.52928634292507,28.6604943713531));
#111209=CARTESIAN_POINT('Ctrl Pts',(4.78661099114014,9.51989265014995,28.5006411245624));
#111210=CARTESIAN_POINT('Origin',(6.,11.5,28.5));
#111211=CARTESIAN_POINT('',(4.78572353544277,9.00510734985006,28.4989685021794));
#111212=CARTESIAN_POINT('',(4.78562084144037,9.06989265014994,28.4989494257994));
#111213=CARTESIAN_POINT('',(4.785,11.5,28.5));
#111214=CARTESIAN_POINT('Ctrl Pts',(4.78572353544277,9.00510734985006,28.4989685021794));
#111215=CARTESIAN_POINT('Ctrl Pts',(4.78803916596806,9.02182390270275,28.7829119346081));
#111216=CARTESIAN_POINT('Ctrl Pts',(4.88746037938484,9.03854045555544,29.0683165908713));
#111217=CARTESIAN_POINT('Ctrl Pts',(5.06938019515906,9.05525700840813,29.2842024138066));
#111218=CARTESIAN_POINT('Ctrl Pts',(5.32776226428058,9.07899965291485,29.5908266558477));
#111219=CARTESIAN_POINT('Ctrl Pts',(5.75256655663188,9.10274229742157,29.7572124154401));
#111220=CARTESIAN_POINT('Ctrl Pts',(6.15046353798807,9.12648494192829,29.707637102245));
#111221=CARTESIAN_POINT('Ctrl Pts',(6.54836051934427,9.15022758643502,29.65806178905));
#111222=CARTESIAN_POINT('Ctrl Pts',(6.91935018970536,9.17397023094176,29.3925254030675));
#111223=CARTESIAN_POINT('Ctrl Pts',(7.09459418876182,9.19771287544849,29.0318742416312));
#111224=CARTESIAN_POINT('Ctrl Pts',(7.26983818781829,9.22145551995522,28.671223080195));
#111225=CARTESIAN_POINT('Ctrl Pts',(7.24933651557014,9.24519816446194,28.2154571433049));
#111226=CARTESIAN_POINT('Ctrl Pts',(7.04241953618214,9.26894080896866,27.8719966898433));
#111227=CARTESIAN_POINT('Ctrl Pts',(6.83550255679414,9.29268345347539,27.5285362363817));
#111228=CARTESIAN_POINT('Ctrl Pts',(6.44217027026628,9.31642609798212,27.2973812663485));
#111229=CARTESIAN_POINT('Ctrl Pts',(6.04142921942195,9.34016874248885,27.2837310055902));
#111230=CARTESIAN_POINT('Ctrl Pts',(5.64068816857763,9.36391138699558,27.2700807448319));
#111231=CARTESIAN_POINT('Ctrl Pts',(5.23253835341683,9.38765403150229,27.4739351933486));
#111232=CARTESIAN_POINT('Ctrl Pts',(5.00272981243747,9.41139667600902,27.8025196633754));
#111233=CARTESIAN_POINT('Ctrl Pts',(4.86170246987407,9.4259669006227,28.0041631463286));
#111234=CARTESIAN_POINT('Ctrl Pts',(4.78783752299161,9.44053712523638,28.2527793062262));
#111235=CARTESIAN_POINT('Ctrl Pts',(4.78654814450966,9.45510734985006,28.5006898848044));
#111236=CARTESIAN_POINT('Ctrl Pts',(4.78661099114014,9.51989265014995,28.5006411245624));
#111237=CARTESIAN_POINT('Ctrl Pts',(4.78778732838813,9.50554369841834,28.2564638263208));
#111238=CARTESIAN_POINT('Ctrl Pts',(4.85926902453589,9.49119474668674,28.0116528082032));
#111239=CARTESIAN_POINT('Ctrl Pts',(4.99630810472276,9.47684579495513,27.8117928929291));
#111240=CARTESIAN_POINT('Ctrl Pts',(5.22306126587803,9.45310315044841,27.4810925736128));
#111241=CARTESIAN_POINT('Ctrl Pts',(5.62930409162803,9.42936050594167,27.2734639492829));
#111242=CARTESIAN_POINT('Ctrl Pts',(6.03015441931446,9.40561786143494,27.2833993449339));
#111243=CARTESIAN_POINT('Ctrl Pts',(6.43100474700089,9.38187521692822,27.2933347405849));
#111244=CARTESIAN_POINT('Ctrl Pts',(6.82646257662373,9.3581325724215,27.5208341562169));
#111245=CARTESIAN_POINT('Ctrl Pts',(7.03655402518042,9.33438992791477,27.8623620182446));
#111246=CARTESIAN_POINT('Ctrl Pts',(7.24664547373712,9.31064728340805,28.2038898802724));
#111247=CARTESIAN_POINT('Ctrl Pts',(7.27137054122764,9.28690463890131,28.6594461886959));
#111248=CARTESIAN_POINT('Ctrl Pts',(7.09947678537309,9.26316199439458,29.0217060871011));
#111249=CARTESIAN_POINT('Ctrl Pts',(6.92758302951854,9.23941934988786,29.3839659855063));
#111250=CARTESIAN_POINT('Ctrl Pts',(6.55907045031891,9.21567670538114,29.6529294738932));
#111251=CARTESIAN_POINT('Ctrl Pts',(6.16165007747503,9.19193406087441,29.7061905717384));
#111252=CARTESIAN_POINT('Ctrl Pts',(5.76422970463114,9.16819141636768,29.7594516695836));
#111253=CARTESIAN_POINT('Ctrl Pts',(5.337901538143,9.14444877186095,29.597010376887));
#111254=CARTESIAN_POINT('Ctrl Pts',(5.07668863130513,9.12070612735422,29.2927941468846));
#111255=CARTESIAN_POINT('Ctrl Pts',(4.89034128931309,9.10376830161946,29.075768554474));
#111256=CARTESIAN_POINT('Ctrl Pts',(4.78802588006844,9.0868304758847,28.7865895946388));
#111257=CARTESIAN_POINT('Ctrl Pts',(4.78562084144037,9.06989265014994,28.4989494257994));
#111258=CARTESIAN_POINT('Origin',(6.,11.5,28.5));
#111259=CARTESIAN_POINT('',(4.78305239341621,8.55510734985006,28.5001606667931));
#111260=CARTESIAN_POINT('',(4.78307934473882,8.61989265014994,28.5002282550221));
#111261=CARTESIAN_POINT('',(4.785,11.5,28.5));
#111262=CARTESIAN_POINT('Ctrl Pts',(4.78305239341621,8.55510734985006,28.5001606667931));
#111263=CARTESIAN_POINT('Ctrl Pts',(4.78303604688816,8.55562539115566,28.5089100350328));
#111264=CARTESIAN_POINT('Ctrl Pts',(4.78312229599692,8.55614343246126,28.5176590726092));
#111265=CARTESIAN_POINT('Ctrl Pts',(4.7833121281823,8.55666147376686,28.5264058621149));
#111266=CARTESIAN_POINT('Ctrl Pts',(4.79201243459565,8.58040411827359,28.9272849263215));
#111267=CARTESIAN_POINT('Ctrl Pts',(5.01829235789579,8.60414676278031,29.3234418448605));
#111268=CARTESIAN_POINT('Ctrl Pts',(5.35917131864016,8.62788940728704,29.5345845775619));
#111269=CARTESIAN_POINT('Ctrl Pts',(5.70005027938453,8.65163205179376,29.7457273102633));
#111270=CARTESIAN_POINT('Ctrl Pts',(6.15552827757312,8.6753746963005,29.771855857127));
#111271=CARTESIAN_POINT('Ctrl Pts',(6.51831609597122,8.69911734080722,29.6010790487697));
#111272=CARTESIAN_POINT('Ctrl Pts',(6.88110391436932,8.72285998531395,29.4303022404123));
#111273=CARTESIAN_POINT('Ctrl Pts',(7.15120155297692,8.74660262982067,29.0626200768339));
#111274=CARTESIAN_POINT('Ctrl Pts',(7.2056868765722,8.7703452743274,28.6653656634368));
#111275=CARTESIAN_POINT('Ctrl Pts',(7.26017220016747,8.79408791883412,28.2681112500397));
#111276=CARTESIAN_POINT('Ctrl Pts',(7.09904520875042,8.81783056334086,27.8412845868238));
#111277=CARTESIAN_POINT('Ctrl Pts',(6.79563521363584,8.84157320784758,27.579135594235));
#111278=CARTESIAN_POINT('Ctrl Pts',(6.49222521852127,8.86531585235431,27.3169866016461));
#111279=CARTESIAN_POINT('Ctrl Pts',(6.04653221970919,8.88905849686104,27.2195152796843));
#111280=CARTESIAN_POINT('Ctrl Pts',(5.66139225586264,8.91280114136776,27.3310810795472));
#111281=CARTESIAN_POINT('Ctrl Pts',(5.2762522920161,8.93654378587449,27.4426468794101));
#111282=CARTESIAN_POINT('Ctrl Pts',(4.9516653631351,8.96028643038121,27.7632498010979));
#111283=CARTESIAN_POINT('Ctrl Pts',(4.83535182164046,8.98402907488794,28.1469826241867));
#111284=CARTESIAN_POINT('Ctrl Pts',(4.80093149399264,8.99105516654198,28.2605395611539));
#111285=CARTESIAN_POINT('Ctrl Pts',(4.78475025868822,8.99808125819602,28.3796249629708));
#111286=CARTESIAN_POINT('Ctrl Pts',(4.78572353544277,9.00510734985006,28.4989685021794));
#111287=CARTESIAN_POINT('Ctrl Pts',(4.78562084144037,9.06989265014994,28.4989494257994));
#111288=CARTESIAN_POINT('Ctrl Pts',(4.78465461045772,9.06308783137798,28.3833891850022));
#111289=CARTESIAN_POINT('Ctrl Pts',(4.79981444337002,9.05628301260601,28.2680773132359));
#111290=CARTESIAN_POINT('Ctrl Pts',(4.8321299779901,9.04947819383405,28.1577923808764));
#111291=CARTESIAN_POINT('Ctrl Pts',(4.94488187870056,9.02573554932732,27.7729980121789));
#111292=CARTESIAN_POINT('Ctrl Pts',(5.26648332730909,9.00199290482059,27.4494004420923));
#111293=CARTESIAN_POINT('Ctrl Pts',(5.65057267120333,8.97825026031386,27.3342697632872));
#111294=CARTESIAN_POINT('Ctrl Pts',(6.03466201509756,8.95450761580713,27.2191390844821));
#111295=CARTESIAN_POINT('Ctrl Pts',(6.4812392542775,8.93076497130041,27.3124752969585));
#111296=CARTESIAN_POINT('Ctrl Pts',(6.78706592999723,8.90702232679368,27.5718008485602));
#111297=CARTESIAN_POINT('Ctrl Pts',(7.09289260571695,8.88327968228696,27.8311264001619));
#111298=CARTESIAN_POINT('Ctrl Pts',(7.25796871797646,8.85953703778023,28.2564412908888));
#111299=CARTESIAN_POINT('Ctrl Pts',(7.20716770033245,8.83579439327351,28.6541836118725));
#111300=CARTESIAN_POINT('Ctrl Pts',(7.15636668268844,8.81205174876678,29.0519259328563));
#111301=CARTESIAN_POINT('Ctrl Pts',(6.8896885351409,8.78830910426005,29.4220956840969));
#111302=CARTESIAN_POINT('Ctrl Pts',(6.52849917366942,8.76456645975332,29.5962276526009));
#111303=CARTESIAN_POINT('Ctrl Pts',(6.16730981219795,8.74082381524659,29.7703596211048));
#111304=CARTESIAN_POINT('Ctrl Pts',(5.71160923680254,8.71708117073987,29.7484538068722));
#111305=CARTESIAN_POINT('Ctrl Pts',(5.36878796018151,8.69333852623314,29.5404796027238));
#111306=CARTESIAN_POINT('Ctrl Pts',(5.02596668356048,8.66959588172642,29.3325053985753));
#111307=CARTESIAN_POINT('Ctrl Pts',(4.79602470571383,8.64585323721969,28.9384628045112));
#111308=CARTESIAN_POINT('Ctrl Pts',(4.78360921659756,8.62211059271296,28.5376816261541));
#111309=CARTESIAN_POINT('Ctrl Pts',(4.78322261487558,8.62137127852529,28.5252018364143));
#111310=CARTESIAN_POINT('Ctrl Pts',(4.78304693037956,8.62063196433762,28.5127155128334));
#111311=CARTESIAN_POINT('Ctrl Pts',(4.78307934473882,8.61989265014994,28.5002282550221));
#111312=CARTESIAN_POINT('Origin',(6.,11.5,28.5));
#111313=CARTESIAN_POINT('',(4.78616577632925,8.10510734985006,28.5008994915339));
#111314=CARTESIAN_POINT('',(4.78625043272942,8.16989265014995,28.5008628615494));
#111315=CARTESIAN_POINT('',(4.785,11.5,28.5));
#111316=CARTESIAN_POINT('Ctrl Pts',(4.78616577632925,8.10510734985006,28.5008994915339));
#111317=CARTESIAN_POINT('Ctrl Pts',(4.78521661554573,8.1131695241153,28.6379677840418));
#111318=CARTESIAN_POINT('Ctrl Pts',(4.80665227509289,8.12123169838054,28.7747480235267));
#111319=CARTESIAN_POINT('Ctrl Pts',(4.85176436536515,8.12929387264578,28.903214055232));
#111320=CARTESIAN_POINT('Ctrl Pts',(4.98461690452544,8.15303651715251,29.2815392094179));
#111321=CARTESIAN_POINT('Ctrl Pts',(5.32280778498557,8.17677916165923,29.587757817879));
#111322=CARTESIAN_POINT('Ctrl Pts',(5.71242546071077,8.20052180616595,29.6825089984159));
#111323=CARTESIAN_POINT('Ctrl Pts',(6.10204313643597,8.22426445067268,29.7772601789527));
#111324=CARTESIAN_POINT('Ctrl Pts',(6.54308760742622,8.24800709517941,29.6605439315654));
#111325=CARTESIAN_POINT('Ctrl Pts',(6.8348383920752,8.27174973968614,29.3854781228805));
#111326=CARTESIAN_POINT('Ctrl Pts',(7.12658917672417,8.29549238419287,29.1104123141956));
#111327=CARTESIAN_POINT('Ctrl Pts',(7.26904627503186,8.31923502869959,28.6769969442132));
#111328=CARTESIAN_POINT('Ctrl Pts',(7.19737709241624,8.34297767320632,28.2824804709019));
#111329=CARTESIAN_POINT('Ctrl Pts',(7.12570790980061,8.36672031771304,27.8879639975905));
#111330=CARTESIAN_POINT('Ctrl Pts',(6.83991244626166,8.39046296221977,27.5323464209502));
#111331=CARTESIAN_POINT('Ctrl Pts',(6.47005695782437,8.4142056067265,27.3774702216052));
#111332=CARTESIAN_POINT('Ctrl Pts',(6.10020146938709,8.43794825123323,27.2225940222601));
#111333=CARTESIAN_POINT('Ctrl Pts',(5.64628595605148,8.46169089573995,27.2684592002103));
#111334=CARTESIAN_POINT('Ctrl Pts',(5.31488854414695,8.48543354024668,27.4941923941224));
#111335=CARTESIAN_POINT('Ctrl Pts',(4.99072189998132,8.5086581434478,27.7150003102939));
#111336=CARTESIAN_POINT('Ctrl Pts',(4.78378523387422,8.53188274664894,28.1079127834113));
#111337=CARTESIAN_POINT('Ctrl Pts',(4.78305239341621,8.55510734985006,28.5001606667931));
#111338=CARTESIAN_POINT('Ctrl Pts',(4.78307934473882,8.61989265014994,28.5002282550221));
#111339=CARTESIAN_POINT('Ctrl Pts',(4.78408789864679,8.59688931983089,28.111694501712));
#111340=CARTESIAN_POINT('Ctrl Pts',(4.98655840647933,8.57388598951183,27.7222563134603));
#111341=CARTESIAN_POINT('Ctrl Pts',(5.3055956680209,8.55088265919278,27.5005856381737));
#111342=CARTESIAN_POINT('Ctrl Pts',(5.63488660894638,8.52714001468605,27.2717905912001));
#111343=CARTESIAN_POINT('Ctrl Pts',(6.08835749118323,8.50339737017933,27.2217202599028));
#111344=CARTESIAN_POINT('Ctrl Pts',(6.4596325411673,8.4796547256726,27.3731617818));
#111345=CARTESIAN_POINT('Ctrl Pts',(6.83090759115138,8.45591208116588,27.5246033036973));
#111346=CARTESIAN_POINT('Ctrl Pts',(7.11998680888268,8.43216943665915,27.8775566787891));
#111347=CARTESIAN_POINT('Ctrl Pts',(7.19530949329411,8.40842679215242,28.2713919114795));
#111348=CARTESIAN_POINT('Ctrl Pts',(7.27063217770554,8.38468414764569,28.6652271441699));
#111349=CARTESIAN_POINT('Ctrl Pts',(7.1321983287971,8.36094150313897,29.0999442344589));
#111350=CARTESIAN_POINT('Ctrl Pts',(6.84300954992419,8.33719885863224,29.3777023080935));
#111351=CARTESIAN_POINT('Ctrl Pts',(6.55382077105129,8.31345621412551,29.6554603817282));
#111352=CARTESIAN_POINT('Ctrl Pts',(6.11387706221393,8.28971356961879,29.7762594387086));
#111353=CARTESIAN_POINT('Ctrl Pts',(5.72339794530988,8.26597092511206,29.6851235151819));
#111354=CARTESIAN_POINT('Ctrl Pts',(5.33291882840583,8.24222828060534,29.5939875916553));
#111355=CARTESIAN_POINT('Ctrl Pts',(4.99190430343508,8.21848563609861,29.2909166876217));
#111356=CARTESIAN_POINT('Ctrl Pts',(4.85555096436684,8.19474299159188,28.9138391568403));
#111357=CARTESIAN_POINT('Ctrl Pts',(4.80797936057134,8.18645954444457,28.7822825479806));
#111358=CARTESIAN_POINT('Ctrl Pts',(4.78531923606525,8.17817609729726,28.641717809214));
#111359=CARTESIAN_POINT('Ctrl Pts',(4.78625043272942,8.16989265014995,28.5008628615494));
#111360=CARTESIAN_POINT('Origin',(6.,11.5,28.5));
#111361=CARTESIAN_POINT('',(4.78619455170653,7.65510734985006,28.4991124767033));
#111362=CARTESIAN_POINT('',(4.78610753914613,7.71989265014994,28.499077712745));
#111363=CARTESIAN_POINT('',(4.785,11.5,28.5));
#111364=CARTESIAN_POINT('Ctrl Pts',(4.78619455170653,7.65510734985006,28.4991124767033));
#111365=CARTESIAN_POINT('Ctrl Pts',(4.78800457873014,7.67071365707494,28.7644574786248));
#111366=CARTESIAN_POINT('Ctrl Pts',(4.87364547425961,7.68631996429982,29.0308656186776));
#111367=CARTESIAN_POINT('Ctrl Pts',(5.03392952076701,7.7019262715247,29.2400908566776));
#111368=CARTESIAN_POINT('Ctrl Pts',(5.27777754205026,7.72566891603142,29.5583955251741));
#111369=CARTESIAN_POINT('Ctrl Pts',(5.69438741094785,7.74941156053815,29.7443501564449));
#111370=CARTESIAN_POINT('Ctrl Pts',(6.09415889663745,7.77315420504487,29.7133263160167));
#111371=CARTESIAN_POINT('Ctrl Pts',(6.49393038232705,7.7968968495516,29.6823024755884));
#111372=CARTESIAN_POINT('Ctrl Pts',(6.87686348480867,7.82063949405833,29.4343001634611));
#111373=CARTESIAN_POINT('Ctrl Pts',(7.06868435683791,7.84438213856505,29.082185874483));
#111374=CARTESIAN_POINT('Ctrl Pts',(7.26050522886715,7.86812478307178,28.730071585505));
#111375=CARTESIAN_POINT('Ctrl Pts',(7.26121387044402,7.8918674275785,28.273845319676));
#111376=CARTESIAN_POINT('Ctrl Pts',(7.07048777696507,7.91561007208523,27.9211368327925));
#111377=CARTESIAN_POINT('Ctrl Pts',(6.87976168348613,7.93935271659196,27.568428345909));
#111378=CARTESIAN_POINT('Ctrl Pts',(6.49760085495136,7.96309536109869,27.3192376379709));
#111379=CARTESIAN_POINT('Ctrl Pts',(6.09792767469521,7.98683800560542,27.2869720458671));
#111380=CARTESIAN_POINT('Ctrl Pts',(5.69825449443906,8.01058065011215,27.2547064537634));
#111381=CARTESIAN_POINT('Ctrl Pts',(5.28106896246153,8.03432329461887,27.4393659774941));
#111382=CARTESIAN_POINT('Ctrl Pts',(5.03623329540298,8.0580659391256,27.7569115893148));
#111383=CARTESIAN_POINT('Ctrl Pts',(4.87453528445568,8.07374640936708,27.9666297828824));
#111384=CARTESIAN_POINT('Ctrl Pts',(4.78801184004987,8.08942687960857,28.2343094612255));
#111385=CARTESIAN_POINT('Ctrl Pts',(4.78616577632925,8.10510734985006,28.5008994915339));
#111386=CARTESIAN_POINT('Ctrl Pts',(4.78625043272942,8.16989265014995,28.5008628615494));
#111387=CARTESIAN_POINT('Ctrl Pts',(4.78798830257463,8.15443345279053,28.2379886744783));
#111388=CARTESIAN_POINT('Ctrl Pts',(4.87189440305332,8.13897425543111,27.9741036940105));
#111389=CARTESIAN_POINT('Ctrl Pts',(5.02938742677268,8.1235150580717,27.7658762532179));
#111390=CARTESIAN_POINT('Ctrl Pts',(5.27126938141252,8.09977241356497,27.4460750379062));
#111391=CARTESIAN_POINT('Ctrl Pts',(5.68672544385794,8.07602976905825,27.2575567648121));
#111392=CARTESIAN_POINT('Ctrl Pts',(6.08668048353732,8.05228712455152,27.2861165885187));
#111393=CARTESIAN_POINT('Ctrl Pts',(6.48663552321671,8.02854448004479,27.3146764122254));
#111394=CARTESIAN_POINT('Ctrl Pts',(6.87108954013006,8.00480183553806,27.5603143327329));
#111395=CARTESIAN_POINT('Ctrl Pts',(7.0650765149634,7.98105919103133,27.9112398959091));
#111396=CARTESIAN_POINT('Ctrl Pts',(7.25906348979675,7.95731654652461,28.2621654590854));
#111397=CARTESIAN_POINT('Ctrl Pts',(7.26258342255009,7.93357390201789,28.7183786649305));
#111398=CARTESIAN_POINT('Ctrl Pts',(7.07403438270397,7.90983125751116,29.0722557012979));
#111399=CARTESIAN_POINT('Ctrl Pts',(6.88548534285785,7.88608861300444,29.4261327376653));
#111400=CARTESIAN_POINT('Ctrl Pts',(6.50486733041225,7.86234596849771,29.6776736045549));
#111401=CARTESIAN_POINT('Ctrl Pts',(6.10540058911368,7.83860332399098,29.7124014016435));
#111402=CARTESIAN_POINT('Ctrl Pts',(5.70593384781511,7.81486067948425,29.7471291987322));
#111403=CARTESIAN_POINT('Ctrl Pts',(5.28761837766355,7.79111803497753,29.5650439260198));
#111404=CARTESIAN_POINT('Ctrl Pts',(5.04083063307749,7.7673753904708,29.2490130629383));
#111405=CARTESIAN_POINT('Ctrl Pts',(4.87631430063006,7.75154781036385,29.0383371291655));
#111406=CARTESIAN_POINT('Ctrl Pts',(4.78802432957745,7.73572023025689,28.7681362122154));
#111407=CARTESIAN_POINT('Ctrl Pts',(4.78610753914613,7.71989265014994,28.499077712745));
#111408=CARTESIAN_POINT('Origin',(6.,11.5,28.5));
#111409=CARTESIAN_POINT('',(4.78306041506863,7.20510734985006,28.4998165775134));
#111410=CARTESIAN_POINT('',(4.78303957841512,7.26989265014994,28.4998847090757));
#111411=CARTESIAN_POINT('',(4.785,11.5,28.5));
#111412=CARTESIAN_POINT('Ctrl Pts',(4.78306041506863,7.20510734985006,28.4998165775134));
#111413=CARTESIAN_POINT('Ctrl Pts',(4.78388808820232,7.22825779003458,28.8908188285037));
#111414=CARTESIAN_POINT('Ctrl Pts',(4.98932111084564,7.25140823021909,29.2825688683523));
#111415=CARTESIAN_POINT('Ctrl Pts',(5.31176728118342,7.27455867040361,29.5036744356945));
#111416=CARTESIAN_POINT('Ctrl Pts',(5.64246184827877,7.29830131491034,29.7304360368572));
#111417=CARTESIAN_POINT('Ctrl Pts',(6.09623268819263,7.32204395941706,29.7777110925591));
#111418=CARTESIAN_POINT('Ctrl Pts',(6.46656751884371,7.34578660392379,29.6239846064782));
#111419=CARTESIAN_POINT('Ctrl Pts',(6.83690234949481,7.36952924843052,29.4702581203973));
#111420=CARTESIAN_POINT('Ctrl Pts',(7.12380117088312,7.39327189293724,29.1155300925335));
#111421=CARTESIAN_POINT('Ctrl Pts',(7.1966955844278,7.41701453744397,28.7212381654897));
#111422=CARTESIAN_POINT('Ctrl Pts',(7.26958999797249,7.4407571819507,28.3269462384458));
#111423=CARTESIAN_POINT('Ctrl Pts',(7.12848000367358,7.46449982645743,27.8930904122219));
#111424=CARTESIAN_POINT('Ctrl Pts',(6.83758512637848,7.48824247096415,27.6171195986246));
#111425=CARTESIAN_POINT('Ctrl Pts',(6.54669024908336,7.51198511547088,27.3411487850273));
#111426=CARTESIAN_POINT('Ctrl Pts',(6.10601048879204,7.5357277599776,27.2230629840567));
#111427=CARTESIAN_POINT('Ctrl Pts',(5.71610034592059,7.55947040448433,27.3166033491798));
#111428=CARTESIAN_POINT('Ctrl Pts',(5.32619020304914,7.58321304899106,27.4101437143029));
#111429=CARTESIAN_POINT('Ctrl Pts',(4.98704967759756,7.60695569349778,27.7153102455197));
#111430=CARTESIAN_POINT('Ctrl Pts',(4.85302250170622,7.63069833800451,28.0932208639892));
#111431=CARTESIAN_POINT('Ctrl Pts',(4.80709289568964,7.63883467528636,28.2227265832611));
#111432=CARTESIAN_POINT('Ctrl Pts',(4.78525089539238,7.64697101256821,28.3607750468054));
#111433=CARTESIAN_POINT('Ctrl Pts',(4.78619455170653,7.65510734985006,28.4991124767033));
#111434=CARTESIAN_POINT('Ctrl Pts',(4.78610753914613,7.71989265014994,28.499077712745));
#111435=CARTESIAN_POINT('Ctrl Pts',(4.78514898960146,7.71197758575017,28.364526799957));
#111436=CARTESIAN_POINT('Ctrl Pts',(4.80579069004693,7.70406252135039,28.2302615835272));
#111437=CARTESIAN_POINT('Ctrl Pts',(4.84930160570745,7.69614745695062,28.103869152572));
#111438=CARTESIAN_POINT('Ctrl Pts',(4.97982034194404,7.67240481244389,27.7247325587378));
#111439=CARTESIAN_POINT('Ctrl Pts',(5.31611783343779,7.64866216793716,27.4164358245197));
#111440=CARTESIAN_POINT('Ctrl Pts',(5.70514422034347,7.62491952343044,27.3192855925029));
#111441=CARTESIAN_POINT('Ctrl Pts',(6.09417060724916,7.60117687892371,27.2221353604861));
#111442=CARTESIAN_POINT('Ctrl Pts',(6.5359258895668,7.57743423441699,27.3361316306704));
#111443=CARTESIAN_POINT('Ctrl Pts',(6.82936609368032,7.55369158991026,27.6093944051656));
#111444=CARTESIAN_POINT('Ctrl Pts',(7.12280629779385,7.52994894540353,27.8826571796608));
#111445=CARTESIAN_POINT('Ctrl Pts',(7.26793142370327,7.5062063008968,28.3151864584669));
#111446=CARTESIAN_POINT('Ctrl Pts',(7.19869465042118,7.48246365639008,28.7101370458817));
#111447=CARTESIAN_POINT('Ctrl Pts',(7.12945787713909,7.45872101188335,29.1050876332965));
#111448=CARTESIAN_POINT('Ctrl Pts',(6.84585920466548,7.43497836737663,29.4624595293201));
#111449=CARTESIAN_POINT('Ctrl Pts',(6.47696512397243,7.4112357228699,29.619611858273));
#111450=CARTESIAN_POINT('Ctrl Pts',(6.10807104327939,7.38749307836317,29.7767641872259));
#111451=CARTESIAN_POINT('Ctrl Pts',(5.65388155436692,7.36375043385644,29.7336969491082));
#111452=CARTESIAN_POINT('Ctrl Pts',(5.3210994700661,7.34000778934971,29.5100101551136));
#111453=CARTESIAN_POINT('Ctrl Pts',(4.99351644174012,7.31663607628312,29.2898180208909));
#111454=CARTESIAN_POINT('Ctrl Pts',(4.78357695409633,7.29326436321653,28.8946058857237));
#111455=CARTESIAN_POINT('Ctrl Pts',(4.78303957841512,7.26989265014994,28.4998847090757));
#111456=CARTESIAN_POINT('Origin',(6.,11.5,28.5));
#111457=CARTESIAN_POINT('',(4.78568939793849,6.75510734985006,28.5010383098413));
#111458=CARTESIAN_POINT('',(4.7857905243208,6.81989265014994,28.5010169731875));
#111459=CARTESIAN_POINT('',(4.785,11.5,28.5));
#111460=CARTESIAN_POINT('Ctrl Pts',(4.78568939793849,6.75510734985006,28.5010383098413));
#111461=CARTESIAN_POINT('Ctrl Pts',(4.7847179759516,6.76205927848748,28.6191136444317));
#111462=CARTESIAN_POINT('Ctrl Pts',(4.80055291679293,6.76901120712491,28.7369340126475));
#111463=CARTESIAN_POINT('Ctrl Pts',(4.83426069151918,6.77596313576234,28.8493975371586));
#111464=CARTESIAN_POINT('Ctrl Pts',(4.94938150966584,6.79970578026907,29.2334897253414));
#111465=CARTESIAN_POINT('Ctrl Pts',(5.27297109019361,6.8234484247758,29.5550996801765));
#111466=CARTESIAN_POINT('Ctrl Pts',(5.65776265710716,6.84719106928253,29.6678614486722));
#111467=CARTESIAN_POINT('Ctrl Pts',(6.04255422402072,6.87093371378926,29.780623217168));
#111468=CARTESIAN_POINT('Ctrl Pts',(6.48854777732007,6.89467635829598,29.6845367993243));
#111469=CARTESIAN_POINT('Ctrl Pts',(6.79277065916322,6.91841900280271,29.4233315931834));
#111470=CARTESIAN_POINT('Ctrl Pts',(7.09699354100638,6.94216164730943,29.1621263870424));
#111471=CARTESIAN_POINT('Ctrl Pts',(7.25944575139334,6.96590429181616,28.7358023926042));
#111472=CARTESIAN_POINT('Ctrl Pts',(7.20619478426713,6.98964693632289,28.3383806513713));
#111473=CARTESIAN_POINT('Ctrl Pts',(7.15294381714092,7.01338958082961,27.9409589101385));
#111474=CARTESIAN_POINT('Ctrl Pts',(6.88398967250154,7.03713222533635,27.572439422111));
#111475=CARTESIAN_POINT('Ctrl Pts',(6.52173412170005,7.06087486984307,27.4005364192623));
#111476=CARTESIAN_POINT('Ctrl Pts',(6.15947857089856,7.0846175143498,27.2286334164135));
#111477=CARTESIAN_POINT('Ctrl Pts',(5.70392161393496,7.10836015885652,27.2533468987435));
#111478=CARTESIAN_POINT('Ctrl Pts',(5.36238838021367,7.13210280336325,27.4634296666103));
#111479=CARTESIAN_POINT('Ctrl Pts',(5.02085514649238,7.15584544786997,27.6735124344772));
#111480=CARTESIAN_POINT('Ctrl Pts',(4.79334563601341,7.1795880923767,28.0689644878809));
#111481=CARTESIAN_POINT('Ctrl Pts',(4.78340002791233,7.20333073688343,28.4698145878945));
#111482=CARTESIAN_POINT('Ctrl Pts',(4.78315195815318,7.20392294120564,28.4798128491126));
#111483=CARTESIAN_POINT('Ctrl Pts',(4.78303924261562,7.20451514552785,28.489814468647));
#111484=CARTESIAN_POINT('Ctrl Pts',(4.78306041506863,7.20510734985006,28.4998165775134));
#111485=CARTESIAN_POINT('Ctrl Pts',(4.78303957841512,7.26989265014994,28.4998847090757));
#111486=CARTESIAN_POINT('Ctrl Pts',(4.78303104974909,7.26952171870981,28.493620106473));
#111487=CARTESIAN_POINT('Ctrl Pts',(4.78307526680697,7.26915078726967,28.4873556275365));
#111488=CARTESIAN_POINT('Ctrl Pts',(4.78317259641123,7.26877985582953,28.4810919739049));
#111489=CARTESIAN_POINT('Ctrl Pts',(4.78940248674633,7.24503721132281,28.0801669365623));
#111490=CARTESIAN_POINT('Ctrl Pts',(5.01323694710571,7.22129456681608,27.6826232117484));
#111491=CARTESIAN_POINT('Ctrl Pts',(5.35280833269681,7.19755192230936,27.4693839769732));
#111492=CARTESIAN_POINT('Ctrl Pts',(5.69237971828791,7.17380927780263,27.256144742198));
#111493=CARTESIAN_POINT('Ctrl Pts',(6.14768802911073,7.1500666332959,27.2272099974613));
#111494=CARTESIAN_POINT('Ctrl Pts',(6.51152127673494,7.12632398878917,27.3957480235561));
#111495=CARTESIAN_POINT('Ctrl Pts',(6.87535452435914,7.10258134428244,27.5642860496508));
#111496=CARTESIAN_POINT('Ctrl Pts',(7.14771270878473,7.07883869977572,27.9302968465769));
#111497=CARTESIAN_POINT('Ctrl Pts',(7.20464490743174,7.05509605526899,28.3272079454368));
#111498=CARTESIAN_POINT('Ctrl Pts',(7.26157710607875,7.03135341076227,28.7241190442966));
#111499=CARTESIAN_POINT('Ctrl Pts',(7.10308331894717,7.00761076625553,29.1519304450902));
#111500=CARTESIAN_POINT('Ctrl Pts',(6.80129449308499,6.98386812174881,29.4159440839734));
#111501=CARTESIAN_POINT('Ctrl Pts',(6.4995056672228,6.96012547724208,29.6799577228565));
#111502=CARTESIAN_POINT('Ctrl Pts',(6.05442180263,6.93638283273536,29.7801735998292));
#111503=CARTESIAN_POINT('Ctrl Pts',(5.66860169247643,6.91264018822864,29.6709831838372));
#111504=CARTESIAN_POINT('Ctrl Pts',(5.28278158232287,6.88889754372191,29.5617927678452));
#111505=CARTESIAN_POINT('Ctrl Pts',(4.95622522660852,6.86515489921517,29.2431960588884));
#111506=CARTESIAN_POINT('Ctrl Pts',(4.83754932146633,6.84141225470845,28.8601872949515));
#111507=CARTESIAN_POINT('Ctrl Pts',(4.80169458831506,6.83423905318894,28.7444714972999));
#111508=CARTESIAN_POINT('Ctrl Pts',(4.78481484417915,6.82706585166944,28.6228762721584));
#111509=CARTESIAN_POINT('Ctrl Pts',(4.7857905243208,6.81989265014994,28.5010169731875));
#111510=CARTESIAN_POINT('Origin',(6.,11.5,28.5));
#111511=CARTESIAN_POINT('',(4.78657973631996,6.30510734985006,28.4993396990272));
#111512=CARTESIAN_POINT('',(4.7865055641924,6.36989265014994,28.4992804641432));
#111513=CARTESIAN_POINT('',(4.785,11.5,28.5));
#111514=CARTESIAN_POINT('Ctrl Pts',(4.78657973631996,6.30510734985006,28.4993396990272));
#111515=CARTESIAN_POINT('Ctrl Pts',(4.78782730054607,6.31960341144713,28.7459941216511));
#111516=CARTESIAN_POINT('Ctrl Pts',(4.86088012182984,6.3340994730442,28.9933240138827));
#111517=CARTESIAN_POINT('Ctrl Pts',(5.00056288347954,6.34859553464127,29.1943722062399));
#111518=CARTESIAN_POINT('Ctrl Pts',(5.2293448965359,6.37233817914799,29.5236627330422));
#111519=CARTESIAN_POINT('Ctrl Pts',(5.63686929643189,6.39608082365472,29.7287973404918));
#111520=CARTESIAN_POINT('Ctrl Pts',(6.03765321153539,6.41982346816145,29.716395274483));
#111521=CARTESIAN_POINT('Ctrl Pts',(6.4384371266389,6.44356611266817,29.7039932084742));
#111522=CARTESIAN_POINT('Ctrl Pts',(6.83248055694992,6.4673087571749,29.4740544690069));
#111523=CARTESIAN_POINT('Ctrl Pts',(7.04046227913832,6.49105140168162,29.1312368157233));
#111524=CARTESIAN_POINT('Ctrl Pts',(7.24844400132672,6.51479404618835,28.7884191624396));
#111525=CARTESIAN_POINT('Ctrl Pts',(7.2703640153925,6.53853669069508,28.3327225953394));
#111526=CARTESIAN_POINT('Ctrl Pts',(7.09624186544805,6.56227933520181,27.9715296209521));
#111527=CARTESIAN_POINT('Ctrl Pts',(6.92211971550361,6.58602197970853,27.6103366465647));
#111528=CARTESIAN_POINT('Ctrl Pts',(6.55195540154897,6.60976462421526,27.34364726489));
#111529=CARTESIAN_POINT('Ctrl Pts',(6.15421402361284,6.63350726872199,27.2928356778359));
#111530=CARTESIAN_POINT('Ctrl Pts',(5.75647264567669,6.65724991322871,27.2420240907819));
#111531=CARTESIAN_POINT('Ctrl Pts',(5.33115420375906,6.68099255773544,27.4070902983484));
#111532=CARTESIAN_POINT('Ctrl Pts',(5.07182101068302,6.70473520224217,27.7129106128969));
#111533=CARTESIAN_POINT('Ctrl Pts',(4.88842147575827,6.72152591811147,27.9291856789363));
#111534=CARTESIAN_POINT('Ctrl Pts',(4.78803563470554,6.73831663398076,28.2158556651857));
#111535=CARTESIAN_POINT('Ctrl Pts',(4.78568939793849,6.75510734985006,28.5010383098413));
#111536=CARTESIAN_POINT('Ctrl Pts',(4.7857905243208,6.81989265014994,28.5010169731875));
#111537=CARTESIAN_POINT('Ctrl Pts',(4.78804425669356,6.80332320716271,28.2195330777089));
#111538=CARTESIAN_POINT('Ctrl Pts',(4.88556881466696,6.78675376417549,27.9366401688485));
#111539=CARTESIAN_POINT('Ctrl Pts',(5.0645656358046,6.77018432118827,27.7215471145434));
#111540=CARTESIAN_POINT('Ctrl Pts',(5.32105330985508,6.74644167668155,27.4133365169892));
#111541=CARTESIAN_POINT('Ctrl Pts',(5.74482411252607,6.72269903217482,27.2443361407978));
#111542=CARTESIAN_POINT('Ctrl Pts',(6.14301905243894,6.69895638766809,27.2914586854481));
#111543=CARTESIAN_POINT('Ctrl Pts',(6.54121399235184,6.67521374316136,27.3385812300984));
#111544=CARTESIAN_POINT('Ctrl Pts',(6.91383306950661,6.65147109865463,27.6018266955903));
#111545=CARTESIAN_POINT('Ctrl Pts',(7.09129598870183,6.62772845414791,27.9613910176794));
#111546=CARTESIAN_POINT('Ctrl Pts',(7.26875890789705,6.60398580964118,28.3209553397684));
#111547=CARTESIAN_POINT('Ctrl Pts',(7.25106566913272,6.58024316513446,28.7768385184546));
#111548=CARTESIAN_POINT('Ctrl Pts',(7.04626926625309,6.55650052062773,29.1215676599761));
#111549=CARTESIAN_POINT('Ctrl Pts',(6.84147286337347,6.532757876121,29.4662968014976));
#111550=CARTESIAN_POINT('Ctrl Pts',(6.44957329637856,6.50901523161427,29.6998719058545));
#111551=CARTESIAN_POINT('Ctrl Pts',(6.04892360307319,6.48527258710755,29.7159909311749));
#111552=CARTESIAN_POINT('Ctrl Pts',(5.64827390976782,6.46152994260082,29.7321099564952));
#111553=CARTESIAN_POINT('Ctrl Pts',(5.238874090152,6.43778729809409,29.5307729027791));
#111554=CARTESIAN_POINT('Ctrl Pts',(5.00704592749372,6.41404465358737,29.2036115246945));
#111555=CARTESIAN_POINT('Ctrl Pts',(4.86334278564024,6.39932731910822,29.0008142571633));
#111556=CARTESIAN_POINT('Ctrl Pts',(4.78786939497795,6.38460998462908,28.7496705221128));
#111557=CARTESIAN_POINT('Ctrl Pts',(4.7865055641924,6.36989265014994,28.4992804641432));
#111558=CARTESIAN_POINT('Origin',(6.,11.5,28.5));
#111559=CARTESIAN_POINT('',(4.78521076863826,5.85510734985006,28.4999698544854));
#111560=CARTESIAN_POINT('',(4.78332770288896,5.91989265014994,28.4996492411853));
#111561=CARTESIAN_POINT('',(4.785,11.5,28.5));
#111562=CARTESIAN_POINT('Ctrl Pts',(4.78521076863826,5.85510734985006,28.4999698544854));
#111563=CARTESIAN_POINT('Ctrl Pts',(4.78688595225555,5.87714754440676,28.8736362294688));
#111564=CARTESIAN_POINT('Ctrl Pts',(4.9692800988606,5.89918773896347,29.2462280232147));
#111565=CARTESIAN_POINT('Ctrl Pts',(5.26571199057474,5.92122793352018,29.4703193131787));
#111566=CARTESIAN_POINT('Ctrl Pts',(5.58504116016609,5.94497057802691,29.7117200785386));
#111567=CARTESIAN_POINT('Ctrl Pts',(6.03670570510543,5.96871322253364,29.7807930774338));
#111568=CARTESIAN_POINT('Ctrl Pts',(6.41393766043131,5.99245586704037,29.6446392534136));
#111569=CARTESIAN_POINT('Ctrl Pts',(6.7911696157572,6.01619851154709,29.5084854293935));
#111570=CARTESIAN_POINT('Ctrl Pts',(7.09396898146964,6.03994115605382,29.1671047824581));
#111571=CARTESIAN_POINT('Ctrl Pts',(7.18504576598691,6.06368380056054,28.7765363638774));
#111572=CARTESIAN_POINT('Ctrl Pts',(7.27612255050417,6.08742644506727,28.3859679452967));
#111573=CARTESIAN_POINT('Ctrl Pts',(7.15547675382629,6.11116908957399,27.9462117550706));
#111574=CARTESIAN_POINT('Ctrl Pts',(6.8777606839509,6.13491173408072,27.6570623303207));
#111575=CARTESIAN_POINT('Ctrl Pts',(6.6000446140755,6.15865437858745,27.3679129055707));
#111576=CARTESIAN_POINT('Ctrl Pts',(6.16525827100258,6.18239702309418,27.2293702462968));
#111577=CARTESIAN_POINT('Ctrl Pts',(5.7714033811428,6.2061396676009,27.3046591166773));
#111578=CARTESIAN_POINT('Ctrl Pts',(5.37754849128302,6.22988231210763,27.3799479870579));
#111579=CARTESIAN_POINT('Ctrl Pts',(5.02462505463636,6.25362495661436,27.6690683870929));
#111580=CARTESIAN_POINT('Ctrl Pts',(4.8731831494214,6.27736760112108,28.0403518101878));
#111581=CARTESIAN_POINT('Ctrl Pts',(4.81420403560912,6.28661418403074,28.1849482957923));
#111582=CARTESIAN_POINT('Ctrl Pts',(4.7857839542398,6.2958607669404,28.3420065810935));
#111583=CARTESIAN_POINT('Ctrl Pts',(4.78657973631996,6.30510734985006,28.4993396990272));
#111584=CARTESIAN_POINT('Ctrl Pts',(4.7865055641924,6.36989265014994,28.4992804641432));
#111585=CARTESIAN_POINT('Ctrl Pts',(4.78566920379832,6.36086734012235,28.3457303831688));
#111586=CARTESIAN_POINT('Ctrl Pts',(4.81270304898673,6.35184203009477,28.1924637357382));
#111587=CARTESIAN_POINT('Ctrl Pts',(4.86896310729236,6.34281672006719,28.0508040477679));
#111588=CARTESIAN_POINT('Ctrl Pts',(5.01696495545002,6.31907407556046,27.6781436513788));
#111589=CARTESIAN_POINT('Ctrl Pts',(5.36722515746609,6.29533143105373,27.3858085610538));
#111590=CARTESIAN_POINT('Ctrl Pts',(5.76035025534992,6.27158878654701,27.3068516283844));
#111591=CARTESIAN_POINT('Ctrl Pts',(6.15347535323376,6.24784614204028,27.2278946957151));
#111592=CARTESIAN_POINT('Ctrl Pts',(6.58946534698536,6.22410349753355,27.3623159207015));
#111593=CARTESIAN_POINT('Ctrl Pts',(6.86987889282973,6.20036085302683,27.6489196092493));
#111594=CARTESIAN_POINT('Ctrl Pts',(7.15029243867409,6.1766182085201,27.9355232977971));
#111595=CARTESIAN_POINT('Ctrl Pts',(7.27512953661121,6.15287556401338,28.3743094499063));
#111596=CARTESIAN_POINT('Ctrl Pts',(7.18761773225989,6.12913291950665,28.76562478708));
#111597=CARTESIAN_POINT('Ctrl Pts',(7.10010592790856,6.10539027499992,29.1569401242537));
#111598=CARTESIAN_POINT('Ctrl Pts',(6.80024522126877,6.08164763049319,29.500784646492));
#111599=CARTESIAN_POINT('Ctrl Pts',(6.42442266508831,6.05790498598646,29.6405969976474));
#111600=CARTESIAN_POINT('Ctrl Pts',(6.04860010890784,6.03416234147974,29.7804093488027));
#111601=CARTESIAN_POINT('Ctrl Pts',(5.5968157031867,6.01041969697301,29.7161895288751));
#111602=CARTESIAN_POINT('Ctrl Pts',(5.27483437848997,5.98667705246629,29.4773138784283));
#111603=CARTESIAN_POINT('Ctrl Pts',(4.97293975282596,5.96441558502751,29.2533404068618));
#111604=CARTESIAN_POINT('Ctrl Pts',(4.78515793691401,5.94215411758873,28.8758230640495));
#111605=CARTESIAN_POINT('Ctrl Pts',(4.78332770288896,5.91989265014994,28.4996492411853));
#111606=CARTESIAN_POINT('Origin',(6.,12.2318726682356,28.5));
#111607=CARTESIAN_POINT('',(5.04299591138157,6.15687266823562,28.4994792317636));
#111608=CARTESIAN_POINT('',(5.04043108748423,6.06812733176437,28.4997233624409));
#111609=CARTESIAN_POINT('',(5.04175,12.2318726682356,28.4999999999999));
#111610=CARTESIAN_POINT('',(6.39740818880394,5.85,29.3719574496336));
#111611=CARTESIAN_POINT('Ctrl Pts',(5.04299591138157,6.15687266823562,28.4994792317636));
#111612=CARTESIAN_POINT('Ctrl Pts',(5.04236829148172,6.14762608532596,28.375393256241));
#111613=CARTESIAN_POINT('Ctrl Pts',(5.12233675351758,6.11463685790957,27.9334624481512));
#111614=CARTESIAN_POINT('Ctrl Pts',(5.78742775715113,6.05790498598646,27.388609494045));
#111615=CARTESIAN_POINT('Ctrl Pts',(6.81615371579216,5.98667705246629,27.7164082674999));
#111616=CARTESIAN_POINT('Ctrl Pts',(7.09388787989744,5.91737539047079,28.7287545013986));
#111617=CARTESIAN_POINT('Ctrl Pts',(6.66163337938062,5.87181637298203,29.2514323241542));
#111618=CARTESIAN_POINT('Ctrl Pts',(6.39766230306601,5.85,29.3734910038904));
#111619=CARTESIAN_POINT('',(6.95384139680377,5.85,28.4081868623593));
#111620=CARTESIAN_POINT('Origin',(6.,5.85,28.5));
#111621=CARTESIAN_POINT('Ctrl Pts',(5.04043108748423,6.06812733176437,28.4997233624409));
#111622=CARTESIAN_POINT('Ctrl Pts',(5.04033504522546,6.06664615469643,28.479983491394));
#111623=CARTESIAN_POINT('Ctrl Pts',(5.0497558598512,6.04142233312176,28.1439016856491));
#111624=CARTESIAN_POINT('Ctrl Pts',(5.44295412205162,5.99245586704036,27.5143710763459));
#111625=CARTESIAN_POINT('Ctrl Pts',(6.52391074184675,5.92122793352018,27.4975948676703));
#111626=CARTESIAN_POINT('Ctrl Pts',(6.92340443678229,5.87374264450673,28.0919790384314));
#111627=CARTESIAN_POINT('Ctrl Pts',(6.95384139680377,5.85,28.4081868623593));
#111628=CARTESIAN_POINT('Origin',(6.,12.2318726682356,28.5));
#111629=CARTESIAN_POINT('',(5.04229371652227,6.60687266823562,28.500818897453));
#111630=CARTESIAN_POINT('',(5.04293741307602,6.51812733176437,28.49943251421));
#111631=CARTESIAN_POINT('',(5.04175,12.2318726682356,28.4999999999999));
#111632=CARTESIAN_POINT('Ctrl Pts',(5.04229371652227,6.60687266823562,28.500818897453));
#111633=CARTESIAN_POINT('Ctrl Pts',(5.04414415387375,6.59008195236632,28.2759001573367));
#111634=CARTESIAN_POINT('Ctrl Pts',(5.23526955473714,6.5495485919903,27.7301068914455));
#111635=CARTESIAN_POINT('Ctrl Pts',(6.14337556352862,6.48527258710754,27.3776706926676));
#111636=CARTESIAN_POINT('Ctrl Pts',(7.01920261006453,6.41404465358737,28.0086709395559));
#111637=CARTESIAN_POINT('Ctrl Pts',(6.96733877431504,6.34281672006719,29.0868715208489));
#111638=CARTESIAN_POINT('Ctrl Pts',(6.03501255926435,6.271588786547,29.630917933428));
#111639=CARTESIAN_POINT('Ctrl Pts',(5.19596203684428,6.20960743593649,29.2085670273447));
#111640=CARTESIAN_POINT('Ctrl Pts',(5.04397984423725,6.17136872983269,28.6940114132281));
#111641=CARTESIAN_POINT('Ctrl Pts',(5.04299591138157,6.15687266823562,28.4994792317636));
#111642=CARTESIAN_POINT('Ctrl Pts',(5.04293741307602,6.51812733176437,28.49943251421));
#111643=CARTESIAN_POINT('Ctrl Pts',(5.04227778974465,6.50910202173679,28.3783301561082));
#111644=CARTESIAN_POINT('Ctrl Pts',(5.11968788031139,6.47633406720248,27.9394586239317));
#111645=CARTESIAN_POINT('Ctrl Pts',(5.77718546973152,6.41982346816144,27.3906962578813));
#111646=CARTESIAN_POINT('Ctrl Pts',(6.80875932531787,6.34859553464126,27.7087435142843));
#111647=CARTESIAN_POINT('Ctrl Pts',(7.10413006383205,6.27736760112109,28.7469332186266));
#111648=CARTESIAN_POINT('Ctrl Pts',(6.39464482398617,6.2061396676009,29.5604863382188));
#111649=CARTESIAN_POINT('Ctrl Pts',(5.34792918744311,6.13639291114867,29.4116987996429));
#111650=CARTESIAN_POINT('Ctrl Pts',(5.04187456217927,6.09038879920316,28.7964053095682));
#111651=CARTESIAN_POINT('Ctrl Pts',(5.04043108748423,6.06812733176437,28.4997233624409));
#111652=CARTESIAN_POINT('Origin',(6.,12.2318726682356,28.5));
#111653=CARTESIAN_POINT('',(5.04022028209014,7.05687266823562,28.4998553377795));
#111654=CARTESIAN_POINT('',(5.04237347319375,6.96812733176437,28.500802069594));
#111655=CARTESIAN_POINT('',(5.04175,12.2318726682356,28.4999999999999));
#111656=CARTESIAN_POINT('Ctrl Pts',(5.04022028209014,7.05687266823562,28.4998553377795));
#111657=CARTESIAN_POINT('Ctrl Pts',(5.04020358373367,7.05628046391341,28.4919668432765));
#111658=CARTESIAN_POINT('Ctrl Pts',(5.04385653111531,7.03194561508447,28.1678288346137));
#111659=CARTESIAN_POINT('Ctrl Pts',(5.40719788686653,6.98386812174881,27.5362768396409));
#111660=CARTESIAN_POINT('Ctrl Pts',(6.48506814368224,6.91264018822863,27.4778035200293));
#111661=CARTESIAN_POINT('Ctrl Pts',(7.12142693158516,6.84141225470845,28.3497388271955));
#111662=CARTESIAN_POINT('Ctrl Pts',(6.73705697947822,6.77018432118827,29.3584424510732));
#111663=CARTESIAN_POINT('Ctrl Pts',(5.68181420799896,6.6989563876681,29.5857876606995));
#111664=CARTESIAN_POINT('Ctrl Pts',(5.09666865493704,6.6445191700172,29.0042218556903));
#111665=CARTESIAN_POINT('Ctrl Pts',(5.04152757239145,6.61382459687305,28.5939429216269));
#111666=CARTESIAN_POINT('Ctrl Pts',(5.04229371652227,6.60687266823562,28.500818897453));
#111667=CARTESIAN_POINT('Ctrl Pts',(5.04237347319375,6.96812733176437,28.500802069594));
#111668=CARTESIAN_POINT('Ctrl Pts',(5.04415095389023,6.95155788877715,28.2788004705469));
#111669=CARTESIAN_POINT('Ctrl Pts',(5.23128117013677,6.9112458012832,27.7359852831753));
#111670=CARTESIAN_POINT('Ctrl Pts',(6.13296796501039,6.84719106928253,27.3763913550898));
#111671=CARTESIAN_POINT('Ctrl Pts',(7.01460310250063,6.77596313576235,27.9992431262198));
#111672=CARTESIAN_POINT('Ctrl Pts',(6.97274002584404,6.70473520224217,29.0778852397409));
#111673=CARTESIAN_POINT('Ctrl Pts',(6.04548629726899,6.63350726872199,29.6305354712223));
#111674=CARTESIAN_POINT('Ctrl Pts',(5.19956529207796,6.57130464522939,29.2145234587558));
#111675=CARTESIAN_POINT('Ctrl Pts',(5.04401304340543,6.53284466624352,28.6969109282424));
#111676=CARTESIAN_POINT('Ctrl Pts',(5.04293741307602,6.51812733176437,28.49943251421));
#111677=CARTESIAN_POINT('Origin',(6.,12.2318726682356,28.5));
#111678=CARTESIAN_POINT('',(5.04269212277596,7.50687266823562,28.4993000253505));
#111679=CARTESIAN_POINT('',(5.04020384857308,7.41812733176437,28.4999090719931));
#111680=CARTESIAN_POINT('',(5.04175,12.2318726682356,28.4999999999999));
#111681=CARTESIAN_POINT('Ctrl Pts',(5.04269212277596,7.50687266823562,28.4993000253505));
#111682=CARTESIAN_POINT('Ctrl Pts',(5.04194787696276,7.49873633095377,28.3901956284784));
#111683=CARTESIAN_POINT('Ctrl Pts',(5.10944269904413,7.4668573491652,27.9636066549997));
#111684=CARTESIAN_POINT('Ctrl Pts',(5.73605199225171,7.41123572286989,27.399769041722));
#111685=CARTESIAN_POINT('Ctrl Pts',(6.77872206706446,7.34000778934971,27.679165878216));
#111686=CARTESIAN_POINT('Ctrl Pts',(7.11259528197041,7.26877985582954,28.705690188041));
#111687=CARTESIAN_POINT('Ctrl Pts',(6.43377850272267,7.19755192230935,29.5449942194001));
#111688=CARTESIAN_POINT('Ctrl Pts',(5.36906079542399,7.12691619311139,29.4340690904762));
#111689=CARTESIAN_POINT('Ctrl Pts',(5.0408730539258,7.08002310842014,28.8082322159783));
#111690=CARTESIAN_POINT('Ctrl Pts',(5.04022028209014,7.05687266823562,28.4998553377795));
#111691=CARTESIAN_POINT('Ctrl Pts',(5.04020384857308,7.41812733176437,28.4999090719931));
#111692=CARTESIAN_POINT('Ctrl Pts',(5.04019712215809,7.41775640032424,28.4949682856195));
#111693=CARTESIAN_POINT('Ctrl Pts',(5.04246416833165,7.39364282437738,28.1737831212255));
#111694=CARTESIAN_POINT('Ctrl Pts',(5.39829109152546,7.34578660392379,27.5418126900042));
#111695=CARTESIAN_POINT('Ctrl Pts',(6.47557303929329,7.27455867040361,27.4733516550811));
#111696=CARTESIAN_POINT('Ctrl Pts',(7.1199859534311,7.20333073688343,28.3393512752155));
#111697=CARTESIAN_POINT('Ctrl Pts',(6.7449818262241,7.13210280336324,29.351574175982));
#111698=CARTESIAN_POINT('Ctrl Pts',(5.69189142314743,7.06087486984307,29.5886898898316));
#111699=CARTESIAN_POINT('Ctrl Pts',(5.09898079581291,7.00621637931011,29.0102311605227));
#111700=CARTESIAN_POINT('Ctrl Pts',(5.04160397072811,6.97530053328388,28.5969104426302));
#111701=CARTESIAN_POINT('Ctrl Pts',(5.04237347319375,6.96812733176437,28.500802069594));
#111702=CARTESIAN_POINT('Origin',(6.,12.2318726682356,28.5));
#111703=CARTESIAN_POINT('',(5.04266942812141,7.95687266823562,28.5007094137961));
#111704=CARTESIAN_POINT('',(5.04262349743768,7.86812733176438,28.4992726076031));
#111705=CARTESIAN_POINT('',(5.04175,12.2318726682356,28.4999999999999));
#111706=CARTESIAN_POINT('Ctrl Pts',(5.04266942812141,7.95687266823562,28.5007094137961));
#111707=CARTESIAN_POINT('Ctrl Pts',(5.04412538743029,7.94119219799413,28.290454354913));
#111708=CARTESIAN_POINT('Ctrl Pts',(5.21569019260146,7.90176908324592,27.7596801563291));
#111709=CARTESIAN_POINT('Ctrl Pts',(6.09104560108126,7.83860332399098,27.372220140497));
#111710=CARTESIAN_POINT('Ctrl Pts',(6.99525699353418,7.76737539047079,27.9618176611926));
#111711=CARTESIAN_POINT('Ctrl Pts',(6.99358031256864,7.69614745695062,29.041271535836));
#111712=CARTESIAN_POINT('Ctrl Pts',(6.08754168182046,7.62491952343044,29.6280572533568));
#111713=CARTESIAN_POINT('Ctrl Pts',(5.2144204906732,7.56182792719211,29.2383378989303));
#111714=CARTESIAN_POINT('Ctrl Pts',(5.04411966054992,7.5224789754605,28.7085731513516));
#111715=CARTESIAN_POINT('Ctrl Pts',(5.04269212277596,7.50687266823562,28.4993000253505));
#111716=CARTESIAN_POINT('Ctrl Pts',(5.04262349743768,7.86812733176438,28.4992726076031));
#111717=CARTESIAN_POINT('Ctrl Pts',(5.04186750558486,7.8602122673646,28.3931545728878));
#111718=CARTESIAN_POINT('Ctrl Pts',(5.10698130687874,7.8285545584581,27.9696178276289));
#111719=CARTESIAN_POINT('Ctrl Pts',(5.72586583137092,7.77315420504486,27.4022627845939));
#111720=CARTESIAN_POINT('Ctrl Pts',(6.7710806444101,7.7019262715247,27.6719835892955));
#111721=CARTESIAN_POINT('Ctrl Pts',(7.11445385898466,7.6306983380045,28.6953692224212));
#111722=CARTESIAN_POINT('Ctrl Pts',(6.44344539503938,7.55947040448434,29.5409287764079));
#111723=CARTESIAN_POINT('Ctrl Pts',(5.37440697636399,7.48861340240428,29.4395602215249));
#111724=CARTESIAN_POINT('Ctrl Pts',(5.04062766770599,7.44149904483097,28.8112190041108));
#111725=CARTESIAN_POINT('Ctrl Pts',(5.04020384857308,7.41812733176437,28.4999090719931));
#111726=CARTESIAN_POINT('Origin',(6.,12.2318726682356,28.5));
#111727=CARTESIAN_POINT('',(5.04021395554822,8.40687266823562,28.5001267151889));
#111728=CARTESIAN_POINT('',(5.04273619519586,8.31812733176437,28.5006805243453));
#111729=CARTESIAN_POINT('',(5.04175,12.2318726682356,28.4999999999999));
#111730=CARTESIAN_POINT('Ctrl Pts',(5.04021395554822,8.40687266823562,28.5001267151889));
#111731=CARTESIAN_POINT('Ctrl Pts',(5.04079193445267,8.38364806503449,28.1907674277398));
#111732=CARTESIAN_POINT('Ctrl Pts',(5.37084730702173,8.33668081732663,27.564088380757));
#111733=CARTESIAN_POINT('Ctrl Pts',(6.43702271497452,8.26597092511206,27.4563583663045));
#111734=CARTESIAN_POINT('Ctrl Pts',(7.11322889506391,8.19474299159188,28.2977671139973));
#111735=CARTESIAN_POINT('Ctrl Pts',(6.77616836554943,8.1235150580717,29.3232492826038));
#111736=CARTESIAN_POINT('Ctrl Pts',(5.73263536721262,8.05228712455152,29.5994056876876));
#111737=CARTESIAN_POINT('Ctrl Pts',(5.10861382433492,7.99673966127282,29.0343785992878));
#111738=CARTESIAN_POINT('Ctrl Pts',(5.04192084102608,7.96493484250086,28.6088128634222));
#111739=CARTESIAN_POINT('Ctrl Pts',(5.04266942812141,7.95687266823562,28.5007094137961));
#111740=CARTESIAN_POINT('Ctrl Pts',(5.04273619519585,8.31812733176437,28.5006805243453));
#111741=CARTESIAN_POINT('Ctrl Pts',(5.04410682382072,8.30266813440496,28.2933560883282));
#111742=CARTESIAN_POINT('Ctrl Pts',(5.21191596650108,8.26346629253882,27.7655957456847));
#111743=CARTESIAN_POINT('Ctrl Pts',(6.08058882997138,8.20052180616596,27.3714248022129));
#111744=CARTESIAN_POINT('Ctrl Pts',(6.99022601937189,8.12929387264577,27.9526162524013));
#111745=CARTESIAN_POINT('Ctrl Pts',(6.99855435409013,8.0580659391256,29.032039226478));
#111746=CARTESIAN_POINT('Ctrl Pts',(6.09799334069262,7.98683800560541,29.62719733931));
#111747=CARTESIAN_POINT('Ctrl Pts',(5.21822287040342,7.92352513648501,29.2442489249259));
#111748=CARTESIAN_POINT('Ctrl Pts',(5.04413523770993,7.88395491187133,28.7114745064653));
#111749=CARTESIAN_POINT('Ctrl Pts',(5.04262349743768,7.86812733176438,28.4992726076031));
#111750=CARTESIAN_POINT('Origin',(6.,12.2318726682356,28.5));
#111751=CARTESIAN_POINT('',(5.04232064019591,8.85687266823562,28.4991864750727));
#111752=CARTESIAN_POINT('',(5.04023521160163,8.76812733176438,28.5001800208846));
#111753=CARTESIAN_POINT('',(5.04175,12.2318726682356,28.4999999999999));
#111754=CARTESIAN_POINT('Ctrl Pts',(5.04232064019591,8.85687266823562,28.4991864750727));
#111755=CARTESIAN_POINT('Ctrl Pts',(5.04155303324115,8.84984657658158,28.4050622393142));
#111756=CARTESIAN_POINT('Ctrl Pts',(5.09743993967769,8.81907784042081,27.9937639308669));
#111757=CARTESIAN_POINT('Ctrl Pts',(5.68518862833307,8.76456645975332,27.4132293189198));
#111758=CARTESIAN_POINT('Ctrl Pts',(6.73972027305326,8.69333852623316,27.6438512800801));
#111759=CARTESIAN_POINT('Ctrl Pts',(7.12095469163445,8.62211059271294,28.6537442431088));
#111760=CARTESIAN_POINT('Ctrl Pts',(6.48189034053387,8.5508826591928,29.5236983992791));
#111761=CARTESIAN_POINT('Ctrl Pts',(5.40420690407899,8.47965472567259,29.4618769671009));
#111762=CARTESIAN_POINT('Ctrl Pts',(5.04338669711544,8.43165139535355,28.8301752268289));
#111763=CARTESIAN_POINT('Ctrl Pts',(5.04020106331735,8.40739070954122,28.5070271942964));
#111764=CARTESIAN_POINT('Ctrl Pts',(5.04021395554822,8.40687266823562,28.5001267151889));
#111765=CARTESIAN_POINT('Ctrl Pts',(5.04023521160163,8.76812733176438,28.5001800208846));
#111766=CARTESIAN_POINT('Ctrl Pts',(5.04103064105211,8.74512400144532,28.1937500051567));
#111767=CARTESIAN_POINT('Ctrl Pts',(5.36553297683283,8.69837802661954,27.5695919335309));
#111768=CARTESIAN_POINT('Ctrl Pts',(6.42733089615622,8.62788940728704,27.4523527111821));
#111769=CARTESIAN_POINT('Ctrl Pts',(7.1113066008254,8.55666147376686,28.2874578264456));
#111770=CARTESIAN_POINT('Ctrl Pts',(6.78376527806854,8.48543354024668,29.3160199295799));
#111771=CARTESIAN_POINT('Ctrl Pts',(5.7428367373441,8.41420560672649,29.601836463781));
#111772=CARTESIAN_POINT('Ctrl Pts',(5.11109853529383,8.35843687056573,29.040389798058));
#111773=CARTESIAN_POINT('Ctrl Pts',(5.04200177609836,8.32641077891169,28.6117704450034));
#111774=CARTESIAN_POINT('Ctrl Pts',(5.04273619519585,8.31812733176437,28.5006805243453));
#111775=CARTESIAN_POINT('Origin',(6.,12.2318726682356,28.5));
#111776=CARTESIAN_POINT('',(5.04297099545381,9.30687266823563,28.5005441005051));
#111777=CARTESIAN_POINT('',(5.04223964716892,9.21812733176437,28.4991714298536));
#111778=CARTESIAN_POINT('',(5.04175,12.2318726682356,28.4999999999999));
#111779=CARTESIAN_POINT('Ctrl Pts',(5.04297099545381,9.30687266823563,28.5005441005051));
#111780=CARTESIAN_POINT('Ctrl Pts',(5.0439879065076,9.29230244362195,28.3050212100339));
#111781=CARTESIAN_POINT('Ctrl Pts',(5.19717400985829,9.25398957450154,27.7894242676125));
#111782=CARTESIAN_POINT('Ctrl Pts',(6.03851769375916,9.19193406087441,27.3692068711474));
#111783=CARTESIAN_POINT('Ctrl Pts',(6.96916130750066,9.12070612735422,27.9161309453062));
#111784=CARTESIAN_POINT('Ctrl Pts',(7.01766927646803,9.04947819383405,28.9944956589479));
#111785=CARTESIAN_POINT('Ctrl Pts',(6.13988939591615,8.97825026031386,29.6227678610904));
#111786=CARTESIAN_POINT('Ctrl Pts',(5.23392768359053,8.91404841844773,29.2679241592235));
#111787=CARTESIAN_POINT('Ctrl Pts',(5.04414693892089,8.87358922108831,28.7231278694141));
#111788=CARTESIAN_POINT('Ctrl Pts',(5.04232064019591,8.85687266823562,28.4991864750727));
#111789=CARTESIAN_POINT('Ctrl Pts',(5.04223964716892,9.21812733176438,28.4991714298536));
#111790=CARTESIAN_POINT('Ctrl Pts',(5.04147759709558,9.21132251299241,28.4080310177188));
#111791=CARTESIAN_POINT('Ctrl Pts',(5.09515055781774,9.18077504971372,27.9997725890198));
#111792=CARTESIAN_POINT('Ctrl Pts',(5.6751294127762,9.1264849419283,27.416193911193));
#111793=CARTESIAN_POINT('Ctrl Pts',(6.73175321387293,9.05525700840812,27.6370319991079));
#111794=CARTESIAN_POINT('Ctrl Pts',(7.1223314473857,8.98402907488794,28.6433480337722));
#111795=CARTESIAN_POINT('Ctrl Pts',(6.49135778099696,8.91280114136776,29.5191879451952));
#111796=CARTESIAN_POINT('Ctrl Pts',(5.41314771587932,8.84157320784758,29.4673577069521));
#111797=CARTESIAN_POINT('Ctrl Pts',(5.044797960694,8.79334860464645,28.8361311061575));
#111798=CARTESIAN_POINT('Ctrl Pts',(5.04020964694338,8.76886664595205,28.5100285104301));
#111799=CARTESIAN_POINT('Ctrl Pts',(5.04023521160163,8.76812733176438,28.5001800208846));
#111800=CARTESIAN_POINT('Origin',(6.,12.2318726682356,28.5));
#111801=CARTESIAN_POINT('',(5.04038444040905,9.75687266823562,28.5003835829357));
#111802=CARTESIAN_POINT('',(5.0430205615309,9.66812733176438,28.500505644125));
#111803=CARTESIAN_POINT('',(5.04175,12.2318726682356,28.4999999999999));
#111804=CARTESIAN_POINT('Ctrl Pts',(5.04038444040905,9.75687266823562,28.5003835829357));
#111805=CARTESIAN_POINT('Ctrl Pts',(5.04188850652928,9.73475831066231,28.2056733548791));
#111806=CARTESIAN_POINT('Ctrl Pts',(5.34466159125839,9.68890130858227,27.5918810980426));
#111807=CARTESIAN_POINT('Ctrl Pts',(6.38803224649353,9.61930166199549,27.4371699623346));
#111808=CARTESIAN_POINT('Ctrl Pts',(7.10262364459654,9.54807372847531,28.2462327614415));
#111809=CARTESIAN_POINT('Ctrl Pts',(6.8136012869641,9.47684579495514,29.286275815956));
#111810=CARTESIAN_POINT('Ctrl Pts',(5.78403482147721,9.40561786143493,29.6106465480502));
#111811=CARTESIAN_POINT('Ctrl Pts',(5.12143631245245,9.34896015252845,29.0645392296898));
#111812=CARTESIAN_POINT('Ctrl Pts',(5.04233081759613,9.31604508812868,28.6236319799069));
#111813=CARTESIAN_POINT('Ctrl Pts',(5.04297099545381,9.30687266823563,28.5005441005051));
#111814=CARTESIAN_POINT('Ctrl Pts',(5.0430205615309,9.66812733176438,28.500505644125));
#111815=CARTESIAN_POINT('Ctrl Pts',(5.04394831887074,9.65377838003277,28.3079271288657));
#111816=CARTESIAN_POINT('Ctrl Pts',(5.193608544855,9.61568678379445,27.7953697292877));
#111817=CARTESIAN_POINT('Ctrl Pts',(6.02803525397329,9.55385254304938,27.3688985186306));
#111818=CARTESIAN_POINT('Ctrl Pts',(6.96370800764262,9.48262460952921,27.9071733705549));
#111819=CARTESIAN_POINT('Ctrl Pts',(7.0222087383162,9.41139667600901,28.9850420928927));
#111820=CARTESIAN_POINT('Ctrl Pts',(6.1502897777778,9.34016874248886,29.6214229885637));
#111821=CARTESIAN_POINT('Ctrl Pts',(5.23794454979289,9.27574562774062,29.2737974975242));
#111822=CARTESIAN_POINT('Ctrl Pts',(5.04413646055601,9.23506515749913,28.7260283778292));
#111823=CARTESIAN_POINT('Ctrl Pts',(5.04223964716892,9.21812733176438,28.4991714298536));
#111824=CARTESIAN_POINT('Origin',(6.,12.2318726682356,28.5));
#111825=CARTESIAN_POINT('',(5.04189765845147,10.2068726682356,28.4991386725514));
#111826=CARTESIAN_POINT('',(5.04043577631992,10.1181273317644,28.5004306020855));
#111827=CARTESIAN_POINT('',(5.04175,12.2318726682356,28.4999999999999));
#111828=CARTESIAN_POINT('Ctrl Pts',(5.04189765845147,10.2068726682356,28.4991386725514));
#111829=CARTESIAN_POINT('Ctrl Pts',(5.04118853070869,10.2009568222094,28.4199766509929));
#111830=CARTESIAN_POINT('Ctrl Pts',(5.08628951303429,10.1712983316764,28.0239028501118));
#111831=CARTESIAN_POINT('Ctrl Pts',(5.63500601835172,10.1178971966368,27.4290396512902));
#111832=CARTESIAN_POINT('Ctrl Pts',(6.69911890163688,10.0466692631166,27.6103880135778));
#111833=CARTESIAN_POINT('Ctrl Pts',(7.12689014474107,9.97544132959639,28.6014658460497));
#111834=CARTESIAN_POINT('Ctrl Pts',(6.52896013424947,9.9042133960762,29.5001889243431));
#111835=CARTESIAN_POINT('Ctrl Pts',(5.44956787014175,9.83298546255604,29.4885348680441));
#111836=CARTESIAN_POINT('Ctrl Pts',(5.05075510596856,9.78387188660917,28.8600837677074));
#111837=CARTESIAN_POINT('Ctrl Pts',(5.04027369555913,9.75850095516903,28.5220831874526));
#111838=CARTESIAN_POINT('Ctrl Pts',(5.04038444040905,9.75687266823562,28.5003835829357));
#111839=CARTESIAN_POINT('Ctrl Pts',(5.04043577631992,10.1181273317644,28.5004306020855));
#111840=CARTESIAN_POINT('Ctrl Pts',(5.04207772203641,10.0962342470731,28.2086278628711));
#111841=CARTESIAN_POINT('Ctrl Pts',(5.33958527277428,10.0505985178752,27.5974716038793));
#111842=CARTESIAN_POINT('Ctrl Pts',(6.37816468677541,9.98122014417046,27.4336192011314));
#111843=CARTESIAN_POINT('Ctrl Pts',(7.10022415948525,9.90999221065029,28.2360239865173));
#111844=CARTESIAN_POINT('Ctrl Pts',(6.82085389946722,9.83876427713011,29.2787011054732));
#111845=CARTESIAN_POINT('Ctrl Pts',(5.79433816650613,9.76753634360992,29.6126004436091));
#111846=CARTESIAN_POINT('Ctrl Pts',(5.12409916514403,9.71065736182135,29.070549220604));
#111847=CARTESIAN_POINT('Ctrl Pts',(5.04241319539131,9.6775210245395,28.6265792027564));
#111848=CARTESIAN_POINT('Ctrl Pts',(5.0430205615309,9.66812733176438,28.500505644125));
#111849=CARTESIAN_POINT('Origin',(6.,12.2318726682356,28.5));
#111850=CARTESIAN_POINT('',(5.0431799682554,10.6568726682356,28.5003376186496));
#111851=CARTESIAN_POINT('',(5.04180976972011,10.5681273317644,28.4991376522761));
#111852=CARTESIAN_POINT('',(5.04175,12.2318726682356,28.4999999999999));
#111853=CARTESIAN_POINT('Ctrl Pts',(5.0431799682554,10.6568726682356,28.5003376186496));
#111854=CARTESIAN_POINT('Ctrl Pts',(5.04375387351073,10.6434126892498,28.3196143998931));
#111855=CARTESIAN_POINT('Ctrl Pts',(5.1796945030962,10.6062100657572,27.8193040088319));
#111856=CARTESIAN_POINT('Ctrl Pts',(5.98590671384625,10.5452647977578,27.3686397261773));
#111857=CARTESIAN_POINT('Ctrl Pts',(6.94096978992682,10.4740368642377,27.8717063333662));
#111858=CARTESIAN_POINT('Ctrl Pts',(7.03955768450863,10.4028089307175,28.9466507169341));
#111859=CARTESIAN_POINT('Ctrl Pts',(6.19193458290324,10.3315809971973,29.6150504691213));
#111860=CARTESIAN_POINT('Ctrl Pts',(5.25452090191919,10.2662689097034,29.2973065776616));
#111861=CARTESIAN_POINT('Ctrl Pts',(5.04403454256094,10.2246994667161,28.73768534861));
#111862=CARTESIAN_POINT('Ctrl Pts',(5.04189765845147,10.2068726682356,28.4991386725514));
#111863=CARTESIAN_POINT('Ctrl Pts',(5.04180976972011,10.5681273317644,28.4991376522761));
#111864=CARTESIAN_POINT('Ctrl Pts',(5.04112072370537,10.5624327586202,28.4229544109879));
#111865=CARTESIAN_POINT('Ctrl Pts',(5.08416676895765,10.5329955409693,28.0299061204628));
#111866=CARTESIAN_POINT('Ctrl Pts',(5.62509554533696,10.4798156788117,27.4324687801292));
#111867=CARTESIAN_POINT('Ctrl Pts',(6.69084341099689,10.4085877452916,27.6039464366949));
#111868=CARTESIAN_POINT('Ctrl Pts',(7.12778211347718,10.3373598117714,28.5910168988298));
#111869=CARTESIAN_POINT('Ctrl Pts',(6.53820764542198,10.2661318782512,29.4952432009378));
#111870=CARTESIAN_POINT('Ctrl Pts',(5.45875381291119,10.194903944731,29.4935940386394));
#111871=CARTESIAN_POINT('Ctrl Pts',(5.05231044100045,10.1455690959021,28.8660517697691));
#111872=CARTESIAN_POINT('Ctrl Pts',(5.04029706234429,10.1199768915799,28.5250825242843));
#111873=CARTESIAN_POINT('Ctrl Pts',(5.04043577631992,10.1181273317644,28.5004306020855));
#111874=CARTESIAN_POINT('Origin',(6.,12.2318726682356,28.5));
#111875=CARTESIAN_POINT('',(5.04070147463229,11.1068726682356,28.5006572399252));
#111876=CARTESIAN_POINT('',(5.04321154726233,11.0181273317644,28.5002974317561));
#111877=CARTESIAN_POINT('',(5.04175,12.2318726682356,28.4999999999999));
#111878=CARTESIAN_POINT('Ctrl Pts',(5.04070147463229,11.1068726682356,28.5006572399252));
#111879=CARTESIAN_POINT('Ctrl Pts',(5.04276136934609,11.0858685562901,28.2205231486132));
#111880=CARTESIAN_POINT('Ctrl Pts',(5.31964162539148,11.0411217998379,27.6200006105552));
#111881=CARTESIAN_POINT('Ctrl Pts',(6.3382146275518,10.9726323988789,27.4203285596915));
#111882=CARTESIAN_POINT('Ctrl Pts',(7.08962794991972,10.9014044653588,28.1952221424384));
#111883=CARTESIAN_POINT('Ctrl Pts',(6.84927801671883,10.8301765318385,29.2476149421817));
#111884=CARTESIAN_POINT('Ctrl Pts',(5.83589966612663,10.7589485983184,29.6194791497386));
#111885=CARTESIAN_POINT('Ctrl Pts',(5.13516398712787,10.7011806437841,29.0946878303018));
#111886=CARTESIAN_POINT('Ctrl Pts',(5.04274153697795,10.6671553337565,28.6383999746367));
#111887=CARTESIAN_POINT('Ctrl Pts',(5.0431799682554,10.6568726682356,28.5003376186496));
#111888=CARTESIAN_POINT('Ctrl Pts',(5.04321154726233,11.0181273317644,28.5002974317561));
#111889=CARTESIAN_POINT('Ctrl Pts',(5.04369879534293,11.0048886256606,28.3225293158624));
#111890=CARTESIAN_POINT('Ctrl Pts',(5.17632882931575,10.9679072750501,27.8252649356805));
#111891=CARTESIAN_POINT('Ctrl Pts',(5.97542374450792,10.9071832799328,27.3688243783781));
#111892=CARTESIAN_POINT('Ctrl Pts',(6.93510468754786,10.8359553464126,27.8630092146581));
#111893=CARTESIAN_POINT('Ctrl Pts',(7.04365340207539,10.7647274128925,28.9369977474397));
#111894=CARTESIAN_POINT('Ctrl Pts',(6.20226086341658,10.6934994793723,29.6132228219541));
#111895=CARTESIAN_POINT('Ctrl Pts',(5.25875722564617,10.6279661189962,29.30313503794));
#111896=CARTESIAN_POINT('Ctrl Pts',(5.04399359479906,10.5861754031269,28.7405886865493));
#111897=CARTESIAN_POINT('Ctrl Pts',(5.04180976972011,10.5681273317644,28.4991376522761));
#111898=CARTESIAN_POINT('Origin',(6.,5.85,28.5));
#111899=CARTESIAN_POINT('',(4.78808807722243,5.85,28.4134292692097));
#111900=CARTESIAN_POINT('Ctrl Pts',(6.39766230306601,5.85,29.3734910038904));
#111901=CARTESIAN_POINT('Ctrl Pts',(6.37560479125928,5.85,29.3873944122752));
#111902=CARTESIAN_POINT('Ctrl Pts',(6.35299337898576,5.85,29.4003106730031));
#111903=CARTESIAN_POINT('Ctrl Pts',(6.32987567746936,5.85,29.41218723318));
#111904=CARTESIAN_POINT('Ctrl Pts',(6.29181373748265,5.85,29.4317412931018));
#111905=CARTESIAN_POINT('Ctrl Pts',(6.25238143582705,5.85,29.4484799626506));
#111906=CARTESIAN_POINT('Ctrl Pts',(6.21188608599289,5.85,29.4624912035614));
#111907=CARTESIAN_POINT('Ctrl Pts',(6.1972630931679,5.85,29.4675507048657));
#111908=CARTESIAN_POINT('Ctrl Pts',(6.18250111093423,5.85,29.4722541335282));
#111909=CARTESIAN_POINT('Ctrl Pts',(6.16761349718974,5.85,29.4766041506807));
#111910=CARTESIAN_POINT('Ctrl Pts',(6.1588421883919,5.85,29.4791670425165));
#111911=CARTESIAN_POINT('Ctrl Pts',(6.15002899407694,5.85,29.481606645163));
#111912=CARTESIAN_POINT('Ctrl Pts',(6.14118581535311,5.85,29.4839213855223));
#111913=CARTESIAN_POINT('Ctrl Pts',(6.09925348827685,5.85,29.4948973538789));
#111914=CARTESIAN_POINT('Ctrl Pts',(6.05659373646623,5.85,29.5030859829525));
#111915=CARTESIAN_POINT('Ctrl Pts',(6.01351014174746,5.85,29.5085736858683));
#111916=CARTESIAN_POINT('Ctrl Pts',(5.98459026202491,5.85,29.5122573085862));
#111917=CARTESIAN_POINT('Ctrl Pts',(5.95547858940136,5.85,29.5147230779385));
#111918=CARTESIAN_POINT('Ctrl Pts',(5.92626036763772,5.85,29.5159859100061));
#111919=CARTESIAN_POINT('Ctrl Pts',(5.91602556356871,5.85,29.5164282654269));
#111920=CARTESIAN_POINT('Ctrl Pts',(5.90577765162887,5.85,29.5167229354698));
#111921=CARTESIAN_POINT('Ctrl Pts',(5.89552020384814,5.85,29.5168702916139));
#111922=CARTESIAN_POINT('Ctrl Pts',(5.88632379011673,5.85,29.517002405186));
#111923=CARTESIAN_POINT('Ctrl Pts',(5.87712958144482,5.85,29.5170159601235));
#111924=CARTESIAN_POINT('Ctrl Pts',(5.86794035624245,5.85,29.5169118945272));
#111925=CARTESIAN_POINT('Ctrl Pts',(5.82159506309469,5.85,29.5163870460814));
#111926=CARTESIAN_POINT('Ctrl Pts',(5.77537862895158,5.85,29.5128744891163));
#111927=CARTESIAN_POINT('Ctrl Pts',(5.72962637037788,5.85,29.506463984083));
#111928=CARTESIAN_POINT('Ctrl Pts',(5.68423642305929,5.85,29.5001042437157));
#111929=CARTESIAN_POINT('Ctrl Pts',(5.63930198692769,5.85,29.4908923183959));
#111930=CARTESIAN_POINT('Ctrl Pts',(5.5951346086702,5.85,29.4788648298534));
#111931=CARTESIAN_POINT('Ctrl Pts',(5.57278650518548,5.85,29.4727790812939));
#111932=CARTESIAN_POINT('Ctrl Pts',(5.55063465678426,5.85,29.4659716680212));
#111933=CARTESIAN_POINT('Ctrl Pts',(5.52871953745136,5.85,29.4584422336643));
#111934=CARTESIAN_POINT('Ctrl Pts',(5.51918689020667,5.85,29.4551670773402));
#111935=CARTESIAN_POINT('Ctrl Pts',(5.50969904152047,5.85,29.4517552645103));
#111936=CARTESIAN_POINT('Ctrl Pts',(5.50025937223982,5.85,29.4482065595265));
#111937=CARTESIAN_POINT('Ctrl Pts',(5.4913953109182,5.85,29.4448742458985));
#111938=CARTESIAN_POINT('Ctrl Pts',(5.48258062850377,5.85,29.4414237433841));
#111939=CARTESIAN_POINT('Ctrl Pts',(5.47382484858967,5.85,29.4378583479916));
#111940=CARTESIAN_POINT('Ctrl Pts',(5.43006407079472,5.85,29.4200387503027));
#111941=CARTESIAN_POINT('Ctrl Pts',(5.38772146838542,5.85,29.3993333169208));
#111942=CARTESIAN_POINT('Ctrl Pts',(5.34712310967584,5.85,29.3758018262265));
#111943=CARTESIAN_POINT('Ctrl Pts',(5.34483356399201,5.85,29.3744747670876));
#111944=CARTESIAN_POINT('Ctrl Pts',(5.3425495652097,5.85,29.3731387061964));
#111945=CARTESIAN_POINT('Ctrl Pts',(5.34027117186927,5.85,29.3717936493299));
#111946=CARTESIAN_POINT('Ctrl Pts',(5.30129849569172,5.85,29.3487860040878));
#111947=CARTESIAN_POINT('Ctrl Pts',(5.26396449537708,5.85,29.3231503642922));
#111948=CARTESIAN_POINT('Ctrl Pts',(5.22835390321961,5.85,29.2951545084538));
#111949=CARTESIAN_POINT('Ctrl Pts',(5.21129296197096,5.85,29.281741767392));
#111950=CARTESIAN_POINT('Ctrl Pts',(5.19462785867648,5.85,29.2677865410265));
#111951=CARTESIAN_POINT('Ctrl Pts',(5.17836963742877,5.85,29.2533145725815));
#111952=CARTESIAN_POINT('Ctrl Pts',(5.16945924558658,5.85,29.2453831446837));
#111953=CARTESIAN_POINT('Ctrl Pts',(5.1606710885947,5.85,29.2372964671565));
#111954=CARTESIAN_POINT('Ctrl Pts',(5.15200716210713,5.85,29.2290585117669));
#111955=CARTESIAN_POINT('Ctrl Pts',(5.14507713634318,5.85,29.2224692080402));
#111956=CARTESIAN_POINT('Ctrl Pts',(5.13822590803877,5.85,29.2157822542096));
#111957=CARTESIAN_POINT('Ctrl Pts',(5.13146656977552,5.85,29.2090121450337));
#111958=CARTESIAN_POINT('Ctrl Pts',(5.0979881630321,5.85,29.1754803909094));
#111959=CARTESIAN_POINT('Ctrl Pts',(5.06669143674257,5.85,29.1398468622296));
#111960=CARTESIAN_POINT('Ctrl Pts',(5.03765905964773,5.85,29.1024199304065));
#111961=CARTESIAN_POINT('Ctrl Pts',(5.00796455502298,5.85,29.0641394204614));
#111962=CARTESIAN_POINT('Ctrl Pts',(4.98063808722797,5.85,29.0239820965496));
#111963=CARTESIAN_POINT('Ctrl Pts',(4.9557940804241,5.85,28.9822296267095));
#111964=CARTESIAN_POINT('Ctrl Pts',(4.94304363266272,5.85,28.960801413064));
#111965=CARTESIAN_POINT('Ctrl Pts',(4.93094754092183,5.85,28.9389523366623));
#111966=CARTESIAN_POINT('Ctrl Pts',(4.91952488154216,5.85,28.9167166416882));
#111967=CARTESIAN_POINT('Ctrl Pts',(4.91126860137239,5.85,28.9006447164584));
#111968=CARTESIAN_POINT('Ctrl Pts',(4.90336419933965,5.85,28.8843707542884));
#111969=CARTESIAN_POINT('Ctrl Pts',(4.89581982809443,5.85,28.8679070326234));
#111970=CARTESIAN_POINT('Ctrl Pts',(4.89200657492442,5.85,28.8595855520403));
#111971=CARTESIAN_POINT('Ctrl Pts',(4.88828572317409,5.85,28.8512162354605));
#111972=CARTESIAN_POINT('Ctrl Pts',(4.88466340885467,5.85,28.8428131220479));
#111973=CARTESIAN_POINT('Ctrl Pts',(4.86467997843789,5.85,28.7964551814171));
#111974=CARTESIAN_POINT('Ctrl Pts',(4.84764801395987,5.85,28.7489758153047));
#111975=CARTESIAN_POINT('Ctrl Pts',(4.83367739160128,5.85,28.7006828495529));
#111976=CARTESIAN_POINT('Ctrl Pts',(4.81980755282921,5.85,28.6527382675857));
#111977=CARTESIAN_POINT('Ctrl Pts',(4.80895438505048,5.85,28.603990769008));
#111978=CARTESIAN_POINT('Ctrl Pts',(4.80126408485538,5.85,28.554709425276));
#111979=CARTESIAN_POINT('Ctrl Pts',(4.79397897921633,5.85,28.5080246683726));
#111980=CARTESIAN_POINT('Ctrl Pts',(4.78953199468363,5.85,28.4608598822724));
#111981=CARTESIAN_POINT('Ctrl Pts',(4.78808807722243,5.85,28.4134292692097));
#111982=CARTESIAN_POINT('',(4.785,5.85,28.5));
#111983=CARTESIAN_POINT('Origin',(6.,5.85,28.5));
#111984=CARTESIAN_POINT('',(5.31875076891147,5.85,27.492807053794));
#111985=CARTESIAN_POINT('Origin',(6.,5.85,28.5));
#111986=CARTESIAN_POINT('Ctrl Pts',(5.31842995130037,5.85,27.4918752544675));
#111987=CARTESIAN_POINT('Ctrl Pts',(5.34708224593995,5.85,27.4762949324899));
#111988=CARTESIAN_POINT('Ctrl Pts',(5.37635092494107,5.85,27.461973165142));
#111989=CARTESIAN_POINT('Ctrl Pts',(5.40619692851071,5.85,27.4489852785675));
#111990=CARTESIAN_POINT('Ctrl Pts',(5.44976279004565,5.85,27.4300270127878));
#111991=CARTESIAN_POINT('Ctrl Pts',(5.49455904383828,5.85,27.4139090963492));
#111992=CARTESIAN_POINT('Ctrl Pts',(5.54030432571948,5.85,27.4006115881595));
#111993=CARTESIAN_POINT('Ctrl Pts',(5.55672681328631,5.85,27.3958378026688));
#111994=CARTESIAN_POINT('Ctrl Pts',(5.57327162018282,5.85,27.3914278984493));
#111995=CARTESIAN_POINT('Ctrl Pts',(5.58992562620212,5.85,27.3873822307481));
#111996=CARTESIAN_POINT('Ctrl Pts',(5.60099327874898,5.85,27.384693625713));
#111997=CARTESIAN_POINT('Ctrl Pts',(5.61211166023121,5.85,27.3821653739662));
#111998=CARTESIAN_POINT('Ctrl Pts',(5.62326865569075,5.85,27.3797994609335));
#111999=CARTESIAN_POINT('Ctrl Pts',(5.67204924285268,5.85,27.369455221991));
#112000=CARTESIAN_POINT('Ctrl Pts',(5.72146861995573,5.85,27.362229542462));
#112001=CARTESIAN_POINT('Ctrl Pts',(5.7711989464513,5.85,27.3580931321149));
#112002=CARTESIAN_POINT('Ctrl Pts',(5.80313722508088,5.85,27.3554366077061));
#112003=CARTESIAN_POINT('Ctrl Pts',(5.8352038278478,5.85,27.3540553674492));
#112004=CARTESIAN_POINT('Ctrl Pts',(5.86730952534731,5.85,27.3539527284191));
#112005=CARTESIAN_POINT('Ctrl Pts',(5.88111738432143,5.85,27.3539085859347));
#112006=CARTESIAN_POINT('Ctrl Pts',(5.8949324342615,5.85,27.3541010447302));
#112007=CARTESIAN_POINT('Ctrl Pts',(5.9087473532397,5.85,27.354530837349));
#112008=CARTESIAN_POINT('Ctrl Pts',(5.92273505299603,5.85,27.354966005309));
#112009=CARTESIAN_POINT('Ctrl Pts',(5.93672831021879,5.85,27.3556450340852));
#112010=CARTESIAN_POINT('Ctrl Pts',(5.95068702636896,5.85,27.3565663028577));
#112011=CARTESIAN_POINT('Ctrl Pts',(5.99984799299835,5.85,27.3598109037862));
#112012=CARTESIAN_POINT('Ctrl Pts',(6.04864581675033,5.85,27.3660555953942));
#112013=CARTESIAN_POINT('Ctrl Pts',(6.09676290916412,5.85,27.375282453497));
#112014=CARTESIAN_POINT('Ctrl Pts',(6.1428988501221,5.85,27.3841294091069));
#112015=CARTESIAN_POINT('Ctrl Pts',(6.18840989818999,5.85,27.3957185910204));
#112016=CARTESIAN_POINT('Ctrl Pts',(6.23299382807648,5.85,27.4100776452759));
#112017=CARTESIAN_POINT('Ctrl Pts',(6.2567216722242,5.85,27.4177196230546));
#112018=CARTESIAN_POINT('Ctrl Pts',(6.28018645016525,5.85,27.4261468450586));
#112019=CARTESIAN_POINT('Ctrl Pts',(6.30333855317582,5.85,27.4353680192718));
#112020=CARTESIAN_POINT('Ctrl Pts',(6.31558983623641,5.85,27.4402475421119));
#112021=CARTESIAN_POINT('Ctrl Pts',(6.32775351143813,5.85,27.4453494353354));
#112022=CARTESIAN_POINT('Ctrl Pts',(6.33982182839314,5.85,27.4506753268719));
#112023=CARTESIAN_POINT('Ctrl Pts',(6.34965281523833,5.85,27.4550138580714));
#112024=CARTESIAN_POINT('Ctrl Pts',(6.35942225137347,5.85,27.4595020494353));
#112025=CARTESIAN_POINT('Ctrl Pts',(6.36910587695464,5.85,27.4641308184335));
#112026=CARTESIAN_POINT('Ctrl Pts',(6.41003918384822,5.85,27.4836969220953));
#112027=CARTESIAN_POINT('Ctrl Pts',(6.44952349193045,5.85,27.5058062551903));
#112028=CARTESIAN_POINT('Ctrl Pts',(6.48728357592312,5.85,27.5304740913914));
#112029=CARTESIAN_POINT('Ctrl Pts',(6.49179366527091,5.85,27.5334204340242));
#112030=CARTESIAN_POINT('Ctrl Pts',(6.49627911696747,5.85,27.5364033231456));
#112031=CARTESIAN_POINT('Ctrl Pts',(6.50073942778498,5.85,27.5394228222158));
#112032=CARTESIAN_POINT('Ctrl Pts',(6.53921831223448,5.85,27.5654718938107));
#112033=CARTESIAN_POINT('Ctrl Pts',(6.57582986883405,5.85,27.5942433472433));
#112034=CARTESIAN_POINT('Ctrl Pts',(6.61041251906095,5.85,27.6254667472186));
#112035=CARTESIAN_POINT('Ctrl Pts',(6.62591613035989,5.85,27.6394643863086));
#112036=CARTESIAN_POINT('Ctrl Pts',(6.64101135713831,5.85,27.6539551741822));
#112037=CARTESIAN_POINT('Ctrl Pts',(6.65568044111702,5.85,27.6689160312498));
#112038=CARTESIAN_POINT('Ctrl Pts',(6.66377388965348,5.85,27.677170461241));
#112039=CARTESIAN_POINT('Ctrl Pts',(6.67173757874651,5.85,27.6855679955746));
#112040=CARTESIAN_POINT('Ctrl Pts',(6.67956824603633,5.85,27.6941048065658));
#112041=CARTESIAN_POINT('Ctrl Pts',(6.68537015773566,5.85,27.700429915491));
#112042=CARTESIAN_POINT('Ctrl Pts',(6.69109781697112,5.85,27.7068302913327));
#112043=CARTESIAN_POINT('Ctrl Pts',(6.69674235679888,5.85,27.7132951997147));
#112044=CARTESIAN_POINT('Ctrl Pts',(6.72642364311295,5.85,27.7472903175694));
#112045=CARTESIAN_POINT('Ctrl Pts',(6.75387231476421,5.85,27.7831346316721));
#112046=CARTESIAN_POINT('Ctrl Pts',(6.77895793001658,5.85,27.8205659891986));
#112047=CARTESIAN_POINT('Ctrl Pts',(6.80387458551433,5.85,27.8577452343922));
#112048=CARTESIAN_POINT('Ctrl Pts',(6.82646026031466,5.85,27.8964914210295));
#112049=CARTESIAN_POINT('Ctrl Pts',(6.84653849813131,5.85,27.9365623451875));
#112050=CARTESIAN_POINT('Ctrl Pts',(6.85571490799722,5.85,27.9548760651034));
#112051=CARTESIAN_POINT('Ctrl Pts',(6.86436686272691,5.85,27.9734665875714));
#112052=CARTESIAN_POINT('Ctrl Pts',(6.87247380103991,5.85,27.992310794561));
#112053=CARTESIAN_POINT('Ctrl Pts',(6.87709299377136,5.85,28.0030478966082));
#112054=CARTESIAN_POINT('Ctrl Pts',(6.88153520171541,5.85,28.01386735387));
#112055=CARTESIAN_POINT('Ctrl Pts',(6.88579626268239,5.85,28.0247648298098));
#112056=CARTESIAN_POINT('Ctrl Pts',(6.8895914343642,5.85,28.0344708144015));
#112057=CARTESIAN_POINT('Ctrl Pts',(6.89324350585179,5.85,28.0442408696217));
#112058=CARTESIAN_POINT('Ctrl Pts',(6.89674209830408,5.85,28.0540500724342));
#112059=CARTESIAN_POINT('Ctrl Pts',(6.91122096775626,5.85,28.094645302913));
#112060=CARTESIAN_POINT('Ctrl Pts',(6.92310787725967,5.85,28.1359903692491));
#112061=CARTESIAN_POINT('Ctrl Pts',(6.93225669319789,5.85,28.1778617780855));
#112062=CARTESIAN_POINT('Ctrl Pts',(6.94107840482362,5.85,28.218236127795));
#112063=CARTESIAN_POINT('Ctrl Pts',(6.9473542837777,5.85,28.25910076306));
#112064=CARTESIAN_POINT('Ctrl Pts',(6.95090629581674,5.85,28.3002511157192));
#112065=CARTESIAN_POINT('Ctrl Pts',(6.95399736759412,5.85,28.3360614374006));
#112066=CARTESIAN_POINT('Ctrl Pts',(6.95502502661388,5.85,28.3720884051317));
#112067=CARTESIAN_POINT('Ctrl Pts',(6.95384139680377,5.85,28.4081868623593));
#112068=CARTESIAN_POINT('Ctrl Pts',(5.58122226519601,11.5482346816144,29.361898063191));
#112069=CARTESIAN_POINT('Ctrl Pts',(5.29549456253745,11.5244920371077,29.2230691167062));
#112070=CARTESIAN_POINT('Ctrl Pts',(4.87780360901464,11.4770067480943,28.6413286057481));
#112071=CARTESIAN_POINT('Ctrl Pts',(5.27059993461702,11.4057788145741,27.6341247030305));
#112072=CARTESIAN_POINT('Ctrl Pts',(6.32832772845592,11.3345508810539,27.417533671549));
#112073=CARTESIAN_POINT('Ctrl Pts',(7.08668716007769,11.2633229475337,28.1849858242981));
#112074=CARTESIAN_POINT('Ctrl Pts',(6.85620622293074,11.1920950140135,29.2397882902982));
#112075=CARTESIAN_POINT('Ctrl Pts',(5.84626444085431,11.1208670804934,29.6209123918368));
#112076=CARTESIAN_POINT('Ctrl Pts',(4.97632415185831,11.0496391469732,28.9819400693107));
#112077=CARTESIAN_POINT('Ctrl Pts',(5.03810268409804,10.978411213453,27.9042192846039));
#112078=CARTESIAN_POINT('Ctrl Pts',(5.97542374450792,10.9071832799328,27.3688243783781));
#112079=CARTESIAN_POINT('Ctrl Pts',(6.93510468754786,10.8359553464126,27.8630092146581));
#112080=CARTESIAN_POINT('Ctrl Pts',(7.04365340207539,10.7647274128925,28.9369977474397));
#112081=CARTESIAN_POINT('Ctrl Pts',(6.20226086341658,10.6934994793723,29.6132228219541));
#112082=CARTESIAN_POINT('Ctrl Pts',(5.17677073134417,10.6222715458521,29.2761897148703));
#112083=CARTESIAN_POINT('Ctrl Pts',(4.90058748232414,10.5510436123319,28.2326631663733));
#112084=CARTESIAN_POINT('Ctrl Pts',(5.62509554533696,10.4798156788117,27.4324687801292));
#112085=CARTESIAN_POINT('Ctrl Pts',(6.69084341099689,10.4085877452916,27.6039464366949));
#112086=CARTESIAN_POINT('Ctrl Pts',(7.12778211347718,10.3373598117714,28.5910168988298));
#112087=CARTESIAN_POINT('Ctrl Pts',(6.53820764542198,10.2661318782512,29.4952432009378));
#112088=CARTESIAN_POINT('Ctrl Pts',(5.45875381291119,10.194903944731,29.4935940386394));
#112089=CARTESIAN_POINT('Ctrl Pts',(4.87194505274743,10.1236760112108,28.5875704048551));
#112090=CARTESIAN_POINT('Ctrl Pts',(5.31189775796595,10.0524480776906,27.6018397492193));
#112091=CARTESIAN_POINT('Ctrl Pts',(6.37816468677541,9.98122014417046,27.4336192011314));
#112092=CARTESIAN_POINT('Ctrl Pts',(7.10022415948525,9.90999221065029,28.2360239865173));
#112093=CARTESIAN_POINT('Ctrl Pts',(6.82085389946722,9.83876427713011,29.2787011054732));
#112094=CARTESIAN_POINT('Ctrl Pts',(5.79433816650613,9.76753634360992,29.6126004436091));
#112095=CARTESIAN_POINT('Ctrl Pts',(4.95501690001259,9.69630841008975,28.9338050913953));
#112096=CARTESIAN_POINT('Ctrl Pts',(5.06684466687464,9.62508047656957,27.8601580970606));
#112097=CARTESIAN_POINT('Ctrl Pts',(6.02803525397329,9.55385254304938,27.3688985186306));
#112098=CARTESIAN_POINT('Ctrl Pts',(6.96370800764262,9.48262460952921,27.9071733705549));
#112099=CARTESIAN_POINT('Ctrl Pts',(7.0222087383162,9.41139667600901,28.9850420928927));
#112100=CARTESIAN_POINT('Ctrl Pts',(6.1502897777778,9.34016874248886,29.6214229885637));
#112101=CARTESIAN_POINT('Ctrl Pts',(5.14157628262408,9.26894080896865,29.2370788682514));
#112102=CARTESIAN_POINT('Ctrl Pts',(4.91420450381539,9.19771287544849,28.1818417421448));
#112103=CARTESIAN_POINT('Ctrl Pts',(5.6751294127762,9.1264849419283,27.416193911193));
#112104=CARTESIAN_POINT('Ctrl Pts',(6.73175321387293,9.05525700840812,27.6370319991079));
#112105=CARTESIAN_POINT('Ctrl Pts',(7.1223314473857,8.98402907488794,28.6433480337722));
#112106=CARTESIAN_POINT('Ctrl Pts',(6.49135778099696,8.91280114136776,29.5191879451952));
#112107=CARTESIAN_POINT('Ctrl Pts',(5.41314771587932,8.84157320784758,29.4673577069521));
#112108=CARTESIAN_POINT('Ctrl Pts',(4.86909364113474,8.7703452743274,28.5350334705028));
#112109=CARTESIAN_POINT('Ctrl Pts',(5.35439639516002,8.69911734080722,27.5708215876404));
#112110=CARTESIAN_POINT('Ctrl Pts',(6.42733089615622,8.62788940728704,27.4523527111821));
#112111=CARTESIAN_POINT('Ctrl Pts',(7.1113066008254,8.55666147376686,28.2874578264456));
#112112=CARTESIAN_POINT('Ctrl Pts',(6.78376527806854,8.48543354024668,29.3160199295799));
#112113=CARTESIAN_POINT('Ctrl Pts',(5.7428367373441,8.41420560672649,29.601836463781));
#112114=CARTESIAN_POINT('Ctrl Pts',(4.93597953103987,8.34297767320632,28.8847557383731));
#112115=CARTESIAN_POINT('Ctrl Pts',(5.09759926987673,8.27174973968613,27.817468345898));
#112116=CARTESIAN_POINT('Ctrl Pts',(6.08058882997138,8.20052180616596,27.3714248022129));
#112117=CARTESIAN_POINT('Ctrl Pts',(6.99022601937189,8.12929387264577,27.9526162524013));
#112118=CARTESIAN_POINT('Ctrl Pts',(6.99855435409013,8.0580659391256,29.032039226478));
#112119=CARTESIAN_POINT('Ctrl Pts',(6.09799334069262,7.98683800560541,29.62719733931));
#112120=CARTESIAN_POINT('Ctrl Pts',(5.10823828075997,7.91561007208523,29.1963745922073));
#112121=CARTESIAN_POINT('Ctrl Pts',(4.93016935921317,7.84438213856506,28.1317080822838));
#112122=CARTESIAN_POINT('Ctrl Pts',(5.72586583137092,7.77315420504486,27.4022627845939));
#112123=CARTESIAN_POINT('Ctrl Pts',(6.7710806444101,7.7019262715247,27.6719835892955));
#112124=CARTESIAN_POINT('Ctrl Pts',(7.11445385898466,7.6306983380045,28.6953692224212));
#112125=CARTESIAN_POINT('Ctrl Pts',(6.44344539503938,7.55947040448434,29.5409287764079));
#112126=CARTESIAN_POINT('Ctrl Pts',(5.36881063516189,7.48824247096415,29.4390295642441));
#112127=CARTESIAN_POINT('Ctrl Pts',(4.86868770476157,7.41701453744397,28.4824207747026));
#112128=CARTESIAN_POINT('Ctrl Pts',(5.39829109152546,7.34578660392379,27.5418126900042));
#112129=CARTESIAN_POINT('Ctrl Pts',(6.47557303929329,7.27455867040361,27.4733516550811));
#112130=CARTESIAN_POINT('Ctrl Pts',(7.1199859534311,7.20333073688343,28.3393512752155));
#112131=CARTESIAN_POINT('Ctrl Pts',(6.7449818262241,7.13210280336324,29.351574175982));
#112132=CARTESIAN_POINT('Ctrl Pts',(5.69189142314743,7.06087486984307,29.5886898898316));
#112133=CARTESIAN_POINT('Ctrl Pts',(4.91924295928752,6.98964693632289,28.8348743432691));
#112134=CARTESIAN_POINT('Ctrl Pts',(5.13030531893757,6.91841900280271,27.7762545908562));
#112135=CARTESIAN_POINT('Ctrl Pts',(6.13296796501039,6.84719106928253,27.3763913550898));
#112136=CARTESIAN_POINT('Ctrl Pts',(7.01460310250063,6.77596313576235,27.9992431262198));
#112137=CARTESIAN_POINT('Ctrl Pts',(6.97274002584404,6.70473520224217,29.0778852397409));
#112138=CARTESIAN_POINT('Ctrl Pts',(6.04548629726899,6.63350726872199,29.6305354712223));
#112139=CARTESIAN_POINT('Ctrl Pts',(5.07682610678296,6.56227933520181,29.1541620595593));
#112140=CARTESIAN_POINT('Ctrl Pts',(4.94845253496139,6.49105140168163,28.0823755178912));
#112141=CARTESIAN_POINT('Ctrl Pts',(5.77718546973152,6.41982346816144,27.3906962578813));
#112142=CARTESIAN_POINT('Ctrl Pts',(6.80875932531787,6.34859553464126,27.7087435142843));
#112143=CARTESIAN_POINT('Ctrl Pts',(7.10413006383205,6.27736760112109,28.7469332186266));
#112144=CARTESIAN_POINT('Ctrl Pts',(6.39464482398617,6.2061396676009,29.5604863382188));
#112145=CARTESIAN_POINT('Ctrl Pts',(5.32570060970894,6.13491173408073,29.4085390729209));
#112146=CARTESIAN_POINT('Ctrl Pts',(4.87099739489662,6.06368380056054,28.4301031676476));
#112147=CARTESIAN_POINT('Ctrl Pts',(5.44295412205162,5.99245586704036,27.5143710763459));
#112148=CARTESIAN_POINT('Ctrl Pts',(6.52391074184675,5.92122793352018,27.4975948676703));
#112149=CARTESIAN_POINT('Ctrl Pts',(6.92340443678229,5.87374264450673,28.0919790384314));
#112150=CARTESIAN_POINT('Ctrl Pts',(6.95384139680377,5.85,28.4081868623593));
#112151=CARTESIAN_POINT('Ctrl Pts',(5.54382034036397,11.4988231210763,29.4388760013506));
#112152=CARTESIAN_POINT('Ctrl Pts',(5.23257369252493,11.4750804765696,29.2876479481574));
#112153=CARTESIAN_POINT('Ctrl Pts',(4.77757787690384,11.4275951875561,28.6539509623099));
#112154=CARTESIAN_POINT('Ctrl Pts',(5.20545567275527,11.3563672540359,27.5567915497139));
#112155=CARTESIAN_POINT('Ctrl Pts',(6.35765137200092,11.2851393205157,27.3208563153164));
#112156=CARTESIAN_POINT('Ctrl Pts',(7.18374148770617,11.2139113869956,28.1568512422956));
#112157=CARTESIAN_POINT('Ctrl Pts',(6.93267581080359,11.1426834534754,29.3058603464889));
#112158=CARTESIAN_POINT('Ctrl Pts',(5.83253399305515,11.0714555199552,29.7210234472691));
#112159=CARTESIAN_POINT('Ctrl Pts',(4.88489749771086,11.000227586435,29.0249831557688));
#112160=CARTESIAN_POINT('Ctrl Pts',(4.95219360127073,10.9289996529149,27.8510088493737));
#112161=CARTESIAN_POINT('Ctrl Pts',(5.97322878717331,10.8577717193947,27.2677966921962));
#112162=CARTESIAN_POINT('Ctrl Pts',(7.01862086409466,10.7865437858745,27.806118220959));
#112163=CARTESIAN_POINT('Ctrl Pts',(7.13686429379914,10.7153158523543,28.9760269401191));
#112164=CARTESIAN_POINT('Ctrl Pts',(6.22032520872738,10.6440879188341,29.7126471056437));
#112165=CARTESIAN_POINT('Ctrl Pts',(5.1032463849741,10.5728599853139,29.3455128592456));
#112166=CARTESIAN_POINT('Ctrl Pts',(4.80239662610593,10.5016320517938,28.2087867485862));
#112167=CARTESIAN_POINT('Ctrl Pts',(5.59161203590667,10.4304041182736,27.3371253100181));
#112168=CARTESIAN_POINT('Ctrl Pts',(6.7525440965429,10.3591761847534,27.5239179986121));
#112169=CARTESIAN_POINT('Ctrl Pts',(7.22850671827248,10.2879482512332,28.5991458104828));
#112170=CARTESIAN_POINT('Ctrl Pts',(6.58627610805773,10.216720317713,29.5841304752541));
#112171=CARTESIAN_POINT('Ctrl Pts',(5.41041397169542,10.1454923841929,29.5823340227843));
#112172=CARTESIAN_POINT('Ctrl Pts',(4.77119608059086,10.0742644506727,28.595391502845));
#112173=CARTESIAN_POINT('Ctrl Pts',(5.25044189201508,10.0030365171525,27.5216231584244));
#112174=CARTESIAN_POINT('Ctrl Pts',(6.4119393744281,9.93180858363231,27.338378477552));
#112175=CARTESIAN_POINT('Ctrl Pts',(7.19848750514933,9.86058065011214,28.2124477306823));
#112176=CARTESIAN_POINT('Ctrl Pts',(6.89416609659331,9.78935271659197,29.3482485474525));
#112177=CARTESIAN_POINT('Ctrl Pts',(5.77597007336775,9.71812478307177,29.711969141373));
#112178=CARTESIAN_POINT('Ctrl Pts',(4.86168725015721,9.64689684955161,28.9725491412138));
#112179=CARTESIAN_POINT('Ctrl Pts',(4.98350259129244,9.57566891603142,27.8030124640213));
#112180=CARTESIAN_POINT('Ctrl Pts',(6.03053914177487,9.50444098251124,27.2678774540714));
#112181=CARTESIAN_POINT('Ctrl Pts',(7.04977880717729,9.43321304899106,27.8542267709862));
#112182=CARTESIAN_POINT('Ctrl Pts',(7.11350436178351,9.36198511547088,29.028362227635));
#112183=CARTESIAN_POINT('Ctrl Pts',(6.1637124755583,9.2907571819507,29.7215796464692));
#112184=CARTESIAN_POINT('Ctrl Pts',(5.06490864563433,9.21952924843051,29.3029089402312));
#112185=CARTESIAN_POINT('Ctrl Pts',(4.81722981257427,9.14830131491035,28.1534263555184));
#112186=CARTESIAN_POINT('Ctrl Pts',(5.64611453382333,9.07707338139014,27.3193968981306));
#112187=CARTESIAN_POINT('Ctrl Pts',(6.79710764040111,9.00584544786999,27.5599585025503));
#112188=CARTESIAN_POINT('Ctrl Pts',(7.22256924166911,8.93461751434979,28.65615074972));
#112189=CARTESIAN_POINT('Ctrl Pts',(6.53524198319577,8.86338958082962,29.6102137752426));
#112190=CARTESIAN_POINT('Ctrl Pts',(5.36073469772192,8.79216164730942,29.5537544688479));
#112191=CARTESIAN_POINT('Ctrl Pts',(4.76809000337889,8.72093371378926,28.5381623838175));
#112192=CARTESIAN_POINT('Ctrl Pts',(5.29673617234319,8.64970578026907,27.4878346992595));
#112193=CARTESIAN_POINT('Ctrl Pts',(6.46549672191084,8.57847784674889,27.3587851169898));
#112194=CARTESIAN_POINT('Ctrl Pts',(7.21055974275493,8.50724991322871,28.2684752355907));
#112195=CARTESIAN_POINT('Ctrl Pts',(6.85376501200857,8.43602197970853,29.3889003946359));
#112196=CARTESIAN_POINT('Ctrl Pts',(5.71986894268827,8.36479404618835,29.7002438077503));
#112197=CARTESIAN_POINT('Ctrl Pts',(4.84094961351468,8.29356611266817,28.9191190867781));
#112198=CARTESIAN_POINT('Ctrl Pts',(5.01700395290686,8.22233817914799,27.7565100009321));
#112199=CARTESIAN_POINT('Ctrl Pts',(6.0877863887487,8.15111024562781,27.2706293653813));
#112200=CARTESIAN_POINT('Ctrl Pts',(7.07866519859573,8.07988231210763,27.9037282526809));
#112201=CARTESIAN_POINT('Ctrl Pts',(7.08773735449456,8.00865437858745,29.0795567745772));
#112202=CARTESIAN_POINT('Ctrl Pts',(6.10674533311731,7.93742644506727,29.7278697166882));
#112203=CARTESIAN_POINT('Ctrl Pts',(5.02859315634396,7.86619851154709,29.2585692792406));
#112204=CARTESIAN_POINT('Ctrl Pts',(4.83462052295889,7.79497057802691,28.0988151525079));
#112205=CARTESIAN_POINT('Ctrl Pts',(5.70138232922444,7.72374264450673,27.3042215531631));
#112206=CARTESIAN_POINT('Ctrl Pts',(6.83994748690155,7.65251471098655,27.5980316931486));
#112207=CARTESIAN_POINT('Ctrl Pts',(7.213988089194,7.58128677746637,28.7128180607051));
#112208=CARTESIAN_POINT('Ctrl Pts',(6.48305044075688,7.51005884394619,29.6338963260532));
#112209=CARTESIAN_POINT('Ctrl Pts',(5.31243777859274,7.438830910426,29.5228962798262));
#112210=CARTESIAN_POINT('Ctrl Pts',(4.76764781197003,7.36760297690583,28.4808507369271));
#112211=CARTESIAN_POINT('Ctrl Pts',(5.34455119683868,7.29637504338564,27.4562349556476));
#112212=CARTESIAN_POINT('Ctrl Pts',(6.51804747284004,7.22514710986547,27.3816595209623));
#112213=CARTESIAN_POINT('Ctrl Pts',(7.22001426669085,7.15391917634529,28.325003397978));
#112214=CARTESIAN_POINT('Ctrl Pts',(6.81151772808792,7.0826912428251,29.4276300659493));
#112215=CARTESIAN_POINT('Ctrl Pts',(5.66437359477736,7.01146330930493,29.6859230854884));
#112216=CARTESIAN_POINT('Ctrl Pts',(4.82271826315641,6.94023537578474,28.8647826788233));
#112217=CARTESIAN_POINT('Ctrl Pts',(5.05263104835308,6.86900744226457,27.7116153582976));
#112218=CARTESIAN_POINT('Ctrl Pts',(6.14484361507261,6.79777950874438,27.2760394915954));
#112219=CARTESIAN_POINT('Ctrl Pts',(7.10521945055422,6.7265515752242,27.9545194711739));
#112220=CARTESIAN_POINT('Ctrl Pts',(7.05961749401882,6.65532364170402,29.1294973922076));
#112221=CARTESIAN_POINT('Ctrl Pts',(6.04954877464054,6.58409570818384,29.7315059842186));
#112222=CARTESIAN_POINT('Ctrl Pts',(4.9943754947007,6.51286777466365,29.2125866560605));
#112223=CARTESIAN_POINT('Ctrl Pts',(4.85453660778559,6.44163984114349,28.0450765924954));
#112224=CARTESIAN_POINT('Ctrl Pts',(5.75728543298173,6.37041190762328,27.2916219954971));
#112225=CARTESIAN_POINT('Ctrl Pts',(6.88099133045757,6.29918397410313,27.6380747247521));
#112226=CARTESIAN_POINT('Ctrl Pts',(7.20274225407082,6.22795604058293,28.7689873464229));
#112227=CARTESIAN_POINT('Ctrl Pts',(6.42989138753377,6.15672810706276,29.6552006150559));
#112228=CARTESIAN_POINT('Ctrl Pts',(5.26547750562782,6.08550017354258,29.4896826182632));
#112229=CARTESIAN_POINT('Ctrl Pts',(4.77016378541396,6.01427224002239,28.4238605337815));
#112230=CARTESIAN_POINT('Ctrl Pts',(5.39320317704308,5.94304430650222,27.4263424734594));
#112231=CARTESIAN_POINT('Ctrl Pts',(6.57070231779914,5.87181637298204,27.4080679461204));
#112232=CARTESIAN_POINT('Ctrl Pts',(7.00587563919775,5.82433108396858,28.0555378237578));
#112233=CARTESIAN_POINT('Ctrl Pts',(7.03903098846544,5.80058843946186,28.3999868369348));
#112234=CARTESIAN_POINT('Ctrl Pts',(5.50641841553193,11.4494115605381,29.5158539395102));
#112235=CARTESIAN_POINT('Ctrl Pts',(5.1696528225124,11.4256689160314,29.3522267796086));
#112236=CARTESIAN_POINT('Ctrl Pts',(4.67735214479306,11.378183627018,28.6665733188716));
#112237=CARTESIAN_POINT('Ctrl Pts',(5.1403114108935,11.3069556934978,27.4794583963973));
#112238=CARTESIAN_POINT('Ctrl Pts',(6.38697501554594,11.2357277599776,27.2241789590838));
#112239=CARTESIAN_POINT('Ctrl Pts',(7.28079581533463,11.1644998264574,28.1287166602932));
#112240=CARTESIAN_POINT('Ctrl Pts',(7.00914539867645,11.0932718929372,29.3719324026795));
#112241=CARTESIAN_POINT('Ctrl Pts',(5.81880354525599,11.0220439594171,29.8211345027015));
#112242=CARTESIAN_POINT('Ctrl Pts',(4.79347084356342,10.9508160258969,29.0680262422269));
#112243=CARTESIAN_POINT('Ctrl Pts',(4.8662845184434,10.8795880923767,27.7977984141436));
#112244=CARTESIAN_POINT('Ctrl Pts',(5.97103382983874,10.8083601588565,27.1667690060142));
#112245=CARTESIAN_POINT('Ctrl Pts',(7.10213704064145,10.7371322253364,27.7492272272599));
#112246=CARTESIAN_POINT('Ctrl Pts',(7.2300751855229,10.6659042918162,29.0150561327986));
#112247=CARTESIAN_POINT('Ctrl Pts',(6.23838955403818,10.594676358296,29.8120713893333));
#112248=CARTESIAN_POINT('Ctrl Pts',(5.02972203860402,10.5234484247758,29.414836003621));
#112249=CARTESIAN_POINT('Ctrl Pts',(4.70420576988773,10.4522204912556,28.184910330799));
#112250=CARTESIAN_POINT('Ctrl Pts',(5.55812852647635,10.3809925577354,27.2417818399071));
#112251=CARTESIAN_POINT('Ctrl Pts',(6.81424478208894,10.3097646242153,27.4438895605293));
#112252=CARTESIAN_POINT('Ctrl Pts',(7.32923132306776,10.2385366906951,28.6072747221359));
#112253=CARTESIAN_POINT('Ctrl Pts',(6.63434457069349,10.1673087571749,29.6730177495704));
#112254=CARTESIAN_POINT('Ctrl Pts',(5.36207413047964,10.0960808236547,29.6710740069293));
#112255=CARTESIAN_POINT('Ctrl Pts',(4.6704471084343,10.0248528901345,28.6032126008349));
#112256=CARTESIAN_POINT('Ctrl Pts',(5.18898602606421,9.95362495661436,27.4414065676294));
#112257=CARTESIAN_POINT('Ctrl Pts',(6.44571406208079,9.88239702309417,27.2431377539727));
#112258=CARTESIAN_POINT('Ctrl Pts',(7.29675085081342,9.811169089574,28.1888714748473));
#112259=CARTESIAN_POINT('Ctrl Pts',(6.9674782937194,9.73994115605381,29.4177959894319));
#112260=CARTESIAN_POINT('Ctrl Pts',(5.75760198022939,9.66871322253364,29.8113378391368));
#112261=CARTESIAN_POINT('Ctrl Pts',(4.76835760030182,9.59748528901345,29.0112931910323));
#112262=CARTESIAN_POINT('Ctrl Pts',(4.90016051571024,9.52625735549328,27.745866830982));
#112263=CARTESIAN_POINT('Ctrl Pts',(6.03304302957645,9.45502942197309,27.1668563895122));
#112264=CARTESIAN_POINT('Ctrl Pts',(7.13584960671193,9.38380148845291,27.8012801714175));
#112265=CARTESIAN_POINT('Ctrl Pts',(7.20479998525085,9.31257355493274,29.0716823623772));
#112266=CARTESIAN_POINT('Ctrl Pts',(6.17713517333878,9.24134562141255,29.8217363043746));
#112267=CARTESIAN_POINT('Ctrl Pts',(4.98824100864461,9.17011768789238,29.3687390122108));
#112268=CARTESIAN_POINT('Ctrl Pts',(4.72025512133315,9.09888975437219,28.125010968892));
#112269=CARTESIAN_POINT('Ctrl Pts',(5.61709965487048,9.02766182085201,27.2225998850682));
#112270=CARTESIAN_POINT('Ctrl Pts',(6.86246206692927,8.95643388733183,27.4828850059926));
#112271=CARTESIAN_POINT('Ctrl Pts',(7.32280703595254,8.88520595381165,28.6689534656679));
#112272=CARTESIAN_POINT('Ctrl Pts',(6.57912618539456,8.81397802029147,29.7012396052901));
#112273=CARTESIAN_POINT('Ctrl Pts',(5.30832167956453,8.74275008677129,29.6401512307437));
#112274=CARTESIAN_POINT('Ctrl Pts',(4.66708636562304,8.67152215325111,28.5412912971322));
#112275=CARTESIAN_POINT('Ctrl Pts',(5.23907594952635,8.60029421973092,27.4048478108784));
#112276=CARTESIAN_POINT('Ctrl Pts',(6.50366254766546,8.52906628621076,27.2652175227977));
#112277=CARTESIAN_POINT('Ctrl Pts',(7.30981288468446,8.45783835269056,28.2494926447358));
#112278=CARTESIAN_POINT('Ctrl Pts',(6.92376474594862,8.3866104191704,29.4617808596919));
#112279=CARTESIAN_POINT('Ctrl Pts',(5.69690114803242,8.3153824856502,29.7986511517196));
#112280=CARTESIAN_POINT('Ctrl Pts',(4.74591969598952,8.24415455213003,28.9534824351831));
#112281=CARTESIAN_POINT('Ctrl Pts',(4.93640863593697,8.17292661860984,27.6955516559662));
#112282=CARTESIAN_POINT('Ctrl Pts',(6.09498394752603,8.10169868508967,27.1698339285496));
#112283=CARTESIAN_POINT('Ctrl Pts',(7.16710437781957,8.03047075156948,27.8548402529606));
#112284=CARTESIAN_POINT('Ctrl Pts',(7.176920354899,7.95924281804931,29.1270743226765));
#112285=CARTESIAN_POINT('Ctrl Pts',(6.11549732554199,7.88801488452911,29.8285420940663));
#112286=CARTESIAN_POINT('Ctrl Pts',(4.94894803192798,7.81678695100895,29.320763966274));
#112287=CARTESIAN_POINT('Ctrl Pts',(4.73907168670459,7.74555901748876,28.0659222227318));
#112288=CARTESIAN_POINT('Ctrl Pts',(5.67689882707798,7.67433108396858,27.2061803217325));
#112289=CARTESIAN_POINT('Ctrl Pts',(6.908814329393,7.6031031504484,27.5240797970017));
#112290=CARTESIAN_POINT('Ctrl Pts',(7.31352231940335,7.53187521692822,28.730266898989));
#112291=CARTESIAN_POINT('Ctrl Pts',(6.52265548647438,7.46064728340804,29.7268638756984));
#112292=CARTESIAN_POINT('Ctrl Pts',(5.25606492202359,7.38941934988787,29.6067629954084));
#112293=CARTESIAN_POINT('Ctrl Pts',(4.6666079191785,7.31819141636767,28.4792806991516));
#112294=CARTESIAN_POINT('Ctrl Pts',(5.29081130215188,7.24696348284751,27.3706572212911));
#112295=CARTESIAN_POINT('Ctrl Pts',(6.56052190638679,7.17573554932731,27.2899673868435));
#112296=CARTESIAN_POINT('Ctrl Pts',(7.32004257995058,7.10450761580715,28.3106555207405));
#112297=CARTESIAN_POINT('Ctrl Pts',(6.87805362995176,7.03327968228694,29.5036859559166));
#112298=CARTESIAN_POINT('Ctrl Pts',(5.63685576640728,6.96205174876679,29.7831562811451));
#112299=CARTESIAN_POINT('Ctrl Pts',(4.7261935670253,6.89082381524659,28.8946910143775));
#112300=CARTESIAN_POINT('Ctrl Pts',(4.97495677776857,6.81959588172642,27.6469761257391));
#112301=CARTESIAN_POINT('Ctrl Pts',(6.15671926513484,6.74836794820624,27.1756876281009));
#112302=CARTESIAN_POINT('Ctrl Pts',(7.19583579860778,6.67714001468605,27.9097958161281));
#112303=CARTESIAN_POINT('Ctrl Pts',(7.14649496219362,6.60591208116588,29.1811095446742));
#112304=CARTESIAN_POINT('Ctrl Pts',(6.05361125201206,6.53468414764569,29.832476497215));
#112305=CARTESIAN_POINT('Ctrl Pts',(4.91192488261846,6.46345621412551,29.2710112525617));
#112306=CARTESIAN_POINT('Ctrl Pts',(4.76062068060977,6.39222828060534,28.0077776670997));
#112307=CARTESIAN_POINT('Ctrl Pts',(5.73738539623194,6.32100034708514,27.1925477331129));
#112308=CARTESIAN_POINT('Ctrl Pts',(6.95322333559726,6.24977241356498,27.56740593522));
#112309=CARTESIAN_POINT('Ctrl Pts',(7.30135444430958,6.17854448004478,28.7910414742192));
#112310=CARTESIAN_POINT('Ctrl Pts',(6.46513795108138,6.10731654652461,29.7499148918931));
#112311=CARTESIAN_POINT('Ctrl Pts',(5.20525440154669,6.03608861300443,29.5708261636053));
#112312=CARTESIAN_POINT('Ctrl Pts',(4.66933017593129,5.96486067948426,28.4176178999154));
#112313=CARTESIAN_POINT('Ctrl Pts',(5.34345223203455,5.89363274596406,27.3383138705728));
#112314=CARTESIAN_POINT('Ctrl Pts',(6.61749389375153,5.82240481244389,27.3185410245704));
#112315=CARTESIAN_POINT('Ctrl Pts',(7.08834684161321,5.77491952343044,28.0190966090843));
#112316=CARTESIAN_POINT('Ctrl Pts',(7.1242205801271,5.75117687892371,28.3917868115102));
#112317=CARTESIAN_POINT('Ctrl Pts',(5.46901649069989,11.4,29.5928318776698));
#112318=CARTESIAN_POINT('Ctrl Pts',(5.10673195249988,11.3762573554933,29.4168056110598));
#112319=CARTESIAN_POINT('Ctrl Pts',(4.57712641268226,11.3287720664798,28.6791956754334));
#112320=CARTESIAN_POINT('Ctrl Pts',(5.07516714903175,11.2575441329596,27.4021252430807));
#112321=CARTESIAN_POINT('Ctrl Pts',(6.41629865909096,11.1863161994395,27.1275016028511));
#112322=CARTESIAN_POINT('Ctrl Pts',(7.3778501429631,11.1150882659193,28.1005820782907));
#112323=CARTESIAN_POINT('Ctrl Pts',(7.0856149865493,11.0438603323991,29.4380044588702));
#112324=CARTESIAN_POINT('Ctrl Pts',(5.80507309745684,10.9726323988789,29.9212455581337));
#112325=CARTESIAN_POINT('Ctrl Pts',(4.70204418941597,10.9014044653588,29.1110693286851));
#112326=CARTESIAN_POINT('Ctrl Pts',(4.78037543561609,10.8301765318385,27.7445879789133));
#112327=CARTESIAN_POINT('Ctrl Pts',(5.96883887250414,10.7589485983184,27.0657413198323));
#112328=CARTESIAN_POINT('Ctrl Pts',(7.18565321718825,10.6877206647982,27.6923362335609));
#112329=CARTESIAN_POINT('Ctrl Pts',(7.32328607724665,10.616492731278,29.0540853254779));
#112330=CARTESIAN_POINT('Ctrl Pts',(6.25645389934898,10.5452647977578,29.9114956730229));
#112331=CARTESIAN_POINT('Ctrl Pts',(4.95619769223396,10.4740368642377,29.4841591479963));
#112332=CARTESIAN_POINT('Ctrl Pts',(4.60601491366951,10.4028089307175,28.1610339130119));
#112333=CARTESIAN_POINT('Ctrl Pts',(5.52464501704607,10.3315809971973,27.1464383697959));
#112334=CARTESIAN_POINT('Ctrl Pts',(6.87594546763495,10.2603530636771,27.3638611224465));
#112335=CARTESIAN_POINT('Ctrl Pts',(7.42995592786307,10.1891251301569,28.6154036337889));
#112336=CARTESIAN_POINT('Ctrl Pts',(6.68241303332923,10.1178971966367,29.7619050238867));
#112337=CARTESIAN_POINT('Ctrl Pts',(5.31373428926388,10.0466692631166,29.7598139910742));
#112338=CARTESIAN_POINT('Ctrl Pts',(4.56969813627773,9.97544132959639,28.6110336988249));
#112339=CARTESIAN_POINT('Ctrl Pts',(5.12753016011334,9.90421339607621,27.3611899768344));
#112340=CARTESIAN_POINT('Ctrl Pts',(6.47948874973347,9.83298546255602,27.1478970303935));
#112341=CARTESIAN_POINT('Ctrl Pts',(7.39501419647751,9.76175752903586,28.1652952190123));
#112342=CARTESIAN_POINT('Ctrl Pts',(7.04079049084549,9.69052959551567,29.4873434314113));
#112343=CARTESIAN_POINT('Ctrl Pts',(5.73923388709102,9.61930166199549,29.9107065369007));
#112344=CARTESIAN_POINT('Ctrl Pts',(4.67502795044644,9.5480737284753,29.0500372408509));
#112345=CARTESIAN_POINT('Ctrl Pts',(4.81681844012803,9.47684579495514,27.6887211979427));
#112346=CARTESIAN_POINT('Ctrl Pts',(6.03554691737803,9.40561786143494,27.065835324953));
#112347=CARTESIAN_POINT('Ctrl Pts',(7.22192040624659,9.33438992791478,27.7483335718489));
#112348=CARTESIAN_POINT('Ctrl Pts',(7.29609560871817,9.26316199439458,29.1150024971194));
#112349=CARTESIAN_POINT('Ctrl Pts',(6.19055787111928,9.19193406087441,29.9218929622801));
#112350=CARTESIAN_POINT('Ctrl Pts',(4.91157337165486,9.12070612735422,29.4345690841905));
#112351=CARTESIAN_POINT('Ctrl Pts',(4.62328043009203,9.04947819383405,28.0965955822655));
#112352=CARTESIAN_POINT('Ctrl Pts',(5.58808477591762,8.97825026031386,27.1258028720057));
#112353=CARTESIAN_POINT('Ctrl Pts',(6.92781649345744,8.90702232679368,27.405811509435));
#112354=CARTESIAN_POINT('Ctrl Pts',(7.42304483023598,8.83579439327351,28.6817561816157));
#112355=CARTESIAN_POINT('Ctrl Pts',(6.62301038759335,8.76456645975332,29.7922654353375));
#112356=CARTESIAN_POINT('Ctrl Pts',(5.25590866140714,8.69333852623314,29.7265479926395));
#112357=CARTESIAN_POINT('Ctrl Pts',(4.56608272786717,8.62211059271296,28.544420210447));
#112358=CARTESIAN_POINT('Ctrl Pts',(5.18141572670952,8.55088265919278,27.3218609224974));
#112359=CARTESIAN_POINT('Ctrl Pts',(6.54182837342008,8.4796547256726,27.1716499286054));
#112360=CARTESIAN_POINT('Ctrl Pts',(7.40906602661399,8.40842679215242,28.230510053881));
#112361=CARTESIAN_POINT('Ctrl Pts',(6.99376447988865,8.33719885863224,29.5346613247478));
#112362=CARTESIAN_POINT('Ctrl Pts',(5.67393335337658,8.26597092511206,29.8970584956889));
#112363=CARTESIAN_POINT('Ctrl Pts',(4.65088977846434,8.19474299159189,28.9878457835881));
#112364=CARTESIAN_POINT('Ctrl Pts',(4.85581331896708,8.12351505807169,27.6345933110003));
#112365=CARTESIAN_POINT('Ctrl Pts',(6.10218150630337,8.05228712455152,27.069038491718));
#112366=CARTESIAN_POINT('Ctrl Pts',(7.2555435570434,7.98105919103133,27.8059522532403));
#112367=CARTESIAN_POINT('Ctrl Pts',(7.26610335530344,7.90983125751117,29.1745918707756));
#112368=CARTESIAN_POINT('Ctrl Pts',(6.12424931796667,7.83860332399097,29.9292144714445));
#112369=CARTESIAN_POINT('Ctrl Pts',(4.86930290751199,7.7673753904708,29.3829586533074));
#112370=CARTESIAN_POINT('Ctrl Pts',(4.64352285045029,7.69614745695061,28.0330292929558));
#112371=CARTESIAN_POINT('Ctrl Pts',(5.65241532493153,7.62491952343044,27.1081390903017));
#112372=CARTESIAN_POINT('Ctrl Pts',(6.97768117188443,7.55369158991026,27.4501279008548));
#112373=CARTESIAN_POINT('Ctrl Pts',(7.41305654961269,7.48246365639007,28.7477157372729));
#112374=CARTESIAN_POINT('Ctrl Pts',(6.56226053219187,7.4112357228699,29.8198314253437));
#112375=CARTESIAN_POINT('Ctrl Pts',(5.19969206545444,7.34000778934971,29.6906297109905));
#112376=CARTESIAN_POINT('Ctrl Pts',(4.56556802638696,7.26877985582953,28.4777106613761));
#112377=CARTESIAN_POINT('Ctrl Pts',(5.23707140746509,7.19755192230936,27.2850794869346));
#112378=CARTESIAN_POINT('Ctrl Pts',(6.60299633993354,7.12632398878917,27.1982752527247));
#112379=CARTESIAN_POINT('Ctrl Pts',(7.42007089321032,7.055096055269,28.296307643503));
#112380=CARTESIAN_POINT('Ctrl Pts',(6.94458953181559,6.9838681217488,29.5797418458838));
#112381=CARTESIAN_POINT('Ctrl Pts',(5.60933793803721,6.91264018822865,29.8803894768019));
#112382=CARTESIAN_POINT('Ctrl Pts',(4.62966887089418,6.84141225470844,28.9245993499317));
#112383=CARTESIAN_POINT('Ctrl Pts',(4.89728250718407,6.77018432118827,27.5823368931806));
#112384=CARTESIAN_POINT('Ctrl Pts',(6.16859491519707,6.69895638766809,27.0753357646064));
#112385=CARTESIAN_POINT('Ctrl Pts',(7.28645214666137,6.62772845414791,27.8650721610822));
#112386=CARTESIAN_POINT('Ctrl Pts',(7.23337243036839,6.55650052062773,29.2327216971408));
#112387=CARTESIAN_POINT('Ctrl Pts',(6.05767372938362,6.48527258710755,29.9334470102113));
#112388=CARTESIAN_POINT('Ctrl Pts',(4.82947427053619,6.41404465358737,29.329435849063));
#112389=CARTESIAN_POINT('Ctrl Pts',(4.66670475343396,6.34281672006718,27.9704787417039));
#112390=CARTESIAN_POINT('Ctrl Pts',(5.71748535948215,6.27158878654701,27.0934734707287));
#112391=CARTESIAN_POINT('Ctrl Pts',(7.02545534073696,6.20036085302682,27.4967371456878));
#112392=CARTESIAN_POINT('Ctrl Pts',(7.39996663454834,6.12913291950666,28.8130956020155));
#112393=CARTESIAN_POINT('Ctrl Pts',(6.50038451462898,6.05790498598646,29.8446291687303));
#112394=CARTESIAN_POINT('Ctrl Pts',(5.14503129746557,5.98667705246629,29.6519697089475));
#112395=CARTESIAN_POINT('Ctrl Pts',(4.56849656644862,5.91544911894611,28.4113752660494));
#112396=CARTESIAN_POINT('Ctrl Pts',(5.29370128702602,5.84422118542592,27.2502852676862));
#112397=CARTESIAN_POINT('Ctrl Pts',(6.66428546970392,5.77299325190575,27.2290141030205));
#112398=CARTESIAN_POINT('Ctrl Pts',(7.17081804402867,5.72550796289229,27.9826553944107));
#112399=CARTESIAN_POINT('Ctrl Pts',(7.20941017178877,5.70176531838556,28.3835867860857));
#112400=CARTESIAN_POINT('Ctrl Pts',(4.78332770288896,5.91989265014994,28.4996492411853));
#112401=CARTESIAN_POINT('Ctrl Pts',(4.78320592741866,5.918411473082,28.4746203412927));
#112402=CARTESIAN_POINT('Ctrl Pts',(4.78390735364816,5.91693029601405,28.4495973891199));
#112403=CARTESIAN_POINT('Ctrl Pts',(4.78545314171435,5.91544911894611,28.4246260068052));
#112404=CARTESIAN_POINT('Ctrl Pts',(4.80822117514724,5.89363274596407,28.056820561903));
#112405=CARTESIAN_POINT('Ctrl Pts',(5.01416991798751,5.87181637298203,27.7002029783913));
#112406=CARTESIAN_POINT('Ctrl Pts',(5.31842995130037,5.85,27.4918752544675));
#112407=CARTESIAN_POINT('',(5.44356679200015,11.4,27.719855688007));
#112408=CARTESIAN_POINT('Ctrl Pts',(5.44236585452934,11.4,27.7188687169901));
#112409=CARTESIAN_POINT('Ctrl Pts',(5.41929639243372,11.4,27.7310193813045));
#112410=CARTESIAN_POINT('Ctrl Pts',(5.39680487402872,11.4,27.7441433138064));
#112411=CARTESIAN_POINT('Ctrl Pts',(5.37496061693956,11.4,27.758225558774));
#112412=CARTESIAN_POINT('Ctrl Pts',(5.33899532853094,11.4,27.781411149368));
#112413=CARTESIAN_POINT('Ctrl Pts',(5.30478305575494,11.4,27.8071912108618));
#112414=CARTESIAN_POINT('Ctrl Pts',(5.27240127912232,11.4,27.8352556189204));
#112415=CARTESIAN_POINT('Ctrl Pts',(5.26070812807527,11.4,27.8453897559753));
#112416=CARTESIAN_POINT('Ctrl Pts',(5.2492538497354,11.4,27.8558222981223));
#112417=CARTESIAN_POINT('Ctrl Pts',(5.23804281847565,11.4,27.8665403464387));
#112418=CARTESIAN_POINT('Ctrl Pts',(5.23143763632547,11.4,27.8728550787576));
#112419=CARTESIAN_POINT('Ctrl Pts',(5.22491828276335,11.4,27.8792677296922));
#112420=CARTESIAN_POINT('Ctrl Pts',(5.21849207070704,11.4,27.8857687790983));
#112421=CARTESIAN_POINT('Ctrl Pts',(5.18802043682045,11.4,27.916595274652));
#112422=CARTESIAN_POINT('Ctrl Pts',(5.15959899380616,11.4,27.9494454109169));
#112423=CARTESIAN_POINT('Ctrl Pts',(5.13330469735818,11.4,27.9840130699589));
#112424=CARTESIAN_POINT('Ctrl Pts',(5.11565463130143,11.4,28.0072166368133));
#112425=CARTESIAN_POINT('Ctrl Pts',(5.09896336056599,11.4,28.0311952291343));
#112426=CARTESIAN_POINT('Ctrl Pts',(5.08326058957769,11.4,28.0558675649596));
#112427=CARTESIAN_POINT('Ctrl Pts',(5.07776016491816,11.4,28.0645098819418));
#112428=CARTESIAN_POINT('Ctrl Pts',(5.072381082364,11.4,28.0732373911495));
#112429=CARTESIAN_POINT('Ctrl Pts',(5.06712480617071,11.4,28.0820468134777));
#112430=CARTESIAN_POINT('Ctrl Pts',(5.06241211437772,11.4,28.0899451983382));
#112431=CARTESIAN_POINT('Ctrl Pts',(5.05780320235102,11.4,28.0979009550975));
#112432=CARTESIAN_POINT('Ctrl Pts',(5.05329864744776,11.4,28.1059112074879));
#112433=CARTESIAN_POINT('Ctrl Pts',(5.0305805054366,11.4,28.1463098828861));
#112434=CARTESIAN_POINT('Ctrl Pts',(5.01051422554295,11.4,28.1880908178382));
#112435=CARTESIAN_POINT('Ctrl Pts',(4.99318973218758,11.4,28.2309187368455));
#112436=CARTESIAN_POINT('Ctrl Pts',(4.97600243405743,11.4,28.2734074952278));
#112437=CARTESIAN_POINT('Ctrl Pts',(4.9615129573089,11.4,28.3169278593784));
#112438=CARTESIAN_POINT('Ctrl Pts',(4.94984536082048,11.4,28.3611917087713));
#112439=CARTESIAN_POINT('Ctrl Pts',(4.94394171134737,11.4,28.383588631));
#112440=CARTESIAN_POINT('Ctrl Pts',(4.93876117027847,11.4,28.406176422574));
#112441=CARTESIAN_POINT('Ctrl Pts',(4.93432428336464,11.4,28.4289202098503));
#112442=CARTESIAN_POINT('Ctrl Pts',(4.93239433792724,11.4,28.4388132428114));
#112443=CARTESIAN_POINT('Ctrl Pts',(4.93060513801621,11.4,28.4487358066513));
#112444=CARTESIAN_POINT('Ctrl Pts',(4.92895857810374,11.4,28.4586850913254));
#112445=CARTESIAN_POINT('Ctrl Pts',(4.92741239852659,11.4,28.4680278310908));
#112446=CARTESIAN_POINT('Ctrl Pts',(4.92599326509749,11.4,28.4773869022515));
#112447=CARTESIAN_POINT('Ctrl Pts',(4.92470308531398,11.4,28.4867524084507));
#112448=CARTESIAN_POINT('Ctrl Pts',(4.91825490900801,11.4,28.533560175817));
#112449=CARTESIAN_POINT('Ctrl Pts',(4.91501503058571,11.4,28.5805826774575));
#112450=CARTESIAN_POINT('Ctrl Pts',(4.91509471552749,11.4,28.6275076383839));
#112451=CARTESIAN_POINT('Ctrl Pts',(4.91509920937683,11.4,28.6301539815936));
#112452=CARTESIAN_POINT('Ctrl Pts',(4.91511427250471,11.4,28.632800021888));
#112453=CARTESIAN_POINT('Ctrl Pts',(4.9151399291788,11.4,28.6354457056802));
#112454=CARTESIAN_POINT('Ctrl Pts',(4.91557879360603,11.4,28.6807008505191));
#112455=CARTESIAN_POINT('Ctrl Pts',(4.91911290856199,11.4,28.7258508482717));
#112456=CARTESIAN_POINT('Ctrl Pts',(4.9255527364275,11.4,28.7706884317727));
#112457=CARTESIAN_POINT('Ctrl Pts',(4.92863804253891,11.4,28.7921700106729));
#112458=CARTESIAN_POINT('Ctrl Pts',(4.93239107473155,11.4,28.8135800248162));
#112459=CARTESIAN_POINT('Ctrl Pts',(4.93679506065869,11.4,28.8348960383463));
#112460=CARTESIAN_POINT('Ctrl Pts',(4.93920868546902,11.4,28.846578377928));
#112461=CARTESIAN_POINT('Ctrl Pts',(4.94181787816965,11.4,28.8582324833904));
#112462=CARTESIAN_POINT('Ctrl Pts',(4.9446201969184,11.4,28.8698546405969));
#112463=CARTESIAN_POINT('Ctrl Pts',(4.94686168957134,11.4,28.8791508635913));
#112464=CARTESIAN_POINT('Ctrl Pts',(4.94922714845825,11.4,28.8884276707925));
#112465=CARTESIAN_POINT('Ctrl Pts',(4.951710567034,11.4,28.8976664763574));
#112466=CARTESIAN_POINT('Ctrl Pts',(4.9640107207681,11.4,28.943425467563));
#112467=CARTESIAN_POINT('Ctrl Pts',(4.97922190573704,11.4,28.9883459503613));
#112468=CARTESIAN_POINT('Ctrl Pts',(4.99711839802598,11.4,29.03220214847));
#112469=CARTESIAN_POINT('Ctrl Pts',(5.0154230471994,11.4,29.0770585542674));
#112470=CARTESIAN_POINT('Ctrl Pts',(5.03653708345249,11.4,29.1208025845277));
#112471=CARTESIAN_POINT('Ctrl Pts',(5.06027378632928,11.4,29.1631943136911));
#112472=CARTESIAN_POINT('Ctrl Pts',(5.07245594705277,11.4,29.184950614922));
#112473=CARTESIAN_POINT('Ctrl Pts',(5.08532976385118,11.4,29.2063506584299));
#112474=CARTESIAN_POINT('Ctrl Pts',(5.09887511842553,11.4,29.2273608018555));
#112475=CARTESIAN_POINT('Ctrl Pts',(5.10866570028309,11.4,29.2425469328584));
#112476=CARTESIAN_POINT('Ctrl Pts',(5.11880719188057,11.4,29.2575293461396));
#112477=CARTESIAN_POINT('Ctrl Pts',(5.12929303687149,11.4,29.272294842613));
#112478=CARTESIAN_POINT('Ctrl Pts',(5.13459302453246,11.4,29.2797579463671));
#112479=CARTESIAN_POINT('Ctrl Pts',(5.13998063995912,11.4,29.2871649462043));
#112480=CARTESIAN_POINT('Ctrl Pts',(5.14544679291759,11.4,29.2945035086901));
#112481=CARTESIAN_POINT('Ctrl Pts',(5.1756022432867,11.4,29.3349885918014));
#112482=CARTESIAN_POINT('Ctrl Pts',(5.20820460790424,11.4,29.3734783462811));
#112483=CARTESIAN_POINT('Ctrl Pts',(5.2430422389611,11.4,29.4097237064037));
#112484=CARTESIAN_POINT('Ctrl Pts',(5.27762857250277,11.4,29.4457076145086));
#112485=CARTESIAN_POINT('Ctrl Pts',(5.31441858772413,11.4,29.4794804704309));
#112486=CARTESIAN_POINT('Ctrl Pts',(5.35325235903682,11.4,29.5107811307126));
#112487=CARTESIAN_POINT('Ctrl Pts',(5.39003997418695,11.4,29.5404325553737));
#112488=CARTESIAN_POINT('Ctrl Pts',(5.42866236215027,11.4,29.5678661195985));
#112489=CARTESIAN_POINT('Ctrl Pts',(5.46901649069989,11.4,29.5928318776698));
#112490=CARTESIAN_POINT('Ctrl Pts',(5.44236585452935,11.4,27.7188687169901));
#112491=CARTESIAN_POINT('Ctrl Pts',(5.68005732911861,11.378183627018,27.551292360927));
#112492=CARTESIAN_POINT('Ctrl Pts',(6.34883662302045,11.3326246095292,27.4382884675306));
#112493=CARTESIAN_POINT('Ctrl Pts',(7.08668716007769,11.2633229475337,28.1849858242981));
#112494=CARTESIAN_POINT('Ctrl Pts',(6.85620622293074,11.1920950140135,29.2397882902982));
#112495=CARTESIAN_POINT('Ctrl Pts',(5.84626444085431,11.1208670804934,29.6209123918368));
#112496=CARTESIAN_POINT('Ctrl Pts',(5.13801470280774,11.062877853077,29.1007019983506));
#112497=CARTESIAN_POINT('Ctrl Pts',(5.04282495179103,11.0286312701673,28.6413433409797));
#112498=CARTESIAN_POINT('Ctrl Pts',(5.04321154726233,11.0181273317644,28.5002974317561));
#112499=CARTESIAN_POINT('Origin',(6.,11.4,28.5));
#112500=CARTESIAN_POINT('',(6.,11.4,27.285));
#112501=CARTESIAN_POINT('Origin',(6.,11.4,28.5));
#112502=CARTESIAN_POINT('',(6.55643320799983,11.4,27.719855688007));
#112503=CARTESIAN_POINT('Ctrl Pts',(6.53227676969645,11.4,29.5943192153712));
#112504=CARTESIAN_POINT('Ctrl Pts',(6.56009586842551,11.4,29.5772957655189));
#112505=CARTESIAN_POINT('Ctrl Pts',(6.58713321731184,11.4,29.559109236633));
#112506=CARTESIAN_POINT('Ctrl Pts',(6.61330405187189,11.4,29.5397557928319));
#112507=CARTESIAN_POINT('Ctrl Pts',(6.65150531228641,11.4,29.5115057977901));
#112508=CARTESIAN_POINT('Ctrl Pts',(6.68786194993602,11.4,29.4807700839748));
#112509=CARTESIAN_POINT('Ctrl Pts',(6.72225055334609,11.4,29.4478022886025));
#112510=CARTESIAN_POINT('Ctrl Pts',(6.73459601655902,11.4,29.4359668935989));
#112511=CARTESIAN_POINT('Ctrl Pts',(6.74668750835909,11.4,29.4238436266695));
#112512=CARTESIAN_POINT('Ctrl Pts',(6.758518161031,11.4,29.4114436725547));
#112513=CARTESIAN_POINT('Ctrl Pts',(6.76638038812047,11.4,29.4032031081621));
#112514=CARTESIAN_POINT('Ctrl Pts',(6.77412910935597,11.4,29.3948384346475));
#112515=CARTESIAN_POINT('Ctrl Pts',(6.78175654779426,11.4,29.3863591511914));
#112516=CARTESIAN_POINT('Ctrl Pts',(6.8151051921031,11.4,29.3492860747895));
#112517=CARTESIAN_POINT('Ctrl Pts',(6.84607247709509,11.4,29.3101005145376));
#112518=CARTESIAN_POINT('Ctrl Pts',(6.87451984987947,11.4,29.2691010316144));
#112519=CARTESIAN_POINT('Ctrl Pts',(6.89278958823532,11.4,29.2427699594479));
#112520=CARTESIAN_POINT('Ctrl Pts',(6.91001905979329,11.4,29.2156901141727));
#112521=CARTESIAN_POINT('Ctrl Pts',(6.9261607775362,11.4,29.1879371115855));
#112522=CARTESIAN_POINT('Ctrl Pts',(6.93310293612802,11.4,29.1760012229504));
#112523=CARTESIAN_POINT('Ctrl Pts',(6.93984378696841,11.4,29.1639408058629));
#112524=CARTESIAN_POINT('Ctrl Pts',(6.94637903470487,11.4,29.1517618350014));
#112525=CARTESIAN_POINT('Ctrl Pts',(6.95299599440079,11.4,29.1394305871928));
#112526=CARTESIAN_POINT('Ctrl Pts',(6.95940454410974,11.4,29.1269725966841));
#112527=CARTESIAN_POINT('Ctrl Pts',(6.96558603837658,11.4,29.1144233999878));
#112528=CARTESIAN_POINT('Ctrl Pts',(6.98735658913844,11.4,29.0702264935599));
#112529=CARTESIAN_POINT('Ctrl Pts',(7.00634741419601,11.4,29.0248440317963));
#112530=CARTESIAN_POINT('Ctrl Pts',(7.02241524341161,11.4,28.9785600143272));
#112531=CARTESIAN_POINT('Ctrl Pts',(7.0378215111397,11.4,28.9341816508849));
#112532=CARTESIAN_POINT('Ctrl Pts',(7.05054049359629,11.4,28.8889733437029));
#112533=CARTESIAN_POINT('Ctrl Pts',(7.06039713686446,11.4,28.8431830029673));
#112534=CARTESIAN_POINT('Ctrl Pts',(7.06564289954092,11.4,28.8188131182268));
#112535=CARTESIAN_POINT('Ctrl Pts',(7.07007708883368,11.4,28.7942784321479));
#112536=CARTESIAN_POINT('Ctrl Pts',(7.07366735925498,11.4,28.769617552813));
#112537=CARTESIAN_POINT('Ctrl Pts',(7.07556720571225,11.4,28.7565678716638));
#112538=CARTESIAN_POINT('Ctrl Pts',(7.0772306699916,11.4,28.7434828754754));
#112539=CARTESIAN_POINT('Ctrl Pts',(7.07865246709527,11.4,28.7303684622724));
#112540=CARTESIAN_POINT('Ctrl Pts',(7.07981067743981,11.4,28.7196853282338));
#112541=CARTESIAN_POINT('Ctrl Pts',(7.08080850347668,11.4,28.7089806683397));
#112542=CARTESIAN_POINT('Ctrl Pts',(7.08164168102371,11.4,28.6982800333765));
#112543=CARTESIAN_POINT('Ctrl Pts',(7.08516358169497,11.4,28.65304768933));
#112544=CARTESIAN_POINT('Ctrl Pts',(7.08575848266697,11.4,28.6077985937119));
#112545=CARTESIAN_POINT('Ctrl Pts',(7.08327554477619,11.4,28.5627634602742));
#112546=CARTESIAN_POINT('Ctrl Pts',(7.08297898295393,11.4,28.5573844690045));
#112547=CARTESIAN_POINT('Ctrl Pts',(7.08263845271376,11.4,28.5520085411666));
#112548=CARTESIAN_POINT('Ctrl Pts',(7.08225364749099,11.4,28.5466360808279));
#112549=CARTESIAN_POINT('Ctrl Pts',(7.07893395049718,11.4,28.5002881120886));
#112550=CARTESIAN_POINT('Ctrl Pts',(7.07232298042015,11.4,28.4541960936328));
#112551=CARTESIAN_POINT('Ctrl Pts',(7.06257414795014,11.4,28.408635171883));
#112552=CARTESIAN_POINT('Ctrl Pts',(7.05820362076849,11.4,28.3882096237426));
#112553=CARTESIAN_POINT('Ctrl Pts',(7.05320181052273,11.4,28.36789117292));
#112554=CARTESIAN_POINT('Ctrl Pts',(7.04757982578894,11.4,28.3477067393106));
#112555=CARTESIAN_POINT('Ctrl Pts',(7.04447805167662,11.4,28.3365705380212));
#112556=CARTESIAN_POINT('Ctrl Pts',(7.04118747121866,11.4,28.3254751580379));
#112557=CARTESIAN_POINT('Ctrl Pts',(7.03770976801826,11.4,28.3144253383296));
#112558=CARTESIAN_POINT('Ctrl Pts',(7.03513303023879,11.4,28.3062381854135));
#112559=CARTESIAN_POINT('Ctrl Pts',(7.03245398332033,11.4,28.2980777026375));
#112560=CARTESIAN_POINT('Ctrl Pts',(7.02967749022565,11.4,28.289956936927));
#112561=CARTESIAN_POINT('Ctrl Pts',(7.01507754006223,11.4,28.2472545888136));
#112562=CARTESIAN_POINT('Ctrl Pts',(6.99775983297723,11.4,28.2055611382969));
#112563=CARTESIAN_POINT('Ctrl Pts',(6.97788617801526,11.4,28.1651206298401));
#112564=CARTESIAN_POINT('Ctrl Pts',(6.95814638641366,11.4,28.1249525172947));
#112565=CARTESIAN_POINT('Ctrl Pts',(6.93588409561569,11.4,28.0860196184813));
#112566=CARTESIAN_POINT('Ctrl Pts',(6.91122083093872,11.4,28.0485958527553));
#112567=CARTESIAN_POINT('Ctrl Pts',(6.89994882389591,11.4,28.0314918336258));
#112568=CARTESIAN_POINT('Ctrl Pts',(6.88817486340293,11.4,28.0147036092703));
#112569=CARTESIAN_POINT('Ctrl Pts',(6.87590868972221,11.4,27.9982605461768));
#112570=CARTESIAN_POINT('Ctrl Pts',(6.86891967402599,11.4,27.9888916240462));
#112571=CARTESIAN_POINT('Ctrl Pts',(6.86177084341387,11.4,27.9796347982128));
#112572=CARTESIAN_POINT('Ctrl Pts',(6.85446387232953,11.4,27.9704958415884));
#112573=CARTESIAN_POINT('Ctrl Pts',(6.84795581120752,11.4,27.9623560956367));
#112574=CARTESIAN_POINT('Ctrl Pts',(6.84132071214378,11.4,27.9543082434474));
#112575=CARTESIAN_POINT('Ctrl Pts',(6.83457496983701,11.4,27.9463737351544));
#112576=CARTESIAN_POINT('Ctrl Pts',(6.80665793921521,11.4,27.9135370359579));
#112577=CARTESIAN_POINT('Ctrl Pts',(6.77679555241335,11.4,27.8825701223949));
#112578=CARTESIAN_POINT('Ctrl Pts',(6.74510829213929,11.4,27.8537112982286));
#112579=CARTESIAN_POINT('Ctrl Pts',(6.71455398152641,11.4,27.8258842955191));
#112580=CARTESIAN_POINT('Ctrl Pts',(6.68230215548925,11.4,27.8000169061952));
#112581=CARTESIAN_POINT('Ctrl Pts',(6.64844095673588,11.4,27.7763655977035));
#112582=CARTESIAN_POINT('Ctrl Pts',(6.61897378626944,11.4,27.7557834220943));
#112583=CARTESIAN_POINT('Ctrl Pts',(6.58828727976892,11.4,27.7368799036835));
#112584=CARTESIAN_POINT('Ctrl Pts',(6.55643320799986,11.4,27.719855688007));
#112585=CARTESIAN_POINT('Origin',(6.,11.4,28.5));
#112586=CARTESIAN_POINT('Origin',(6.,11.4,28.5));
#112587=CARTESIAN_POINT('Origin',(6.,12.2318726682356,28.5));
#112588=CARTESIAN_POINT('Ctrl Pts',(6.55643320799984,11.4,27.719855688007));
#112589=CARTESIAN_POINT('Ctrl Pts',(6.81505873638613,11.3762573554933,27.9043187805636));
#112590=CARTESIAN_POINT('Ctrl Pts',(7.13006311729091,11.3287720664798,28.5474835379439));
#112591=CARTESIAN_POINT('Ctrl Pts',(6.57505709906184,11.2575441329596,29.4752298620382));
#112592=CARTESIAN_POINT('Ctrl Pts',(5.49603095095993,11.1863161994395,29.5126937568152));
#112593=CARTESIAN_POINT('Ctrl Pts',(5.05886120171314,11.1360923778648,28.8900758133155));
#112594=CARTESIAN_POINT('Ctrl Pts',(5.04043290394666,11.1096112007968,28.5371813420894));
#112595=CARTESIAN_POINT('Ctrl Pts',(5.04070147463229,11.1068726682356,28.5006572399252));
#112596=CARTESIAN_POINT('Ctrl Pts',(6.70552188648034,11.5482346816144,27.5108266745928));
#112597=CARTESIAN_POINT('Ctrl Pts',(7.03344259296544,11.5244920371077,27.7447141334565));
#112598=CARTESIAN_POINT('Ctrl Pts',(7.43284809549538,11.4770067480942,28.5602061034195));
#112599=CARTESIAN_POINT('Ctrl Pts',(6.72913579479277,11.4057788145741,29.7365293841653));
#112600=CARTESIAN_POINT('Ctrl Pts',(5.36099932733244,11.3345508810539,29.7840312178768));
#112601=CARTESIAN_POINT('Ctrl Pts',(4.57488060118859,11.2633229475337,28.6644395135981));
#112602=CARTESIAN_POINT('Ctrl Pts',(5.08570913854379,11.1920950140135,27.3943397937036));
#112603=CARTESIAN_POINT('Ctrl Pts',(6.42883461776721,11.1208670804934,27.1310453430996));
#112604=CARTESIAN_POINT('Ctrl Pts',(7.38157887727883,11.0496391469732,28.1135610780722));
#112605=CARTESIAN_POINT('Ctrl Pts',(7.07683046210633,10.978411213453,29.4479281552317));
#112606=CARTESIAN_POINT('Ctrl Pts',(5.79193122289995,10.9071832799328,29.9194282983902));
#112607=CARTESIAN_POINT('Ctrl Pts',(4.69642452967151,10.8359553464126,29.0989871246045));
#112608=CARTESIAN_POINT('Ctrl Pts',(4.78743525526326,10.7647274128924,27.7333295326587));
#112609=CARTESIAN_POINT('Ctrl Pts',(5.98213061030333,10.6934994793723,27.0655071925963));
#112610=CARTESIAN_POINT('Ctrl Pts',(7.19308979364578,10.6222715458521,27.7033636264439));
#112611=CARTESIAN_POINT('Ctrl Pts',(7.31809296809601,10.5510436123319,29.0663246763108));
#112612=CARTESIAN_POINT('Ctrl Pts',(6.24336083300543,10.4798156788117,29.9138130132872));
#112613=CARTESIAN_POINT('Ctrl Pts',(4.94712053941611,10.4085877452916,29.4744419613097));
#112614=CARTESIAN_POINT('Ctrl Pts',(4.60921651917625,10.3373598117713,28.148128507454));
#112615=CARTESIAN_POINT('Ctrl Pts',(5.53721086595077,10.2661318782512,27.1420904527186));
#112616=CARTESIAN_POINT('Ctrl Pts',(6.88643826296769,10.194903944731,27.372028631878));
#112617=CARTESIAN_POINT('Ctrl Pts',(7.42882496828635,10.1236760112108,28.6286522337076));
#112618=CARTESIAN_POINT('Ctrl Pts',(6.67068777783787,10.0524480776906,29.7681758863312));
#112619=CARTESIAN_POINT('Ctrl Pts',(5.3020870985883,9.98122014417048,29.7533992848146));
#112620=CARTESIAN_POINT('Ctrl Pts',(4.56873035789448,9.90999221065029,28.5977721534116));
#112621=CARTESIAN_POINT('Ctrl Pts',(5.13812266365143,9.83876427713011,27.3531523038847));
#112622=CARTESIAN_POINT('Ctrl Pts',(6.49200018730981,9.76753634360992,27.1523991695659));
#112623=CARTESIAN_POINT('Ctrl Pts',(7.39805659085291,9.69630841008975,28.178239295749));
#112624=CARTESIAN_POINT('Ctrl Pts',(7.03159463987624,9.62508047656957,29.4969476821148));
#112625=CARTESIAN_POINT('Ctrl Pts',(5.7261699014817,9.55385254304938,29.9082291217125));
#112626=CARTESIAN_POINT('Ctrl Pts',(4.66998673786223,9.48262460952922,29.0377331164763));
#112627=CARTESIAN_POINT('Ctrl Pts',(4.82438853825604,9.41139667600901,27.6777896418652));
#112628=CARTESIAN_POINT('Ctrl Pts',(6.04883798373843,9.34016874248886,27.0662262963153));
#112629=CARTESIAN_POINT('Ctrl Pts',(7.22883484332198,9.26894080896865,27.7596912064148));
#112630=CARTESIAN_POINT('Ctrl Pts',(7.29033986006644,9.1977128754485,29.1269890170851));
#112631=CARTESIAN_POINT('Ctrl Pts',(6.17737084898319,9.12648494192828,29.9235981750324));
#112632=CARTESIAN_POINT('Ctrl Pts',(4.90295797192927,9.05525700840813,29.4244408962554));
#112633=CARTESIAN_POINT('Ctrl Pts',(4.6270784342541,8.98402907488794,28.0838527227856));
#112634=CARTESIAN_POINT('Ctrl Pts',(5.60083922089711,8.91280114136776,27.1220439577224));
#112635=CARTESIAN_POINT('Ctrl Pts',(6.93791821733336,8.84157320784759,27.414457923608));
#112636=CARTESIAN_POINT('Ctrl Pts',(7.42129919158453,8.77034527432739,28.6949379132555));
#112637=CARTESIAN_POINT('Ctrl Pts',(6.61100627576171,8.69911734080723,29.7979844039908));
#112638=CARTESIAN_POINT('Ctrl Pts',(5.24457228119594,8.62788940728703,29.7195987633995));
#112639=CARTESIAN_POINT('Ctrl Pts',(4.5657325112955,8.55666147376687,28.5311280077824));
#112640=CARTESIAN_POINT('Ctrl Pts',(5.19237044271588,8.48543354024667,27.3143243781604));
#112641=CARTESIAN_POINT('Ctrl Pts',(6.5541169827227,8.4142056067265,27.1767288443099));
#112642=CARTESIAN_POINT('Ctrl Pts',(7.41150337333956,8.34297767320631,28.2435815742308));
#112643=CARTESIAN_POINT('Ctrl Pts',(6.98413207841647,8.27174973968614,29.543827684178));
#112644=CARTESIAN_POINT('Ctrl Pts',(5.66099866544571,8.20052180616594,29.8939764263401));
#112645=CARTESIAN_POINT('Ctrl Pts',(4.6464260240653,8.12929387264578,28.9753206009569));
#112646=CARTESIAN_POINT('Ctrl Pts',(4.86388343048399,8.05806593912559,27.6240255012248));
#112647=CARTESIAN_POINT('Ctrl Pts',(6.11544002641659,7.98683800560542,27.0700469300327));
#112648=CARTESIAN_POINT('Ctrl Pts',(7.26192251202089,7.91561007208523,27.8176190538471));
#112649=CARTESIAN_POINT('Ctrl Pts',(7.25979658729028,7.84438213856505,29.1862978513339));
#112650=CARTESIAN_POINT('Ctrl Pts',(6.11099727984544,7.77315420504487,29.9303047877157));
#112651=CARTESIAN_POINT('Ctrl Pts',(4.86116767315267,7.7019262715247,29.3724408939033));
#112652=CARTESIAN_POINT('Ctrl Pts',(4.64790915214598,7.63069833800451,28.0204767767365));
#112653=CARTESIAN_POINT('Ctrl Pts',(5.66533072850072,7.55947040448433,27.104977183086));
#112654=CARTESIAN_POINT('Ctrl Pts',(6.98737000937468,7.48824247096415,27.4592345859979));
#112655=CARTESIAN_POINT('Ctrl Pts',(7.4106999922714,7.41701453744397,28.7608020646698));
#112656=CARTESIAN_POINT('Ctrl Pts',(6.55000352810652,7.34578660392379,29.824986148261));
#112657=CARTESIAN_POINT('Ctrl Pts',(5.18869100836491,7.27455867040361,29.6831609811553));
#112658=CARTESIAN_POINT('Ctrl Pts',(4.56583612553444,7.20333073688343,28.4644165412846));
#112659=CARTESIAN_POINT('Ctrl Pts',(5.24836465697135,7.13210280336324,27.2780603810734));
#112660=CARTESIAN_POINT('Ctrl Pts',(6.61503552786216,7.06087486984307,27.2039199340835));
#112661=CARTESIAN_POINT('Ctrl Pts',(7.4218979617803,6.98964693632288,28.3094783981659));
#112662=CARTESIAN_POINT('Ctrl Pts',(6.93454133061941,6.91841900280271,29.5884503814807));
#112663=CARTESIAN_POINT('Ctrl Pts',(5.59656067072138,6.84719106928253,29.8767096350116));
#112664=CARTESIAN_POINT('Ctrl Pts',(4.62579192913807,6.77596313576234,28.9118797705062));
#112665=CARTESIAN_POINT('Ctrl Pts',(4.90583576184143,6.70473520224217,27.5721565059149));
#112666=CARTESIAN_POINT('Ctrl Pts',(6.18179108759432,6.63350726872198,27.0769578832154));
#112667=CARTESIAN_POINT('Ctrl Pts',(7.29228402945827,6.56227933520181,27.8770260282393));
#112668=CARTESIAN_POINT('Ctrl Pts',(7.22652398726094,6.49105140168162,29.2441157295397));
#112669=CARTESIAN_POINT('Ctrl Pts',(6.04439369632789,6.41982346816145,29.9339319479415));
#112670=CARTESIAN_POINT('Ctrl Pts',(4.82182049663989,6.34859553464126,29.3185281255925));
#112671=CARTESIAN_POINT('Ctrl Pts',(4.67170161798971,6.27736760112108,27.9581887871279));
#112672=CARTESIAN_POINT('Ctrl Pts',(5.73047192792967,6.2061396676009,27.0908275870229));
#112673=CARTESIAN_POINT('Ctrl Pts',(7.0348309571484,6.13491173408072,27.5064555648446));
#112674=CARTESIAN_POINT('Ctrl Pts',(7.39676834718207,6.06368380056054,28.8257241355228));
#112675=CARTESIAN_POINT('Ctrl Pts',(6.48837025004477,5.99245586704037,29.8498660763289));
#112676=CARTESIAN_POINT('Ctrl Pts',(5.13337661522674,5.92122793352017,29.6426470796435));
#112677=CARTESIAN_POINT('Ctrl Pts',(4.75938902674003,5.87374264450673,28.8151900159942));
#112678=CARTESIAN_POINT('Ctrl Pts',(4.78808807722243,5.85,28.4134292692096));
#112679=CARTESIAN_POINT('Ctrl Pts',(6.65582566032017,11.4988231210763,27.5805030123975));
#112680=CARTESIAN_POINT('Ctrl Pts',(6.96064797410567,11.4750804765696,27.7979156824922));
#112681=CARTESIAN_POINT('Ctrl Pts',(7.33191976942723,11.4275951875561,28.5559652482609));
#112682=CARTESIAN_POINT('Ctrl Pts',(6.67777622954912,11.3563672540359,29.6494295434563));
#112683=CARTESIAN_POINT('Ctrl Pts',(5.40600986854162,11.2851393205158,29.6935853975229));
#112684=CARTESIAN_POINT('Ctrl Pts',(4.67526452591967,11.2139113869956,28.6528565656924));
#112685=CARTESIAN_POINT('Ctrl Pts',(5.15011083365461,11.1426834534754,27.4722213459578));
#112686=CARTESIAN_POINT('Ctrl Pts',(6.39862795436207,11.0714555199552,27.2274730819635));
#112687=CARTESIAN_POINT('Ctrl Pts',(7.28426190149246,11.000227586435,28.140781432861));
#112688=CARTESIAN_POINT('Ctrl Pts',(7.00097964697716,10.9289996529148,29.381157084215));
#112689=CARTESIAN_POINT('Ctrl Pts',(5.80658737064218,10.8577717193947,29.8194452488397));
#112690=CARTESIAN_POINT('Ctrl Pts',(4.78824702679272,10.7865437858745,29.0567950960058));
#112691=CARTESIAN_POINT('Ctrl Pts',(4.87284705175466,10.7153158523543,27.7873330011059));
#112692=CARTESIAN_POINT('Ctrl Pts',(5.9833893114843,10.6440879188341,27.1665513704566));
#112693=CARTESIAN_POINT('Ctrl Pts',(7.10904979240614,10.5728599853139,27.7594778620847));
#112694=CARTESIAN_POINT('Ctrl Pts',(7.22524787356688,10.5016320517938,29.0264333565185));
#112695=CARTESIAN_POINT('Ctrl Pts',(6.22621874963804,10.4304041182736,29.8142254985652));
#112696=CARTESIAN_POINT('Ctrl Pts',(5.02128427096752,10.3591761847534,29.4058032854341));
#112697=CARTESIAN_POINT('Ctrl Pts',(4.70718185764031,10.2879482512332,28.1729139685544));
#112698=CARTESIAN_POINT('Ctrl Pts',(5.56980925008441,10.2167203177131,27.2377401855758));
#112699=CARTESIAN_POINT('Ctrl Pts',(6.82399847585742,10.1454923841929,27.4514817591112));
#112700=CARTESIAN_POINT('Ctrl Pts',(7.32818002710458,10.0742644506727,28.6195901044883));
#112701=CARTESIAN_POINT('Ctrl Pts',(6.62344522997508,10.0030365171525,29.6788468990019));
#112702=CARTESIAN_POINT('Ctrl Pts',(5.35124735577278,9.93180858363233,29.6651111458911));
#112703=CARTESIAN_POINT('Ctrl Pts',(4.66954749935143,9.86058065011214,28.5908851848551));
#112704=CARTESIAN_POINT('Ctrl Pts',(5.19883240469601,9.78935271659197,27.4339350599828));
#112705=CARTESIAN_POINT('Ctrl Pts',(6.45734420703772,9.71812478307177,27.2473227671554));
#112706=CARTESIAN_POINT('Ctrl Pts',(7.29957894210078,9.6468968495516,28.2009037843132));
#112707=CARTESIAN_POINT('Ctrl Pts',(6.95893018890553,9.57566891603142,29.4267237267286));
#112708=CARTESIAN_POINT('Ctrl Pts',(5.74545820814686,9.50444098251123,29.8090349304917));
#112709=CARTESIAN_POINT('Ctrl Pts',(4.76367148547647,9.43321304899107,28.9998557563513));
#112710=CARTESIAN_POINT('Ctrl Pts',(4.90719738401812,9.36198511547087,27.7357052823182));
#112711=CARTESIAN_POINT('Ctrl Pts',(6.04539788707867,9.2907571819507,27.1672198212593));
#112712=CARTESIAN_POINT('Ctrl Pts',(7.14227699804821,9.21952924843051,27.8118377860453));
#112713=CARTESIAN_POINT('Ctrl Pts',(7.19944966553364,9.14830131491035,29.0828245643727));
#112714=CARTESIAN_POINT('Ctrl Pts',(6.16487703129417,9.07707338139014,29.8233214037184));
#112715=CARTESIAN_POINT('Ctrl Pts',(4.98023246869392,9.00584544786998,29.359324243275));
#112716=CARTESIAN_POINT('Ctrl Pts',(4.72378559804155,8.93461751434979,28.1131657031491));
#112717=CARTESIAN_POINT('Ctrl Pts',(5.62895569004243,8.86338958082961,27.2191057447881));
#112718=CARTESIAN_POINT('Ctrl Pts',(6.87185223590666,8.79216164730945,27.4909223757654));
#112719=CARTESIAN_POINT('Ctrl Pts',(7.32118435826784,8.72093371378924,28.6812066898732));
#112720=CARTESIAN_POINT('Ctrl Pts',(6.56796763068576,8.64970578026909,29.7065557357536));
#112721=CARTESIAN_POINT('Ctrl Pts',(5.29778382215697,8.57847784674889,29.6336914979667));
#112722=CARTESIAN_POINT('Ctrl Pts',(4.66676081794155,8.50724991322872,28.5289353833659));
#112723=CARTESIAN_POINT('Ctrl Pts',(5.24925902675779,8.43602197970853,27.3978421328676));
#112724=CARTESIAN_POINT('Ctrl Pts',(6.51508556013996,8.36479404618836,27.2699386849748));
#112725=CARTESIAN_POINT('Ctrl Pts',(7.31207854724769,8.29356611266817,28.2616434208196));
#112726=CARTESIAN_POINT('Ctrl Pts',(6.91481084079411,8.222338179148,29.4703015503199));
#112727=CARTESIAN_POINT('Ctrl Pts',(5.68487756603469,8.15111024562781,29.7957861801226));
#112728=CARTESIAN_POINT('Ctrl Pts',(4.74177036379677,8.07988231210764,28.9418395133586));
#112729=CARTESIAN_POINT('Ctrl Pts',(4.94391029721191,8.00865437858744,27.685728231694));
#112730=CARTESIAN_POINT('Ctrl Pts',(6.10730855130481,7.93742644506728,27.1707713335208));
#112731=CARTESIAN_POINT('Ctrl Pts',(7.17303400585866,7.86619851154708,27.8656852562957));
#112732=CARTESIAN_POINT('Ctrl Pts',(7.17105782904973,7.79497057802691,29.1379557461679));
#112733=CARTESIAN_POINT('Ctrl Pts',(6.10317874717044,7.72374264450673,29.829555609596));
#112734=CARTESIAN_POINT('Ctrl Pts',(4.94138583499576,7.65251471098655,29.3109870668774));
#112735=CARTESIAN_POINT('Ctrl Pts',(4.74314902188165,7.58128677746636,28.0542538926687));
#112736=CARTESIAN_POINT('Ctrl Pts',(5.68890448308438,7.51005884394619,27.2032411359647));
#112737=CARTESIAN_POINT('Ctrl Pts',(6.91782069527128,7.43883091042601,27.5325450167373));
#112738=CARTESIAN_POINT('Ctrl Pts',(7.3113317555044,7.36760297690582,28.7424314391268));
#112739=CARTESIAN_POINT('Ctrl Pts',(6.51126185297857,7.29637504338565,29.7316555053074));
#112740=CARTESIAN_POINT('Ctrl Pts',(5.24583876792657,7.22514710986546,29.5998203551165));
#112741=CARTESIAN_POINT('Ctrl Pts',(4.66685713370152,7.15391917634529,28.4669230030199));
#112742=CARTESIAN_POINT('Ctrl Pts',(5.30130906693641,7.0826912428251,27.3641325339293));
#112743=CARTESIAN_POINT('Ctrl Pts',(6.57171306646886,7.01146330930493,27.2952144627321));
#112744=CARTESIAN_POINT('Ctrl Pts',(7.32174095171524,6.94023537578474,28.3228985411758));
#112745=CARTESIAN_POINT('Ctrl Pts',(6.86871321357235,6.86900744226456,29.5117810713448));
#112746=CARTESIAN_POINT('Ctrl Pts',(5.62497851648057,6.79777950874438,29.7797356435743));
#112747=CARTESIAN_POINT('Ctrl Pts',(4.72258971300468,6.72655157522421,28.8828673888663));
#112748=CARTESIAN_POINT('Ctrl Pts',(4.98290755008484,6.65532364170402,27.6375128343392));
#112749=CARTESIAN_POINT('Ctrl Pts',(6.16898591290576,6.58409570818384,27.1771954863661));
#112750=CARTESIAN_POINT('Ctrl Pts',(7.20125688966036,6.51286777466366,27.9209076653449));
#112751=CARTESIAN_POINT('Ctrl Pts',(7.14012891627897,6.44163984114348,29.1917009933094));
#112752=CARTESIAN_POINT('Ctrl Pts',(6.04126665064005,6.37041190762329,29.832927276437));
#112753=CARTESIAN_POINT('Ctrl Pts',(4.90481023257615,6.29918397410313,29.2608718577609));
#112754=CARTESIAN_POINT('Ctrl Pts',(4.76526557123557,6.22795604058293,27.9963534041114));
#112755=CARTESIAN_POINT('Ctrl Pts',(5.74945720433682,6.15672810706276,27.1900882226969));
#112756=CARTESIAN_POINT('Ctrl Pts',(6.96193854336298,6.08550017354258,27.576439799063));
#112757=CARTESIAN_POINT('Ctrl Pts',(7.29838144097109,6.01427224002239,28.8027804669918));
#112758=CARTESIAN_POINT('Ctrl Pts',(6.45396995876933,5.94304430650222,29.7547829171801));
#112759=CARTESIAN_POINT('Ctrl Pts',(5.19442066297447,5.87181637298203,29.5621602105904));
#112760=CARTESIAN_POINT('Ctrl Pts',(4.84677637032974,5.82433108396858,28.7929883598607));
#112761=CARTESIAN_POINT('Ctrl Pts',(4.87345388961561,5.80058843946185,28.4195272212344));
#112762=CARTESIAN_POINT('Ctrl Pts',(6.60612943416,11.4494115605381,27.6501793502023));
#112763=CARTESIAN_POINT('Ctrl Pts',(6.8878533552459,11.4256689160314,27.8511172315279));
#112764=CARTESIAN_POINT('Ctrl Pts',(7.23099144335906,11.378183627018,28.5517243931024));
#112765=CARTESIAN_POINT('Ctrl Pts',(6.62641666430548,11.3069556934978,29.5623297027472));
#112766=CARTESIAN_POINT('Ctrl Pts',(5.45102040975077,11.2357277599776,29.6031395771691));
#112767=CARTESIAN_POINT('Ctrl Pts',(4.77564845065076,11.1644998264574,28.6412736177867));
#112768=CARTESIAN_POINT('Ctrl Pts',(5.21451252876542,11.0932718929373,27.550102898212));
#112769=CARTESIAN_POINT('Ctrl Pts',(6.36842129095693,11.0220439594171,27.3239008208275));
#112770=CARTESIAN_POINT('Ctrl Pts',(7.18694492570609,10.9508160258969,28.1680017876497));
#112771=CARTESIAN_POINT('Ctrl Pts',(6.925128831848,10.8795880923767,29.3143860131983));
#112772=CARTESIAN_POINT('Ctrl Pts',(5.8212435183844,10.8083601588565,29.7194621992891));
#112773=CARTESIAN_POINT('Ctrl Pts',(4.88006952391394,10.7371322253364,29.0146030674072));
#112774=CARTESIAN_POINT('Ctrl Pts',(4.95825884824606,10.6659042918161,27.841336469553));
#112775=CARTESIAN_POINT('Ctrl Pts',(5.98464801266528,10.594676358296,27.267595548317));
#112776=CARTESIAN_POINT('Ctrl Pts',(7.02500979116647,10.5234484247758,27.8155920977254));
#112777=CARTESIAN_POINT('Ctrl Pts',(7.13240277903776,10.4522204912556,28.9865420367263));
#112778=CARTESIAN_POINT('Ctrl Pts',(6.20907666627063,10.3809925577354,29.7146379838433));
#112779=CARTESIAN_POINT('Ctrl Pts',(5.09544800251893,10.3097646242153,29.3371646095586));
#112780=CARTESIAN_POINT('Ctrl Pts',(4.80514719610438,10.2385366906951,28.1976994296549));
#112781=CARTESIAN_POINT('Ctrl Pts',(5.60240763421806,10.1673087571749,27.333389918433));
#112782=CARTESIAN_POINT('Ctrl Pts',(6.76155868874716,10.0960808236547,27.5309348863446));
#112783=CARTESIAN_POINT('Ctrl Pts',(7.22753508592282,10.0248528901345,28.610527975269));
#112784=CARTESIAN_POINT('Ctrl Pts',(6.57620268211228,9.95362495661436,29.5895179116725));
#112785=CARTESIAN_POINT('Ctrl Pts',(5.40040761295726,9.88239702309417,29.5768230069675));
#112786=CARTESIAN_POINT('Ctrl Pts',(4.77036464080839,9.811169089574,28.5839982162986));
#112787=CARTESIAN_POINT('Ctrl Pts',(5.2595421457406,9.73994115605382,27.5147178160809));
#112788=CARTESIAN_POINT('Ctrl Pts',(6.42268822676563,9.66871322253363,27.342246364745));
#112789=CARTESIAN_POINT('Ctrl Pts',(7.20110129334866,9.59748528901346,28.2235682728773));
#112790=CARTESIAN_POINT('Ctrl Pts',(6.88626573793482,9.52625735549327,29.3564997713423));
#112791=CARTESIAN_POINT('Ctrl Pts',(5.76474651481203,9.45502942197309,29.7098407392709));
#112792=CARTESIAN_POINT('Ctrl Pts',(4.8573562330907,9.38380148845293,28.9619783962264));
#112793=CARTESIAN_POINT('Ctrl Pts',(4.99000622978019,9.31257355493272,27.7936209227711));
#112794=CARTESIAN_POINT('Ctrl Pts',(6.04195779041892,9.24134562141256,27.2682133462034));
#112795=CARTESIAN_POINT('Ctrl Pts',(7.05571915277443,9.17011768789236,27.8639843656757));
#112796=CARTESIAN_POINT('Ctrl Pts',(7.10855947100084,9.0988897543722,29.0386601116603));
#112797=CARTESIAN_POINT('Ctrl Pts',(6.15238321360516,9.027661820852,29.7230446324044));
#112798=CARTESIAN_POINT('Ctrl Pts',(5.05750696545857,8.95643388733184,29.2942075902946));
#112799=CARTESIAN_POINT('Ctrl Pts',(4.820492761829,8.88520595381164,28.1424786835125));
#112800=CARTESIAN_POINT('Ctrl Pts',(5.65707215918775,8.81397802029147,27.3161675318539));
#112801=CARTESIAN_POINT('Ctrl Pts',(6.80578625447995,8.74275008677129,27.5673868279228));
#112802=CARTESIAN_POINT('Ctrl Pts',(7.22106952495115,8.67152215325111,28.667475466491));
#112803=CARTESIAN_POINT('Ctrl Pts',(6.52492898560981,8.60029421973093,29.6151270675163));
#112804=CARTESIAN_POINT('Ctrl Pts',(5.35099536311798,8.52906628621074,29.5477842325338));
#112805=CARTESIAN_POINT('Ctrl Pts',(4.76778912458761,8.45783835269057,28.5267427589494));
#112806=CARTESIAN_POINT('Ctrl Pts',(5.30614761079969,8.38661041917038,27.4813598875746));
#112807=CARTESIAN_POINT('Ctrl Pts',(6.47605413755724,8.31538248565021,27.3631485256397));
#112808=CARTESIAN_POINT('Ctrl Pts',(7.2126537211558,8.24415455213002,28.2797052674085));
#112809=CARTESIAN_POINT('Ctrl Pts',(6.84548960317178,8.17292661860985,29.3967754164618));
#112810=CARTESIAN_POINT('Ctrl Pts',(5.70875646662365,8.10169868508966,29.6975959339051));
#112811=CARTESIAN_POINT('Ctrl Pts',(4.83711470352825,8.03047075156948,28.9083584257603));
#112812=CARTESIAN_POINT('Ctrl Pts',(5.02393716393983,7.95924281804931,27.7474309621633));
#112813=CARTESIAN_POINT('Ctrl Pts',(6.09917707619303,7.88801488452912,27.2714957370089));
#112814=CARTESIAN_POINT('Ctrl Pts',(7.08414549969642,7.81678695100894,27.9137514587441));
#112815=CARTESIAN_POINT('Ctrl Pts',(7.08231907080919,7.74555901748876,29.0896136410019));
#112816=CARTESIAN_POINT('Ctrl Pts',(6.09536021449545,7.67433108396859,29.7288064314764));
#112817=CARTESIAN_POINT('Ctrl Pts',(5.02160399683884,7.60310315044839,29.2495332398514));
#112818=CARTESIAN_POINT('Ctrl Pts',(4.83838889161733,7.53187521692823,28.0880310086008));
#112819=CARTESIAN_POINT('Ctrl Pts',(5.71247823766805,7.46064728340803,27.3015050888434));
#112820=CARTESIAN_POINT('Ctrl Pts',(6.84827138116787,7.38941934988786,27.6058554474766));
#112821=CARTESIAN_POINT('Ctrl Pts',(7.21196351873741,7.31819141636768,28.724060813584));
#112822=CARTESIAN_POINT('Ctrl Pts',(6.47252017785062,7.24696348284751,29.6383248623537));
#112823=CARTESIAN_POINT('Ctrl Pts',(5.30298652748825,7.17573554932731,29.5164797290777));
#112824=CARTESIAN_POINT('Ctrl Pts',(4.76787814186861,7.10450761580714,28.4694294647551));
#112825=CARTESIAN_POINT('Ctrl Pts',(5.35425347690147,7.03327968228695,27.4502046867851));
#112826=CARTESIAN_POINT('Ctrl Pts',(6.52839060507555,6.96205174876678,27.3865089913807));
#112827=CARTESIAN_POINT('Ctrl Pts',(7.22158394165021,6.89082381524659,28.3363186841856));
#112828=CARTESIAN_POINT('Ctrl Pts',(6.80288509652527,6.81959588172642,29.435111761209));
#112829=CARTESIAN_POINT('Ctrl Pts',(5.65339636223977,6.74836794820623,29.6827616521368));
#112830=CARTESIAN_POINT('Ctrl Pts',(4.81938749687129,6.67714001468605,28.8538550072264));
#112831=CARTESIAN_POINT('Ctrl Pts',(5.05997933832825,6.60591208116587,27.7028691627634));
#112832=CARTESIAN_POINT('Ctrl Pts',(6.15618073821719,6.5346841476457,27.2774330895168));
#112833=CARTESIAN_POINT('Ctrl Pts',(7.11022974986244,6.46345621412551,27.9647893024504));
#112834=CARTESIAN_POINT('Ctrl Pts',(7.05373384529701,6.39222828060534,29.1392862570791));
#112835=CARTESIAN_POINT('Ctrl Pts',(6.0381396049522,6.32100034708515,29.7319226049325));
#112836=CARTESIAN_POINT('Ctrl Pts',(4.98779996851242,6.24977241356497,29.2032155899294));
#112837=CARTESIAN_POINT('Ctrl Pts',(4.85882952448143,6.17854448004479,28.034518021095));
#112838=CARTESIAN_POINT('Ctrl Pts',(5.76844248074397,6.10731654652461,27.289348858371));
#112839=CARTESIAN_POINT('Ctrl Pts',(6.88904612957757,6.03608861300443,27.6464240332814));
#112840=CARTESIAN_POINT('Ctrl Pts',(7.19999453476011,5.96486067948425,28.7798367984608));
#112841=CARTESIAN_POINT('Ctrl Pts',(6.41956966749388,5.89363274596407,29.6596997580312));
#112842=CARTESIAN_POINT('Ctrl Pts',(5.25546471072222,5.82240481244388,29.4816733415374));
#112843=CARTESIAN_POINT('Ctrl Pts',(4.93416371391945,5.77491952343044,28.7707867037272));
#112844=CARTESIAN_POINT('Ctrl Pts',(4.95881970200879,5.75117687892371,28.4256251732592));
#112845=CARTESIAN_POINT('Ctrl Pts',(6.55643320799984,11.4,27.719855688007));
#112846=CARTESIAN_POINT('Ctrl Pts',(6.81505873638613,11.3762573554933,27.9043187805636));
#112847=CARTESIAN_POINT('Ctrl Pts',(7.13006311729091,11.3287720664798,28.5474835379439));
#112848=CARTESIAN_POINT('Ctrl Pts',(6.57505709906184,11.2575441329596,29.4752298620382));
#112849=CARTESIAN_POINT('Ctrl Pts',(5.49603095095993,11.1863161994395,29.5126937568152));
#112850=CARTESIAN_POINT('Ctrl Pts',(4.87603237538185,11.1150882659193,28.629690669881));
#112851=CARTESIAN_POINT('Ctrl Pts',(5.27891422387623,11.0438603323991,27.6279844504662));
#112852=CARTESIAN_POINT('Ctrl Pts',(6.3382146275518,10.9726323988789,27.4203285596915));
#112853=CARTESIAN_POINT('Ctrl Pts',(7.08962794991972,10.9014044653588,28.1952221424384));
#112854=CARTESIAN_POINT('Ctrl Pts',(6.84927801671883,10.8301765318385,29.2476149421817));
#112855=CARTESIAN_POINT('Ctrl Pts',(5.83589966612663,10.7589485983184,29.6194791497386));
#112856=CARTESIAN_POINT('Ctrl Pts',(4.97189202103516,10.6877206647982,28.9724110388085));
#112857=CARTESIAN_POINT('Ctrl Pts',(5.04367064473747,10.616492731278,27.8953399380002));
#112858=CARTESIAN_POINT('Ctrl Pts',(5.98590671384625,10.5452647977578,27.3686397261773));
#112859=CARTESIAN_POINT('Ctrl Pts',(6.94096978992682,10.4740368642377,27.8717063333662));
#112860=CARTESIAN_POINT('Ctrl Pts',(7.03955768450863,10.4028089307175,28.9466507169341));
#112861=CARTESIAN_POINT('Ctrl Pts',(6.19193458290324,10.3315809971973,29.6150504691213));
#112862=CARTESIAN_POINT('Ctrl Pts',(5.16961173407035,10.2603530636771,29.2685259336831));
#112863=CARTESIAN_POINT('Ctrl Pts',(4.90311253456843,10.1891251301569,28.2224848907553));
#112864=CARTESIAN_POINT('Ctrl Pts',(5.63500601835172,10.1178971966368,27.4290396512902));
#112865=CARTESIAN_POINT('Ctrl Pts',(6.69911890163688,10.0466692631166,27.6103880135778));
#112866=CARTESIAN_POINT('Ctrl Pts',(7.12689014474107,9.97544132959639,28.6014658460497));
#112867=CARTESIAN_POINT('Ctrl Pts',(6.52896013424947,9.9042133960762,29.5001889243431));
#112868=CARTESIAN_POINT('Ctrl Pts',(5.44956787014175,9.83298546255604,29.4885348680441));
#112869=CARTESIAN_POINT('Ctrl Pts',(4.87118178226534,9.76175752903585,28.5771112477421));
#112870=CARTESIAN_POINT('Ctrl Pts',(5.32025188678519,9.69052959551568,27.595500572179));
#112871=CARTESIAN_POINT('Ctrl Pts',(6.38803224649353,9.61930166199549,27.4371699623346));
#112872=CARTESIAN_POINT('Ctrl Pts',(7.10262364459654,9.54807372847531,28.2462327614415));
#112873=CARTESIAN_POINT('Ctrl Pts',(6.8136012869641,9.47684579495514,29.286275815956));
#112874=CARTESIAN_POINT('Ctrl Pts',(5.78403482147721,9.40561786143493,29.6106465480502));
#112875=CARTESIAN_POINT('Ctrl Pts',(4.95104098070492,9.33438992791478,28.9241010361015));
#112876=CARTESIAN_POINT('Ctrl Pts',(5.07281507554227,9.26316199439458,27.8515365632241));
#112877=CARTESIAN_POINT('Ctrl Pts',(6.03851769375916,9.19193406087441,27.3692068711474));
#112878=CARTESIAN_POINT('Ctrl Pts',(6.96916130750066,9.12070612735422,27.9161309453062));
#112879=CARTESIAN_POINT('Ctrl Pts',(7.01766927646803,9.04947819383405,28.9944956589479));
#112880=CARTESIAN_POINT('Ctrl Pts',(6.13988939591615,8.97825026031386,29.6227678610904));
#112881=CARTESIAN_POINT('Ctrl Pts',(5.13478146222322,8.90702232679369,29.2290909373142));
#112882=CARTESIAN_POINT('Ctrl Pts',(4.91719992561646,8.8357943932735,28.1717916638759));
#112883=CARTESIAN_POINT('Ctrl Pts',(5.68518862833307,8.76456645975332,27.4132293189198));
#112884=CARTESIAN_POINT('Ctrl Pts',(6.73972027305326,8.69333852623316,27.6438512800801));
#112885=CARTESIAN_POINT('Ctrl Pts',(7.12095469163445,8.62211059271294,28.6537442431088));
#112886=CARTESIAN_POINT('Ctrl Pts',(6.48189034053387,8.5508826591928,29.5236983992791));
#112887=CARTESIAN_POINT('Ctrl Pts',(5.40420690407899,8.47965472567259,29.4618769671009));
#112888=CARTESIAN_POINT('Ctrl Pts',(4.86881743123368,8.40842679215243,28.5245501345329));
#112889=CARTESIAN_POINT('Ctrl Pts',(5.36303619484158,8.33719885863223,27.5648776422817));
#112890=CARTESIAN_POINT('Ctrl Pts',(6.43702271497452,8.26597092511206,27.4563583663045));
#112891=CARTESIAN_POINT('Ctrl Pts',(7.11322889506391,8.19474299159188,28.2977671139973));
#112892=CARTESIAN_POINT('Ctrl Pts',(6.77616836554943,8.1235150580717,29.3232492826038));
#112893=CARTESIAN_POINT('Ctrl Pts',(5.73263536721262,8.05228712455152,29.5994056876876));
#112894=CARTESIAN_POINT('Ctrl Pts',(4.93245904325973,7.98105919103134,28.874877338162));
#112895=CARTESIAN_POINT('Ctrl Pts',(5.10396403066773,7.90983125751116,27.8091336926326));
#112896=CARTESIAN_POINT('Ctrl Pts',(6.09104560108126,7.83860332399098,27.372220140497));
#112897=CARTESIAN_POINT('Ctrl Pts',(6.99525699353418,7.76737539047079,27.9618176611926));
#112898=CARTESIAN_POINT('Ctrl Pts',(6.99358031256864,7.69614745695062,29.041271535836));
#112899=CARTESIAN_POINT('Ctrl Pts',(6.08754168182046,7.62491952343044,29.6280572533568));
#112900=CARTESIAN_POINT('Ctrl Pts',(5.10182215868192,7.55369158991026,29.1880794128254));
#112901=CARTESIAN_POINT('Ctrl Pts',(4.933628761353,7.48246365639008,28.1218081245331));
#112902=CARTESIAN_POINT('Ctrl Pts',(5.73605199225171,7.41123572286989,27.399769041722));
#112903=CARTESIAN_POINT('Ctrl Pts',(6.77872206706446,7.34000778934971,27.679165878216));
#112904=CARTESIAN_POINT('Ctrl Pts',(7.11259528197041,7.26877985582954,28.705690188041));
#112905=CARTESIAN_POINT('Ctrl Pts',(6.43377850272267,7.19755192230935,29.5449942194001));
#112906=CARTESIAN_POINT('Ctrl Pts',(5.36013428704992,7.12632398878918,29.4331391030388));
#112907=CARTESIAN_POINT('Ctrl Pts',(4.86889915003569,7.05509605526898,28.4719359264905));
#112908=CARTESIAN_POINT('Ctrl Pts',(5.40719788686653,6.98386812174881,27.5362768396409));
#112909=CARTESIAN_POINT('Ctrl Pts',(6.48506814368224,6.91264018822863,27.4778035200293));
#112910=CARTESIAN_POINT('Ctrl Pts',(7.12142693158516,6.84141225470845,28.3497388271955));
#112911=CARTESIAN_POINT('Ctrl Pts',(6.73705697947822,6.77018432118827,29.3584424510732));
#112912=CARTESIAN_POINT('Ctrl Pts',(5.68181420799896,6.6989563876681,29.5857876606995));
#112913=CARTESIAN_POINT('Ctrl Pts',(4.9161852807379,6.6277284541479,28.8248426255865));
#112914=CARTESIAN_POINT('Ctrl Pts',(5.13705112657166,6.55650052062773,27.7682254911877));
#112915=CARTESIAN_POINT('Ctrl Pts',(6.14337556352862,6.48527258710754,27.3776706926676));
#112916=CARTESIAN_POINT('Ctrl Pts',(7.01920261006453,6.41404465358737,28.0086709395559));
#112917=CARTESIAN_POINT('Ctrl Pts',(6.96733877431504,6.34281672006719,29.0868715208489));
#112918=CARTESIAN_POINT('Ctrl Pts',(6.03501255926435,6.271588786547,29.630917933428));
#112919=CARTESIAN_POINT('Ctrl Pts',(5.07078970444869,6.20036085302683,29.1455593220979));
#112920=CARTESIAN_POINT('Ctrl Pts',(4.95239347772729,6.12913291950664,28.0726826380785));
#112921=CARTESIAN_POINT('Ctrl Pts',(5.78742775715113,6.05790498598646,27.388609494045));
#112922=CARTESIAN_POINT('Ctrl Pts',(6.81615371579216,5.98667705246629,27.7164082674999));
#112923=CARTESIAN_POINT('Ctrl Pts',(7.10160762854914,5.9154491189461,28.7568931299298));
#112924=CARTESIAN_POINT('Ctrl Pts',(6.38516937621842,5.84422118542593,29.5646165988824));
#112925=CARTESIAN_POINT('Ctrl Pts',(5.31650875846996,5.77299325190574,29.4011864724843));
#112926=CARTESIAN_POINT('Ctrl Pts',(5.02155105750916,5.72550796289229,28.7485850475937));
#112927=CARTESIAN_POINT('Ctrl Pts',(5.04418551440197,5.70176531838556,28.431723125284));
#112928=CARTESIAN_POINT('Ctrl Pts',(4.78808807722243,5.85,28.4134292692097));
#112929=CARTESIAN_POINT('Ctrl Pts',(4.78603023160016,5.85170244995002,28.4422372464798));
#112930=CARTESIAN_POINT('Ctrl Pts',(4.78508137249078,5.85340489990004,28.4711067562139));
#112931=CARTESIAN_POINT('Ctrl Pts',(4.78521076863826,5.85510734985006,28.4999698544854));
#112932=CARTESIAN_POINT('Origin',(6.,11.4,28.5));
#112933=CARTESIAN_POINT('',(6.,11.5,27.185));
#112934=CARTESIAN_POINT('Origin',(6.,11.4,27.185));
#112935=CARTESIAN_POINT('Origin',(6.,11.5,28.5));
#112936=CARTESIAN_POINT('Origin',(6.,11.5,28.5));
#112937=CARTESIAN_POINT('Origin',(6.,5.85,28.5));
#112938=CARTESIAN_POINT('Origin',(6.,11.5,28.5));
#112939=CARTESIAN_POINT('',(6.,11.5,26.45));
#112940=CARTESIAN_POINT('Origin',(6.,11.5,28.5));
#112941=CARTESIAN_POINT('Origin',(6.,5.675,28.5));
#112942=CARTESIAN_POINT('',(5.135,5.5,28.5));
#112943=CARTESIAN_POINT('',(4.96,5.675,28.5));
#112944=CARTESIAN_POINT('Origin',(6.,5.5,28.5));
#112945=CARTESIAN_POINT('Origin',(6.,5.5,28.5));
#112946=CARTESIAN_POINT('Origin',(8.06809628132564,14.,28.1353388268994));
#112947=CARTESIAN_POINT('',(8.06809628132564,13.85,28.1353388268994));
#112948=CARTESIAN_POINT('',(8.20597752546084,13.7,28.0570968986768));
#112949=CARTESIAN_POINT('Ctrl Pts',(8.06809628132564,13.85,28.1353388268994));
#112950=CARTESIAN_POINT('Ctrl Pts',(8.13465964056348,13.7778888548063,28.0975668615505));
#112951=CARTESIAN_POINT('Ctrl Pts',(8.20597752546084,13.7,28.0570968986768));
#112952=CARTESIAN_POINT('',(8.06809628132564,12.1,28.1353388268994));
#112953=CARTESIAN_POINT('',(8.06809628132564,14.,28.1353388268994));
#112954=CARTESIAN_POINT('',(8.20597752546084,12.1,28.0570968986768));
#112955=CARTESIAN_POINT('',(8.06809628132564,12.1,28.1353388268994));
#112956=CARTESIAN_POINT('',(8.20597752546084,11.5,28.0570968986768));
#112957=CARTESIAN_POINT('Origin',(8.28967802575338,12.1,28.0962679869244));
#112958=CARTESIAN_POINT('',(8.22442258448904,12.1,28.1617040266052));
#112959=CARTESIAN_POINT('Origin',(6.,12.1,28.5));
#112960=CARTESIAN_POINT('',(8.53904347860784,12.1,28.2147663874313));
#112961=CARTESIAN_POINT('Origin',(8.53904347860784,14.,28.2147663874313));
#112962=CARTESIAN_POINT('',(8.22442258448904,13.7,28.1617040266052));
#112963=CARTESIAN_POINT('Ctrl Pts',(8.22442258448904,13.7,28.1617040266052));
#112964=CARTESIAN_POINT('Ctrl Pts',(8.14356415181841,13.7778888548064,28.1480668543436));
#112965=CARTESIAN_POINT('Ctrl Pts',(8.06809628132564,13.85,28.1353388268994));
#112966=CARTESIAN_POINT('',(8.22442258448904,11.5,28.1617040266052));
#112967=CARTESIAN_POINT('Origin',(6.,11.5,28.5));
#112968=CARTESIAN_POINT('',(8.24937308647232,13.7,28.4468895692543));
#112969=CARTESIAN_POINT('Origin',(6.,13.7,28.5));
#112970=CARTESIAN_POINT('',(8.24937308647232,12.1,28.4468895692543));
#112971=CARTESIAN_POINT('',(8.24937308647232,11.5,28.4468895692543));
#112972=CARTESIAN_POINT('',(8.24937308647232,12.1,28.5531104307457));
#112973=CARTESIAN_POINT('Origin',(6.,12.1,28.5));
#112974=CARTESIAN_POINT('',(8.24937308647232,13.7,28.5531104307457));
#112975=CARTESIAN_POINT('',(8.24937308647232,11.5,28.5531104307457));
#112976=CARTESIAN_POINT('',(8.22442258448904,13.7,28.8382959733948));
#112977=CARTESIAN_POINT('Origin',(6.,13.7,28.5));
#112978=CARTESIAN_POINT('',(8.22442258448904,12.1,28.8382959733948));
#112979=CARTESIAN_POINT('',(8.22442258448904,11.5,28.8382959733948));
#112980=CARTESIAN_POINT('',(8.20597752546084,12.1,28.9429031013232));
#112981=CARTESIAN_POINT('Origin',(6.,12.1,28.5));
#112982=CARTESIAN_POINT('',(8.20597752546084,13.7,28.9429031013232));
#112983=CARTESIAN_POINT('',(8.20597752546084,11.5,28.9429031013232));
#112984=CARTESIAN_POINT('',(8.1318841278882,13.7,29.2194234255697));
#112985=CARTESIAN_POINT('Origin',(6.,13.7,28.5));
#112986=CARTESIAN_POINT('',(8.1318841278882,12.1,29.2194234255697));
#112987=CARTESIAN_POINT('',(8.1318841278882,11.5,29.2194234255697));
#112988=CARTESIAN_POINT('',(8.09555445361672,12.1,29.3192383852867));
#112989=CARTESIAN_POINT('Origin',(6.,12.1,28.5));
#112990=CARTESIAN_POINT('',(8.09555445361672,13.7,29.3192383852867));
#112991=CARTESIAN_POINT('',(8.09555445361672,11.5,29.3192383852867));
#112992=CARTESIAN_POINT('',(7.97456945084689,13.7,29.5786915610044));
#112993=CARTESIAN_POINT('Origin',(6.,13.7,28.5));
#112994=CARTESIAN_POINT('',(7.97456945084689,12.1,29.5786915610044));
#112995=CARTESIAN_POINT('',(7.97456945084689,11.5,29.5786915610044));
#112996=CARTESIAN_POINT('',(7.92145902010118,12.1,29.6706815254679));
#112997=CARTESIAN_POINT('Origin',(6.,12.1,28.5));
#112998=CARTESIAN_POINT('',(7.92145902010118,13.7,29.6706815254679));
#112999=CARTESIAN_POINT('',(7.92145902010118,11.5,29.6706815254679));
#113000=CARTESIAN_POINT('',(7.75725848022197,13.7,29.9051841992024));
#113001=CARTESIAN_POINT('Origin',(6.,13.7,28.5));
#113002=CARTESIAN_POINT('',(7.75725848022197,12.1,29.9051841992024));
#113003=CARTESIAN_POINT('',(7.75725848022197,11.5,29.9051841992024));
#113004=CARTESIAN_POINT('',(7.68898102656505,12.1,29.9865540998912));
#113005=CARTESIAN_POINT('Origin',(6.,12.1,28.5));
#113006=CARTESIAN_POINT('',(7.68898102656505,13.7,29.9865540998912));
#113007=CARTESIAN_POINT('',(7.68898102656505,11.5,29.9865540998912));
#113008=CARTESIAN_POINT('',(7.48655409989118,13.7,30.188981026565));
#113009=CARTESIAN_POINT('Origin',(6.,13.7,28.5));
#113010=CARTESIAN_POINT('',(7.48655409989118,12.1,30.188981026565));
#113011=CARTESIAN_POINT('',(7.48655409989118,11.5,30.188981026565));
#113012=CARTESIAN_POINT('',(7.40518419920237,12.1,30.257258480222));
#113013=CARTESIAN_POINT('Origin',(6.,12.1,28.5));
#113014=CARTESIAN_POINT('',(7.40518419920237,13.7,30.257258480222));
#113015=CARTESIAN_POINT('',(7.40518419920237,11.5,30.257258480222));
#113016=CARTESIAN_POINT('',(7.17068152546788,13.7,30.4214590201012));
#113017=CARTESIAN_POINT('Origin',(6.,13.7,28.5));
#113018=CARTESIAN_POINT('',(7.17068152546788,12.1,30.4214590201012));
#113019=CARTESIAN_POINT('',(7.17068152546788,11.5,30.4214590201012));
#113020=CARTESIAN_POINT('',(7.07869156100444,12.1,30.4745694508469));
#113021=CARTESIAN_POINT('Origin',(6.,12.1,28.5));
#113022=CARTESIAN_POINT('',(7.07869156100444,13.7,30.4745694508469));
#113023=CARTESIAN_POINT('',(7.07869156100444,11.5,30.4745694508469));
#113024=CARTESIAN_POINT('',(6.81923838528667,13.7,30.5955544536167));
#113025=CARTESIAN_POINT('Origin',(6.,13.7,28.5));
#113026=CARTESIAN_POINT('',(6.81923838528667,12.1,30.5955544536167));
#113027=CARTESIAN_POINT('',(6.81923838528667,11.5,30.5955544536167));
#113028=CARTESIAN_POINT('',(6.71942342556966,12.1,30.6318841278882));
#113029=CARTESIAN_POINT('Origin',(6.,12.1,28.5));
#113030=CARTESIAN_POINT('',(6.71942342556966,13.7,30.6318841278882));
#113031=CARTESIAN_POINT('',(6.71942342556966,11.5,30.6318841278882));
#113032=CARTESIAN_POINT('',(6.44290310132316,13.7,30.7059775254608));
#113033=CARTESIAN_POINT('Origin',(6.,13.7,28.5));
#113034=CARTESIAN_POINT('',(6.44290310132316,12.1,30.7059775254608));
#113035=CARTESIAN_POINT('',(6.44290310132316,11.5,30.7059775254608));
#113036=CARTESIAN_POINT('',(6.33829597339476,12.1,30.724422584489));
#113037=CARTESIAN_POINT('Origin',(6.,12.1,28.5));
#113038=CARTESIAN_POINT('',(6.33829597339476,13.7,30.724422584489));
#113039=CARTESIAN_POINT('',(6.33829597339476,11.5,30.724422584489));
#113040=CARTESIAN_POINT('',(6.05311043074571,13.7,30.7493730864723));
#113041=CARTESIAN_POINT('Origin',(6.,13.7,28.5));
#113042=CARTESIAN_POINT('',(6.05311043074571,12.1,30.7493730864723));
#113043=CARTESIAN_POINT('',(6.05311043074571,11.5,30.7493730864723));
#113044=CARTESIAN_POINT('',(5.94688956925429,12.1,30.7493730864723));
#113045=CARTESIAN_POINT('Origin',(6.,12.1,28.5));
#113046=CARTESIAN_POINT('',(5.94688956925429,13.7,30.7493730864723));
#113047=CARTESIAN_POINT('',(5.94688956925429,11.5,30.7493730864723));
#113048=CARTESIAN_POINT('',(5.66170402660524,13.7,30.724422584489));
#113049=CARTESIAN_POINT('Origin',(6.,13.7,28.5));
#113050=CARTESIAN_POINT('',(5.66170402660524,12.1,30.724422584489));
#113051=CARTESIAN_POINT('',(5.66170402660524,11.5,30.724422584489));
#113052=CARTESIAN_POINT('',(5.55709689867685,12.1,30.7059775254608));
#113053=CARTESIAN_POINT('Origin',(6.,12.1,28.5));
#113054=CARTESIAN_POINT('',(5.55709689867685,13.7,30.7059775254608));
#113055=CARTESIAN_POINT('',(5.55709689867685,11.5,30.7059775254608));
#113056=CARTESIAN_POINT('',(5.28057657443035,13.7,30.6318841278882));
#113057=CARTESIAN_POINT('Origin',(6.,13.7,28.5));
#113058=CARTESIAN_POINT('',(5.28057657443035,12.1,30.6318841278882));
#113059=CARTESIAN_POINT('',(5.28057657443035,11.5,30.6318841278882));
#113060=CARTESIAN_POINT('',(5.18076161471333,12.1,30.5955544536167));
#113061=CARTESIAN_POINT('Origin',(6.,12.1,28.5));
#113062=CARTESIAN_POINT('',(5.18076161471333,13.7,30.5955544536167));
#113063=CARTESIAN_POINT('',(5.18076161471333,11.5,30.5955544536167));
#113064=CARTESIAN_POINT('',(4.92130843899556,13.7,30.4745694508469));
#113065=CARTESIAN_POINT('Origin',(6.,13.7,28.5));
#113066=CARTESIAN_POINT('',(4.92130843899556,12.1,30.4745694508469));
#113067=CARTESIAN_POINT('',(4.92130843899556,11.5,30.4745694508469));
#113068=CARTESIAN_POINT('',(4.82931847453212,12.1,30.4214590201012));
#113069=CARTESIAN_POINT('Origin',(6.,12.1,28.5));
#113070=CARTESIAN_POINT('',(4.82931847453212,13.7,30.4214590201012));
#113071=CARTESIAN_POINT('',(4.82931847453212,11.5,30.4214590201012));
#113072=CARTESIAN_POINT('',(4.59481580079764,13.7,30.257258480222));
#113073=CARTESIAN_POINT('Origin',(6.,13.7,28.5));
#113074=CARTESIAN_POINT('',(4.59481580079764,12.1,30.257258480222));
#113075=CARTESIAN_POINT('',(4.59481580079764,11.5,30.257258480222));
#113076=CARTESIAN_POINT('',(4.51344590010882,12.1,30.188981026565));
#113077=CARTESIAN_POINT('Origin',(6.,12.1,28.5));
#113078=CARTESIAN_POINT('',(4.51344590010882,13.7,30.188981026565));
#113079=CARTESIAN_POINT('',(4.51344590010882,11.5,30.188981026565));
#113080=CARTESIAN_POINT('',(4.31101897343496,13.7,29.9865540998912));
#113081=CARTESIAN_POINT('Origin',(6.,13.7,28.5));
#113082=CARTESIAN_POINT('',(4.31101897343496,12.1,29.9865540998912));
#113083=CARTESIAN_POINT('',(4.31101897343496,11.5,29.9865540998912));
#113084=CARTESIAN_POINT('',(4.24274151977804,12.1,29.9051841992024));
#113085=CARTESIAN_POINT('Origin',(6.,12.1,28.5));
#113086=CARTESIAN_POINT('',(4.24274151977804,13.7,29.9051841992024));
#113087=CARTESIAN_POINT('',(4.24274151977804,11.5,29.9051841992024));
#113088=CARTESIAN_POINT('',(4.07854097989882,13.7,29.6706815254679));
#113089=CARTESIAN_POINT('Origin',(6.,13.7,28.5));
#113090=CARTESIAN_POINT('',(4.07854097989882,12.1,29.6706815254679));
#113091=CARTESIAN_POINT('',(4.07854097989882,11.5,29.6706815254679));
#113092=CARTESIAN_POINT('',(4.0254305491531,12.1,29.5786915610044));
#113093=CARTESIAN_POINT('Origin',(6.,12.1,28.5));
#113094=CARTESIAN_POINT('',(4.0254305491531,13.7,29.5786915610044));
#113095=CARTESIAN_POINT('',(4.0254305491531,11.5,29.5786915610044));
#113096=CARTESIAN_POINT('',(3.90444554638328,13.7,29.3192383852867));
#113097=CARTESIAN_POINT('Origin',(6.,13.7,28.5));
#113098=CARTESIAN_POINT('',(3.90444554638328,12.1,29.3192383852867));
#113099=CARTESIAN_POINT('',(3.90444554638328,11.5,29.3192383852867));
#113100=CARTESIAN_POINT('',(3.8681158721118,12.1,29.2194234255697));
#113101=CARTESIAN_POINT('Origin',(6.,12.1,28.5));
#113102=CARTESIAN_POINT('',(3.8681158721118,13.7,29.2194234255697));
#113103=CARTESIAN_POINT('',(3.8681158721118,11.5,29.2194234255697));
#113104=CARTESIAN_POINT('',(3.79402247453916,13.7,28.9429031013232));
#113105=CARTESIAN_POINT('Origin',(6.,13.7,28.5));
#113106=CARTESIAN_POINT('',(3.79402247453916,12.1,28.9429031013232));
#113107=CARTESIAN_POINT('',(3.79402247453916,11.5,28.9429031013232));
#113108=CARTESIAN_POINT('',(3.77557741551096,12.1,28.8382959733948));
#113109=CARTESIAN_POINT('Origin',(6.,12.1,28.5));
#113110=CARTESIAN_POINT('',(3.77557741551096,13.7,28.8382959733948));
#113111=CARTESIAN_POINT('',(3.77557741551096,11.5,28.8382959733948));
#113112=CARTESIAN_POINT('',(3.75062691352768,13.7,28.5531104307457));
#113113=CARTESIAN_POINT('Origin',(6.,13.7,28.5));
#113114=CARTESIAN_POINT('',(3.75062691352768,12.1,28.5531104307457));
#113115=CARTESIAN_POINT('',(3.75062691352768,11.5,28.5531104307457));
#113116=CARTESIAN_POINT('',(3.75,12.1,28.5));
#113117=CARTESIAN_POINT('Origin',(6.,12.1,28.5));
#113118=CARTESIAN_POINT('',(3.75,11.7,28.5));
#113119=CARTESIAN_POINT('',(3.75,11.5,28.5));
#113120=CARTESIAN_POINT('',(6.,11.7,26.25));
#113121=CARTESIAN_POINT('Origin',(6.,11.7,28.5));
#113122=CARTESIAN_POINT('Origin',(6.,11.7,28.5));
#113123=CARTESIAN_POINT('',(3.75062691352768,12.1,28.4468895692543));
#113124=CARTESIAN_POINT('Origin',(6.,12.1,28.5));
#113125=CARTESIAN_POINT('',(3.75062691352768,13.7,28.4468895692543));
#113126=CARTESIAN_POINT('',(3.75062691352768,11.5,28.4468895692543));
#113127=CARTESIAN_POINT('',(3.77557741551096,13.7,28.1617040266052));
#113128=CARTESIAN_POINT('Origin',(6.,13.7,28.5));
#113129=CARTESIAN_POINT('',(3.77557741551096,12.1,28.1617040266052));
#113130=CARTESIAN_POINT('',(3.77557741551096,11.5,28.1617040266052));
#113131=CARTESIAN_POINT('',(3.79402247453916,12.1,28.0570968986769));
#113132=CARTESIAN_POINT('Origin',(6.,12.1,28.5));
#113133=CARTESIAN_POINT('',(3.79402247453916,13.7,28.0570968986769));
#113134=CARTESIAN_POINT('',(3.79402247453916,11.5,28.0570968986769));
#113135=CARTESIAN_POINT('',(3.8681158721118,13.7,27.7805765744303));
#113136=CARTESIAN_POINT('Origin',(6.,13.7,28.5));
#113137=CARTESIAN_POINT('',(3.8681158721118,12.1,27.7805765744303));
#113138=CARTESIAN_POINT('',(3.8681158721118,11.5,27.7805765744303));
#113139=CARTESIAN_POINT('',(3.90444554638328,12.1,27.6807616147133));
#113140=CARTESIAN_POINT('Origin',(6.,12.1,28.5));
#113141=CARTESIAN_POINT('',(3.90444554638328,13.7,27.6807616147133));
#113142=CARTESIAN_POINT('',(3.90444554638328,11.5,27.6807616147133));
#113143=CARTESIAN_POINT('',(4.0254305491531,13.7,27.4213084389956));
#113144=CARTESIAN_POINT('Origin',(6.,13.7,28.5));
#113145=CARTESIAN_POINT('',(4.0254305491531,12.1,27.4213084389956));
#113146=CARTESIAN_POINT('',(4.0254305491531,11.5,27.4213084389956));
#113147=CARTESIAN_POINT('',(4.07854097989881,12.1,27.3293184745321));
#113148=CARTESIAN_POINT('Origin',(6.,12.1,28.5));
#113149=CARTESIAN_POINT('',(4.07854097989881,13.7,27.3293184745321));
#113150=CARTESIAN_POINT('',(4.07854097989881,11.5,27.3293184745321));
#113151=CARTESIAN_POINT('',(4.24274151977803,13.7,27.0948158007976));
#113152=CARTESIAN_POINT('Origin',(6.,13.7,28.5));
#113153=CARTESIAN_POINT('',(4.24274151977803,12.1,27.0948158007976));
#113154=CARTESIAN_POINT('',(4.24274151977803,11.5,27.0948158007976));
#113155=CARTESIAN_POINT('',(4.31101897343496,12.1,27.0134459001088));
#113156=CARTESIAN_POINT('Origin',(6.,12.1,28.5));
#113157=CARTESIAN_POINT('',(4.31101897343495,13.7,27.0134459001088));
#113158=CARTESIAN_POINT('',(4.31101897343495,11.5,27.0134459001088));
#113159=CARTESIAN_POINT('',(4.51344590010881,13.7,26.811018973435));
#113160=CARTESIAN_POINT('Origin',(6.,13.7,28.5));
#113161=CARTESIAN_POINT('',(4.51344590010881,12.1,26.811018973435));
#113162=CARTESIAN_POINT('',(4.51344590010881,11.5,26.811018973435));
#113163=CARTESIAN_POINT('',(4.59481580079763,12.1,26.742741519778));
#113164=CARTESIAN_POINT('Origin',(6.,12.1,28.5));
#113165=CARTESIAN_POINT('',(4.59481580079763,13.7,26.742741519778));
#113166=CARTESIAN_POINT('',(4.59481580079763,11.5,26.742741519778));
#113167=CARTESIAN_POINT('',(4.82931847453212,13.7,26.5785409798988));
#113168=CARTESIAN_POINT('Origin',(6.,13.7,28.5));
#113169=CARTESIAN_POINT('',(4.82931847453212,12.1,26.5785409798988));
#113170=CARTESIAN_POINT('',(4.82931847453212,11.5,26.5785409798988));
#113171=CARTESIAN_POINT('',(4.92130843899556,12.1,26.5254305491531));
#113172=CARTESIAN_POINT('Origin',(6.,12.1,28.5));
#113173=CARTESIAN_POINT('',(4.92130843899556,13.7,26.5254305491531));
#113174=CARTESIAN_POINT('',(4.92130843899556,11.5,26.5254305491531));
#113175=CARTESIAN_POINT('',(5.18076161471333,13.7,26.4044455463833));
#113176=CARTESIAN_POINT('Origin',(6.,13.7,28.5));
#113177=CARTESIAN_POINT('',(5.18076161471333,12.1,26.4044455463833));
#113178=CARTESIAN_POINT('',(5.18076161471333,11.5,26.4044455463833));
#113179=CARTESIAN_POINT('',(5.28057657443034,12.1,26.3681158721118));
#113180=CARTESIAN_POINT('Origin',(6.,12.1,28.5));
#113181=CARTESIAN_POINT('',(5.28057657443034,13.7,26.3681158721118));
#113182=CARTESIAN_POINT('',(5.28057657443034,11.5,26.3681158721118));
#113183=CARTESIAN_POINT('',(5.55709689867685,13.7,26.2940224745392));
#113184=CARTESIAN_POINT('Origin',(6.,13.7,28.5));
#113185=CARTESIAN_POINT('',(5.55709689867685,12.1,26.2940224745392));
#113186=CARTESIAN_POINT('',(5.55709689867685,11.5,26.2940224745392));
#113187=CARTESIAN_POINT('',(5.66170402660524,12.1,26.275577415511));
#113188=CARTESIAN_POINT('Origin',(6.,12.1,28.5));
#113189=CARTESIAN_POINT('',(5.66170402660524,13.7,26.275577415511));
#113190=CARTESIAN_POINT('',(5.66170402660524,11.5,26.275577415511));
#113191=CARTESIAN_POINT('',(5.94688956925429,13.7,26.2506269135277));
#113192=CARTESIAN_POINT('Origin',(6.,13.7,28.5));
#113193=CARTESIAN_POINT('',(5.94688956925429,12.1,26.2506269135277));
#113194=CARTESIAN_POINT('',(5.94688956925429,11.5,26.2506269135277));
#113195=CARTESIAN_POINT('',(6.05311043074571,12.1,26.2506269135277));
#113196=CARTESIAN_POINT('Origin',(6.,12.1,28.5));
#113197=CARTESIAN_POINT('',(6.05311043074571,13.7,26.2506269135277));
#113198=CARTESIAN_POINT('',(6.05311043074571,11.5,26.2506269135277));
#113199=CARTESIAN_POINT('',(6.33829597339476,13.7,26.275577415511));
#113200=CARTESIAN_POINT('Origin',(6.,13.7,28.5));
#113201=CARTESIAN_POINT('',(6.33829597339476,12.1,26.275577415511));
#113202=CARTESIAN_POINT('',(6.33829597339476,11.5,26.275577415511));
#113203=CARTESIAN_POINT('',(6.44290310132316,12.1,26.2940224745392));
#113204=CARTESIAN_POINT('Origin',(6.,12.1,28.5));
#113205=CARTESIAN_POINT('',(6.44290310132316,13.7,26.2940224745392));
#113206=CARTESIAN_POINT('',(6.44290310132316,11.5,26.2940224745392));
#113207=CARTESIAN_POINT('',(6.71942342556966,13.7,26.3681158721118));
#113208=CARTESIAN_POINT('Origin',(6.,13.7,28.5));
#113209=CARTESIAN_POINT('',(6.71942342556966,12.1,26.3681158721118));
#113210=CARTESIAN_POINT('',(6.71942342556966,11.5,26.3681158721118));
#113211=CARTESIAN_POINT('',(6.81923838528667,12.1,26.4044455463833));
#113212=CARTESIAN_POINT('Origin',(6.,12.1,28.5));
#113213=CARTESIAN_POINT('',(6.81923838528667,13.7,26.4044455463833));
#113214=CARTESIAN_POINT('',(6.81923838528667,11.5,26.4044455463833));
#113215=CARTESIAN_POINT('',(7.07869156100444,13.7,26.5254305491531));
#113216=CARTESIAN_POINT('Origin',(6.,13.7,28.5));
#113217=CARTESIAN_POINT('',(7.07869156100444,12.1,26.5254305491531));
#113218=CARTESIAN_POINT('',(7.07869156100444,11.5,26.5254305491531));
#113219=CARTESIAN_POINT('',(7.17068152546788,12.1,26.5785409798988));
#113220=CARTESIAN_POINT('Origin',(6.,12.1,28.5));
#113221=CARTESIAN_POINT('',(7.17068152546788,13.7,26.5785409798988));
#113222=CARTESIAN_POINT('',(7.17068152546788,11.5,26.5785409798988));
#113223=CARTESIAN_POINT('',(7.40518419920236,13.7,26.742741519778));
#113224=CARTESIAN_POINT('Origin',(6.,13.7,28.5));
#113225=CARTESIAN_POINT('',(7.40518419920237,12.1,26.742741519778));
#113226=CARTESIAN_POINT('',(7.40518419920236,11.5,26.742741519778));
#113227=CARTESIAN_POINT('',(7.48655409989118,12.1,26.811018973435));
#113228=CARTESIAN_POINT('Origin',(6.,12.1,28.5));
#113229=CARTESIAN_POINT('',(7.48655409989118,13.7,26.811018973435));
#113230=CARTESIAN_POINT('',(7.48655409989118,11.5,26.811018973435));
#113231=CARTESIAN_POINT('',(7.68898102656504,13.7,27.0134459001088));
#113232=CARTESIAN_POINT('Origin',(6.,13.7,28.5));
#113233=CARTESIAN_POINT('',(7.68898102656504,12.1,27.0134459001088));
#113234=CARTESIAN_POINT('',(7.68898102656504,11.5,27.0134459001088));
#113235=CARTESIAN_POINT('',(7.75725848022196,12.1,27.0948158007976));
#113236=CARTESIAN_POINT('Origin',(6.,12.1,28.5));
#113237=CARTESIAN_POINT('',(7.75725848022196,13.7,27.0948158007976));
#113238=CARTESIAN_POINT('',(7.75725848022196,11.5,27.0948158007976));
#113239=CARTESIAN_POINT('',(7.92145902010118,13.7,27.3293184745321));
#113240=CARTESIAN_POINT('Origin',(6.,13.7,28.5));
#113241=CARTESIAN_POINT('',(7.92145902010118,12.1,27.3293184745321));
#113242=CARTESIAN_POINT('',(7.92145902010118,11.5,27.3293184745321));
#113243=CARTESIAN_POINT('',(7.97456945084689,12.1,27.4213084389956));
#113244=CARTESIAN_POINT('Origin',(6.,12.1,28.5));
#113245=CARTESIAN_POINT('',(7.97456945084689,13.7,27.4213084389956));
#113246=CARTESIAN_POINT('',(7.97456945084689,11.5,27.4213084389956));
#113247=CARTESIAN_POINT('',(8.09555445361672,13.7,27.6807616147133));
#113248=CARTESIAN_POINT('Origin',(6.,13.7,28.5));
#113249=CARTESIAN_POINT('',(8.09555445361672,12.1,27.6807616147133));
#113250=CARTESIAN_POINT('',(8.09555445361672,11.5,27.6807616147133));
#113251=CARTESIAN_POINT('',(8.1318841278882,12.1,27.7805765744303));
#113252=CARTESIAN_POINT('Origin',(6.,12.1,28.5));
#113253=CARTESIAN_POINT('',(8.1318841278882,13.7,27.7805765744303));
#113254=CARTESIAN_POINT('',(8.1318841278882,11.5,27.7805765744303));
#113255=CARTESIAN_POINT('Origin',(6.,13.7,28.5));
#113256=CARTESIAN_POINT('Origin',(7.97335450365041,14.,27.7817576990161));
#113257=CARTESIAN_POINT('',(7.97335450365041,13.85,27.7817576990161));
#113258=CARTESIAN_POINT('Ctrl Pts',(7.97335450365041,13.85,27.7817576990161));
#113259=CARTESIAN_POINT('Ctrl Pts',(8.03234758294447,13.7778888548065,27.7330009686631));
#113260=CARTESIAN_POINT('Ctrl Pts',(8.09555445361672,13.7,27.6807616147133));
#113261=CARTESIAN_POINT('',(7.97335450365041,12.1,27.7817576990161));
#113262=CARTESIAN_POINT('',(7.97335450365041,14.,27.7817576990161));
#113263=CARTESIAN_POINT('',(7.97335450365041,12.1,27.7817576990161));
#113264=CARTESIAN_POINT('Origin',(8.18478534332724,12.1,27.7048031667678));
#113265=CARTESIAN_POINT('',(8.45093940593617,12.1,27.7781994538453));
#113266=CARTESIAN_POINT('Origin',(8.45093940593617,14.,27.7781994538453));
#113267=CARTESIAN_POINT('Ctrl Pts',(8.1318841278882,13.7,27.7805765744303));
#113268=CARTESIAN_POINT('Ctrl Pts',(8.04988604638594,13.7778888548064,27.7811875009402));
#113269=CARTESIAN_POINT('Ctrl Pts',(7.97335450365041,13.85,27.7817576990161));
#113270=CARTESIAN_POINT('Origin',(7.81865334794732,14.,27.45));
#113271=CARTESIAN_POINT('',(7.81865334794732,13.85,27.45));
#113272=CARTESIAN_POINT('Ctrl Pts',(7.81865334794732,13.85,27.45));
#113273=CARTESIAN_POINT('Ctrl Pts',(7.86828367243552,13.7778888548063,27.3917399532223));
#113274=CARTESIAN_POINT('Ctrl Pts',(7.92145902010118,13.7,27.3293184745321));
#113275=CARTESIAN_POINT('',(7.81865334794732,12.1,27.45));
#113276=CARTESIAN_POINT('',(7.81865334794732,14.,27.45));
#113277=CARTESIAN_POINT('',(7.81865334794732,12.1,27.45));
#113278=CARTESIAN_POINT('Origin',(8.01350906379882,12.1,27.3375));
#113279=CARTESIAN_POINT('',(8.28836477965032,12.1,27.3635640646055));
#113280=CARTESIAN_POINT('Origin',(8.28836477965032,14.,27.3635640646055));
#113281=CARTESIAN_POINT('Ctrl Pts',(7.9745694508469,13.7,27.4213084389956));
#113282=CARTESIAN_POINT('Ctrl Pts',(7.89392319072658,13.7778888548063,27.436148901584));
#113283=CARTESIAN_POINT('Ctrl Pts',(7.81865334794732,13.85,27.45));
#113284=CARTESIAN_POINT('Origin',(7.60869333054985,14.,27.1501460196583));
#113285=CARTESIAN_POINT('',(7.60869333054985,13.85,27.1501460196583));
#113286=CARTESIAN_POINT('Ctrl Pts',(7.60869333054985,13.85,27.1501460196583));
#113287=CARTESIAN_POINT('Ctrl Pts',(7.64745290793648,13.7778888548065,27.0841528584965));
#113288=CARTESIAN_POINT('Ctrl Pts',(7.68898102656505,13.7,27.0134459001088));
#113289=CARTESIAN_POINT('',(7.60869333054985,12.1,27.1501460196583));
#113290=CARTESIAN_POINT('',(7.60869333054985,14.,27.1501460196583));
#113291=CARTESIAN_POINT('',(7.60869333054985,12.1,27.1501460196583));
#113292=CARTESIAN_POINT('Origin',(7.78105333025163,12.1,27.0055188074788));
#113293=CARTESIAN_POINT('',(8.05625934750324,12.1,26.9834587061984));
#113294=CARTESIAN_POINT('Origin',(8.05625934750324,14.,26.9834587061984));
#113295=CARTESIAN_POINT('Ctrl Pts',(7.75725848022197,13.7,27.0948158007976));
#113296=CARTESIAN_POINT('Ctrl Pts',(7.68041443728832,13.7778888548063,27.1234348795186));
#113297=CARTESIAN_POINT('Ctrl Pts',(7.60869333054985,13.85,27.1501460196583));
#113298=CARTESIAN_POINT('Origin',(7.34985398034173,14.,26.8913066694501));
#113299=CARTESIAN_POINT('',(7.34985398034173,13.85,26.8913066694501));
#113300=CARTESIAN_POINT('Ctrl Pts',(7.34985398034173,13.85,26.8913066694501));
#113301=CARTESIAN_POINT('Ctrl Pts',(7.37656512048136,13.7778888548064,26.8195855627119));
#113302=CARTESIAN_POINT('Ctrl Pts',(7.40518419920237,13.7,26.742741519778));
#113303=CARTESIAN_POINT('',(7.34985398034173,12.1,26.8913066694501));
#113304=CARTESIAN_POINT('',(7.34985398034173,14.,26.8913066694501));
#113305=CARTESIAN_POINT('',(7.34985398034173,12.1,26.8913066694501));
#113306=CARTESIAN_POINT('Origin',(7.49448119252121,12.1,26.7189466697484));
#113307=CARTESIAN_POINT('',(7.76167551559972,12.1,26.6494326875964));
#113308=CARTESIAN_POINT('Origin',(7.76167551559972,14.,26.6494326875964));
#113309=CARTESIAN_POINT('Ctrl Pts',(7.48655409989118,13.7,26.811018973435));
#113310=CARTESIAN_POINT('Ctrl Pts',(7.4158471415036,13.7778888548064,26.8525470920635));
#113311=CARTESIAN_POINT('Ctrl Pts',(7.34985398034173,13.85,26.8913066694501));
#113312=CARTESIAN_POINT('Origin',(7.05000000000001,14.,26.6813466520527));
#113313=CARTESIAN_POINT('',(7.05000000000001,13.85,26.6813466520527));
#113314=CARTESIAN_POINT('Ctrl Pts',(7.05000000000001,13.85,26.6813466520527));
#113315=CARTESIAN_POINT('Ctrl Pts',(7.06385109841592,13.7778888548066,26.6060768092737));
#113316=CARTESIAN_POINT('Ctrl Pts',(7.07869156100444,13.7,26.5254305491531));
#113317=CARTESIAN_POINT('',(7.05000000000001,12.1,26.6813466520527));
#113318=CARTESIAN_POINT('',(7.05000000000001,14.,26.6813466520527));
#113319=CARTESIAN_POINT('',(7.05000000000001,12.1,26.6813466520527));
#113320=CARTESIAN_POINT('Origin',(7.1625,12.1,26.4864909362012));
#113321=CARTESIAN_POINT('',(7.41356406460552,12.1,26.3716352203497));
#113322=CARTESIAN_POINT('Origin',(7.41356406460552,14.,26.3716352203497));
#113323=CARTESIAN_POINT('Ctrl Pts',(7.17068152546789,13.7,26.5785409798988));
#113324=CARTESIAN_POINT('Ctrl Pts',(7.10826004677746,13.7778888548066,26.6317163275647));
#113325=CARTESIAN_POINT('Ctrl Pts',(7.05000000000001,13.85,26.6813466520527));
#113326=CARTESIAN_POINT('Origin',(6.71824230098391,14.,26.5266454963496));
#113327=CARTESIAN_POINT('',(6.71824230098391,13.85,26.5266454963496));
#113328=CARTESIAN_POINT('Ctrl Pts',(6.71824230098391,13.85,26.5266454963496));
#113329=CARTESIAN_POINT('Ctrl Pts',(6.71881249905978,13.7778888548067,26.4501139536144));
#113330=CARTESIAN_POINT('Ctrl Pts',(6.71942342556966,13.7,26.3681158721118));
#113331=CARTESIAN_POINT('',(6.71824230098391,12.1,26.5266454963496));
#113332=CARTESIAN_POINT('',(6.71824230098391,14.,26.5266454963496));
#113333=CARTESIAN_POINT('',(6.71824230098391,12.1,26.5266454963496));
#113334=CARTESIAN_POINT('Origin',(6.79519683323218,12.1,26.3152146566728));
#113335=CARTESIAN_POINT('',(7.0225021848062,12.1,26.158507039928));
#113336=CARTESIAN_POINT('Origin',(7.0225021848062,14.,26.158507039928));
#113337=CARTESIAN_POINT('Ctrl Pts',(6.81923838528667,13.7,26.4044455463833));
#113338=CARTESIAN_POINT('Ctrl Pts',(6.76699903133701,13.7778888548064,26.4676524170555));
#113339=CARTESIAN_POINT('Ctrl Pts',(6.71824230098391,13.85,26.5266454963496));
#113340=CARTESIAN_POINT('Origin',(6.36466117310055,14.,26.4319037186744));
#113341=CARTESIAN_POINT('',(6.36466117310056,13.85,26.4319037186744));
#113342=CARTESIAN_POINT('Ctrl Pts',(6.36466117310056,13.85,26.4319037186744));
#113343=CARTESIAN_POINT('Ctrl Pts',(6.35193314565639,13.7778888548065,26.3564358481817));
#113344=CARTESIAN_POINT('Ctrl Pts',(6.33829597339476,13.7,26.275577415511));
#113345=CARTESIAN_POINT('',(6.36466117310055,12.1,26.4319037186744));
#113346=CARTESIAN_POINT('',(6.36466117310055,14.,26.4319037186744));
#113347=CARTESIAN_POINT('',(6.36466117310055,12.1,26.4319037186744));
#113348=CARTESIAN_POINT('Origin',(6.40373201307562,12.1,26.2103219742466));
#113349=CARTESIAN_POINT('',(6.60037209353263,12.1,26.0165239382456));
#113350=CARTESIAN_POINT('Origin',(6.60037209353263,14.,26.0165239382456));
#113351=CARTESIAN_POINT('Ctrl Pts',(6.44290310132316,13.7,26.2940224745392));
#113352=CARTESIAN_POINT('Ctrl Pts',(6.40243313844953,13.7778888548062,26.3653403594364));
#113353=CARTESIAN_POINT('Ctrl Pts',(6.36466117310056,13.85,26.4319037186744));
#113354=CARTESIAN_POINT('Origin',(6.,14.,26.4));
#113355=CARTESIAN_POINT('',(6.,13.85,26.4));
#113356=CARTESIAN_POINT('Ctrl Pts',(6.,13.85,26.4));
#113357=CARTESIAN_POINT('Ctrl Pts',(5.97436048170878,13.7778888548059,26.3278888548059));
#113358=CARTESIAN_POINT('Ctrl Pts',(5.94688956925429,13.7,26.2506269135277));
#113359=CARTESIAN_POINT('',(6.,12.1,26.4));
#113360=CARTESIAN_POINT('',(6.,14.,26.4));
#113361=CARTESIAN_POINT('',(6.,12.1,26.4));
#113362=CARTESIAN_POINT('Origin',(6.,12.1,26.175));
#113363=CARTESIAN_POINT('',(6.16,12.1,25.95));
#113364=CARTESIAN_POINT('Origin',(6.16,14.,25.95));
#113365=CARTESIAN_POINT('Ctrl Pts',(6.05311043074571,13.7,26.2506269135277));
#113366=CARTESIAN_POINT('Ctrl Pts',(6.02563951829103,13.7778888548065,26.3278888548065));
#113367=CARTESIAN_POINT('Ctrl Pts',(6.,13.85,26.4));
#113368=CARTESIAN_POINT('Origin',(5.63533882689945,14.,26.4319037186744));
#113369=CARTESIAN_POINT('',(5.63533882689945,13.85,26.4319037186744));
#113370=CARTESIAN_POINT('Ctrl Pts',(5.63533882689945,13.85,26.4319037186744));
#113371=CARTESIAN_POINT('Ctrl Pts',(5.59756686155053,13.7778888548063,26.3653403594365));
#113372=CARTESIAN_POINT('Ctrl Pts',(5.55709689867685,13.7,26.2940224745392));
#113373=CARTESIAN_POINT('',(5.63533882689945,12.1,26.4319037186744));
#113374=CARTESIAN_POINT('',(5.63533882689945,14.,26.4319037186744));
#113375=CARTESIAN_POINT('',(5.63533882689945,12.1,26.4319037186744));
#113376=CARTESIAN_POINT('Origin',(5.59626798692439,12.1,26.2103219742466));
#113377=CARTESIAN_POINT('',(5.71476638743128,12.1,25.9609565213922));
#113378=CARTESIAN_POINT('Origin',(5.71476638743128,14.,25.9609565213922));
#113379=CARTESIAN_POINT('Ctrl Pts',(5.66170402660524,13.7,26.275577415511));
#113380=CARTESIAN_POINT('Ctrl Pts',(5.64806685434361,13.7778888548065,26.3564358481818));
#113381=CARTESIAN_POINT('Ctrl Pts',(5.63533882689945,13.85,26.4319037186744));
#113382=CARTESIAN_POINT('Origin',(5.28175769901609,14.,26.5266454963496));
#113383=CARTESIAN_POINT('',(5.28175769901609,13.85,26.5266454963496));
#113384=CARTESIAN_POINT('Ctrl Pts',(5.28175769901609,13.85,26.5266454963496));
#113385=CARTESIAN_POINT('Ctrl Pts',(5.23300096866302,13.7778888548065,26.4676524170555));
#113386=CARTESIAN_POINT('Ctrl Pts',(5.18076161471333,13.7,26.4044455463833));
#113387=CARTESIAN_POINT('',(5.28175769901609,12.1,26.5266454963496));
#113388=CARTESIAN_POINT('',(5.28175769901609,14.,26.5266454963496));
#113389=CARTESIAN_POINT('',(5.28175769901609,12.1,26.5266454963496));
#113390=CARTESIAN_POINT('Origin',(5.20480316676782,12.1,26.3152146566728));
#113391=CARTESIAN_POINT('',(5.27819945384529,12.1,26.0490605940638));
#113392=CARTESIAN_POINT('Origin',(5.27819945384529,14.,26.0490605940638));
#113393=CARTESIAN_POINT('Ctrl Pts',(5.28057657443035,13.7,26.3681158721118));
#113394=CARTESIAN_POINT('Ctrl Pts',(5.28118750094021,13.7778888548061,26.4501139536138));
#113395=CARTESIAN_POINT('Ctrl Pts',(5.28175769901609,13.85,26.5266454963496));
#113396=CARTESIAN_POINT('Origin',(4.95,14.,26.6813466520527));
#113397=CARTESIAN_POINT('',(4.95,13.85,26.6813466520527));
#113398=CARTESIAN_POINT('Ctrl Pts',(4.95,13.85,26.6813466520527));
#113399=CARTESIAN_POINT('Ctrl Pts',(4.89173995322247,13.7778888548066,26.6317163275647));
#113400=CARTESIAN_POINT('Ctrl Pts',(4.82931847453212,13.7,26.5785409798988));
#113401=CARTESIAN_POINT('',(4.95,12.1,26.6813466520527));
#113402=CARTESIAN_POINT('',(4.95,14.,26.6813466520527));
#113403=CARTESIAN_POINT('',(4.95,12.1,26.6813466520527));
#113404=CARTESIAN_POINT('Origin',(4.8375,12.1,26.4864909362012));
#113405=CARTESIAN_POINT('',(4.86356406460551,12.1,26.2116352203497));
#113406=CARTESIAN_POINT('Origin',(4.86356406460551,14.,26.2116352203497));
#113407=CARTESIAN_POINT('Ctrl Pts',(4.92130843899556,13.7,26.5254305491531));
#113408=CARTESIAN_POINT('Ctrl Pts',(4.936148901584,13.7778888548062,26.6060768092732));
#113409=CARTESIAN_POINT('Ctrl Pts',(4.95,13.85,26.6813466520527));
#113410=CARTESIAN_POINT('Origin',(4.65014601965827,14.,26.8913066694501));
#113411=CARTESIAN_POINT('',(4.65014601965827,13.85,26.8913066694501));
#113412=CARTESIAN_POINT('Ctrl Pts',(4.65014601965827,13.85,26.8913066694501));
#113413=CARTESIAN_POINT('Ctrl Pts',(4.58415285849654,13.7778888548066,26.8525470920636));
#113414=CARTESIAN_POINT('Ctrl Pts',(4.51344590010882,13.7,26.811018973435));
#113415=CARTESIAN_POINT('',(4.65014601965827,12.1,26.8913066694501));
#113416=CARTESIAN_POINT('',(4.65014601965827,14.,26.8913066694501));
#113417=CARTESIAN_POINT('',(4.65014601965827,12.1,26.8913066694501));
#113418=CARTESIAN_POINT('Origin',(4.50551880747879,12.1,26.7189466697484));
#113419=CARTESIAN_POINT('',(4.48345870619836,12.1,26.4437406524968));
#113420=CARTESIAN_POINT('Origin',(4.48345870619836,14.,26.4437406524968));
#113421=CARTESIAN_POINT('Ctrl Pts',(4.59481580079763,13.7,26.742741519778));
#113422=CARTESIAN_POINT('Ctrl Pts',(4.62343487951859,13.7778888548063,26.8195855627117));
#113423=CARTESIAN_POINT('Ctrl Pts',(4.65014601965827,13.85,26.8913066694502));
#113424=CARTESIAN_POINT('Origin',(4.39130666945015,14.,27.1501460196583));
#113425=CARTESIAN_POINT('',(4.39130666945015,13.85,27.1501460196583));
#113426=CARTESIAN_POINT('Ctrl Pts',(4.39130666945015,13.85,27.1501460196583));
#113427=CARTESIAN_POINT('Ctrl Pts',(4.31958556271188,13.7778888548065,27.1234348795187));
#113428=CARTESIAN_POINT('Ctrl Pts',(4.24274151977803,13.7,27.0948158007976));
#113429=CARTESIAN_POINT('',(4.39130666945015,12.1,27.1501460196583));
#113430=CARTESIAN_POINT('',(4.39130666945015,14.,27.1501460196583));
#113431=CARTESIAN_POINT('',(4.39130666945015,12.1,27.1501460196583));
#113432=CARTESIAN_POINT('Origin',(4.21894666974837,12.1,27.0055188074788));
#113433=CARTESIAN_POINT('',(4.14943268759645,12.1,26.7383244844003));
#113434=CARTESIAN_POINT('Origin',(4.14943268759645,14.,26.7383244844003));
#113435=CARTESIAN_POINT('Ctrl Pts',(4.31101897343495,13.7,27.0134459001088));
#113436=CARTESIAN_POINT('Ctrl Pts',(4.35254709206349,13.7778888548065,27.0841528584965));
#113437=CARTESIAN_POINT('Ctrl Pts',(4.39130666945015,13.85,27.1501460196583));
#113438=CARTESIAN_POINT('Origin',(4.18134665205268,14.,27.45));
#113439=CARTESIAN_POINT('',(4.18134665205268,13.85,27.45));
#113440=CARTESIAN_POINT('Ctrl Pts',(4.18134665205268,13.85,27.45));
#113441=CARTESIAN_POINT('Ctrl Pts',(4.10607680927348,13.7778888548064,27.436148901584));
#113442=CARTESIAN_POINT('Ctrl Pts',(4.0254305491531,13.7,27.4213084389956));
#113443=CARTESIAN_POINT('',(4.18134665205268,12.1,27.45));
#113444=CARTESIAN_POINT('',(4.18134665205268,14.,27.45));
#113445=CARTESIAN_POINT('',(4.18134665205268,12.1,27.45));
#113446=CARTESIAN_POINT('Origin',(3.98649093620118,12.1,27.3375));
#113447=CARTESIAN_POINT('',(3.87163522034968,12.1,27.0864359353945));
#113448=CARTESIAN_POINT('Origin',(3.87163522034968,14.,27.0864359353945));
#113449=CARTESIAN_POINT('Ctrl Pts',(4.07854097989881,13.7,27.3293184745321));
#113450=CARTESIAN_POINT('Ctrl Pts',(4.13171632756462,13.7778888548065,27.3917399532224));
#113451=CARTESIAN_POINT('Ctrl Pts',(4.18134665205268,13.85,27.45));
#113452=CARTESIAN_POINT('Origin',(4.02664549634959,14.,27.7817576990161));
#113453=CARTESIAN_POINT('',(4.02664549634959,13.85,27.7817576990161));
#113454=CARTESIAN_POINT('Ctrl Pts',(4.02664549634959,13.85,27.7817576990161));
#113455=CARTESIAN_POINT('Ctrl Pts',(3.95011395361384,13.7778888548062,27.7811875009402));
#113456=CARTESIAN_POINT('Ctrl Pts',(3.8681158721118,13.7,27.7805765744303));
#113457=CARTESIAN_POINT('',(4.02664549634959,12.1,27.7817576990161));
#113458=CARTESIAN_POINT('',(4.02664549634959,14.,27.7817576990161));
#113459=CARTESIAN_POINT('',(4.02664549634959,12.1,27.7817576990161));
#113460=CARTESIAN_POINT('Origin',(3.81521465667276,12.1,27.7048031667678));
#113461=CARTESIAN_POINT('',(3.65850703992804,12.1,27.4774978151938));
#113462=CARTESIAN_POINT('Origin',(3.65850703992804,14.,27.4774978151938));
#113463=CARTESIAN_POINT('Ctrl Pts',(3.90444554638328,13.7,27.6807616147133));
#113464=CARTESIAN_POINT('Ctrl Pts',(3.96765241705571,13.7778888548067,27.7330009686632));
#113465=CARTESIAN_POINT('Ctrl Pts',(4.02664549634959,13.85,27.7817576990161));
#113466=CARTESIAN_POINT('Origin',(3.93190371867436,14.,28.1353388268995));
#113467=CARTESIAN_POINT('',(3.93190371867436,13.85,28.1353388268995));
#113468=CARTESIAN_POINT('Ctrl Pts',(3.93190371867436,13.85,28.1353388268995));
#113469=CARTESIAN_POINT('Ctrl Pts',(3.85643584818165,13.7778888548064,28.1480668543436));
#113470=CARTESIAN_POINT('Ctrl Pts',(3.77557741551096,13.7,28.1617040266052));
#113471=CARTESIAN_POINT('',(3.93190371867436,12.1,28.1353388268995));
#113472=CARTESIAN_POINT('',(3.93190371867436,14.,28.1353388268995));
#113473=CARTESIAN_POINT('',(3.93190371867436,12.1,28.1353388268995));
#113474=CARTESIAN_POINT('Origin',(3.71032197424662,12.1,28.0962679869244));
#113475=CARTESIAN_POINT('',(3.51652393824558,12.1,27.8996279064674));
#113476=CARTESIAN_POINT('Origin',(3.51652393824558,14.,27.8996279064674));
#113477=CARTESIAN_POINT('Ctrl Pts',(3.79402247453916,13.7,28.0570968986768));
#113478=CARTESIAN_POINT('Ctrl Pts',(3.86534035943646,13.7778888548062,28.0975668615505));
#113479=CARTESIAN_POINT('Ctrl Pts',(3.93190371867436,13.85,28.1353388268995));
#113480=CARTESIAN_POINT('Origin',(3.9,14.,28.5));
#113481=CARTESIAN_POINT('',(3.9,13.85,28.5));
#113482=CARTESIAN_POINT('Ctrl Pts',(3.9,13.85,28.5));
#113483=CARTESIAN_POINT('Ctrl Pts',(3.82788885480655,13.7778888548065,28.525639518291));
#113484=CARTESIAN_POINT('Ctrl Pts',(3.75062691352768,13.7,28.5531104307457));
#113485=CARTESIAN_POINT('',(3.9,12.1,28.5));
#113486=CARTESIAN_POINT('',(3.9,14.,28.5));
#113487=CARTESIAN_POINT('',(3.9,12.1,28.5));
#113488=CARTESIAN_POINT('Origin',(3.675,12.1,28.5));
#113489=CARTESIAN_POINT('',(3.45,12.1,28.34));
#113490=CARTESIAN_POINT('Origin',(3.45,14.,28.34));
#113491=CARTESIAN_POINT('Ctrl Pts',(3.75062691352768,13.7,28.4468895692543));
#113492=CARTESIAN_POINT('Ctrl Pts',(3.82788885480652,13.7778888548065,28.474360481709));
#113493=CARTESIAN_POINT('Ctrl Pts',(3.9,13.85,28.5));
#113494=CARTESIAN_POINT('Origin',(3.93190371867437,14.,28.8646611731006));
#113495=CARTESIAN_POINT('',(3.93190371867437,13.85,28.8646611731006));
#113496=CARTESIAN_POINT('Ctrl Pts',(3.93190371867437,13.85,28.8646611731006));
#113497=CARTESIAN_POINT('Ctrl Pts',(3.86534035943652,13.7778888548063,28.9024331384495));
#113498=CARTESIAN_POINT('Ctrl Pts',(3.79402247453916,13.7,28.9429031013232));
#113499=CARTESIAN_POINT('',(3.93190371867437,12.1,28.8646611731006));
#113500=CARTESIAN_POINT('',(3.93190371867437,14.,28.8646611731006));
#113501=CARTESIAN_POINT('',(3.93190371867437,12.1,28.8646611731006));
#113502=CARTESIAN_POINT('Origin',(3.71032197424662,12.1,28.9037320130756));
#113503=CARTESIAN_POINT('',(3.46095652139216,12.1,28.7852336125687));
#113504=CARTESIAN_POINT('Origin',(3.46095652139216,14.,28.7852336125687));
#113505=CARTESIAN_POINT('Ctrl Pts',(3.77557741551096,13.7,28.8382959733948));
#113506=CARTESIAN_POINT('Ctrl Pts',(3.8564358481818,13.7778888548066,28.8519331456564));
#113507=CARTESIAN_POINT('Ctrl Pts',(3.93190371867437,13.85,28.8646611731006));
#113508=CARTESIAN_POINT('Origin',(4.02664549634959,14.,29.2182423009839));
#113509=CARTESIAN_POINT('',(4.02664549634959,13.85,29.2182423009839));
#113510=CARTESIAN_POINT('Ctrl Pts',(4.02664549634959,13.85,29.2182423009839));
#113511=CARTESIAN_POINT('Ctrl Pts',(3.96765241705536,13.7778888548063,29.2669990313371));
#113512=CARTESIAN_POINT('Ctrl Pts',(3.90444554638327,13.7,29.3192383852867));
#113513=CARTESIAN_POINT('',(4.02664549634959,12.1,29.2182423009839));
#113514=CARTESIAN_POINT('',(4.02664549634959,14.,29.2182423009839));
#113515=CARTESIAN_POINT('',(4.02664549634959,12.1,29.2182423009839));
#113516=CARTESIAN_POINT('Origin',(3.81521465667276,12.1,29.2951968332322));
#113517=CARTESIAN_POINT('',(3.54906059406382,12.1,29.2218005461547));
#113518=CARTESIAN_POINT('Origin',(3.54906059406382,14.,29.2218005461547));
#113519=CARTESIAN_POINT('Ctrl Pts',(3.8681158721118,13.7,29.2194234255697));
#113520=CARTESIAN_POINT('Ctrl Pts',(3.95011395361416,13.7778888548065,29.2188124990598));
#113521=CARTESIAN_POINT('Ctrl Pts',(4.02664549634959,13.85,29.2182423009839));
#113522=CARTESIAN_POINT('Origin',(4.18134665205268,14.,29.55));
#113523=CARTESIAN_POINT('',(4.18134665205268,13.85,29.55));
#113524=CARTESIAN_POINT('Ctrl Pts',(4.18134665205268,13.85,29.55));
#113525=CARTESIAN_POINT('Ctrl Pts',(4.1317163275649,13.7778888548069,29.6082600467773));
#113526=CARTESIAN_POINT('Ctrl Pts',(4.07854097989881,13.7,29.6706815254679));
#113527=CARTESIAN_POINT('',(4.18134665205268,12.1,29.55));
#113528=CARTESIAN_POINT('',(4.18134665205268,14.,29.55));
#113529=CARTESIAN_POINT('',(4.18134665205268,12.1,29.55));
#113530=CARTESIAN_POINT('Origin',(3.98649093620118,12.1,29.6625));
#113531=CARTESIAN_POINT('',(3.71163522034968,12.1,29.6364359353945));
#113532=CARTESIAN_POINT('Origin',(3.71163522034968,14.,29.6364359353945));
#113533=CARTESIAN_POINT('Ctrl Pts',(4.02543054915311,13.7,29.5786915610044));
#113534=CARTESIAN_POINT('Ctrl Pts',(4.1060768092734,13.7778888548063,29.563851098416));
#113535=CARTESIAN_POINT('Ctrl Pts',(4.18134665205268,13.85,29.55));
#113536=CARTESIAN_POINT('Origin',(4.39130666945015,14.,29.8498539803417));
#113537=CARTESIAN_POINT('',(4.39130666945015,13.85,29.8498539803417));
#113538=CARTESIAN_POINT('Ctrl Pts',(4.39130666945015,13.85,29.8498539803417));
#113539=CARTESIAN_POINT('Ctrl Pts',(4.35254709206352,13.7778888548065,29.9158471415035));
#113540=CARTESIAN_POINT('Ctrl Pts',(4.31101897343496,13.7,29.9865540998912));
#113541=CARTESIAN_POINT('',(4.39130666945015,12.1,29.8498539803417));
#113542=CARTESIAN_POINT('',(4.39130666945015,14.,29.8498539803417));
#113543=CARTESIAN_POINT('',(4.39130666945015,12.1,29.8498539803417));
#113544=CARTESIAN_POINT('Origin',(4.21894666974838,12.1,29.9944811925212));
#113545=CARTESIAN_POINT('',(3.94374065249676,12.1,30.0165412938016));
#113546=CARTESIAN_POINT('Origin',(3.94374065249676,14.,30.0165412938016));
#113547=CARTESIAN_POINT('Ctrl Pts',(4.24274151977804,13.7,29.9051841992024));
#113548=CARTESIAN_POINT('Ctrl Pts',(4.31958556271157,13.7778888548062,29.8765651204815));
#113549=CARTESIAN_POINT('Ctrl Pts',(4.39130666945015,13.85,29.8498539803417));
#113550=CARTESIAN_POINT('Origin',(4.65014601965827,14.,30.1086933305499));
#113551=CARTESIAN_POINT('',(4.65014601965827,13.85,30.1086933305499));
#113552=CARTESIAN_POINT('Ctrl Pts',(4.65014601965827,13.85,30.1086933305499));
#113553=CARTESIAN_POINT('Ctrl Pts',(4.62343487951865,13.7778888548065,30.1804144372881));
#113554=CARTESIAN_POINT('Ctrl Pts',(4.59481580079763,13.7,30.257258480222));
#113555=CARTESIAN_POINT('',(4.65014601965827,12.1,30.1086933305499));
#113556=CARTESIAN_POINT('',(4.65014601965827,14.,30.1086933305499));
#113557=CARTESIAN_POINT('',(4.65014601965827,12.1,30.1086933305499));
#113558=CARTESIAN_POINT('Origin',(4.50551880747879,12.1,30.2810533302516));
#113559=CARTESIAN_POINT('',(4.23832448440029,12.1,30.3505673124035));
#113560=CARTESIAN_POINT('Origin',(4.23832448440029,14.,30.3505673124035));
#113561=CARTESIAN_POINT('Ctrl Pts',(4.51344590010882,13.7,30.188981026565));
#113562=CARTESIAN_POINT('Ctrl Pts',(4.58415285849637,13.7778888548064,30.1474529079366));
#113563=CARTESIAN_POINT('Ctrl Pts',(4.65014601965827,13.85,30.1086933305499));
#113564=CARTESIAN_POINT('Origin',(4.95,14.,30.3186533479473));
#113565=CARTESIAN_POINT('',(4.95,13.85,30.3186533479473));
#113566=CARTESIAN_POINT('Ctrl Pts',(4.95,13.85,30.3186533479473));
#113567=CARTESIAN_POINT('Ctrl Pts',(4.93614890158408,13.7778888548066,30.3939231907263));
#113568=CARTESIAN_POINT('Ctrl Pts',(4.92130843899556,13.7,30.4745694508469));
#113569=CARTESIAN_POINT('',(4.95,12.1,30.3186533479473));
#113570=CARTESIAN_POINT('',(4.95,14.,30.3186533479473));
#113571=CARTESIAN_POINT('',(4.95,12.1,30.3186533479473));
#113572=CARTESIAN_POINT('Origin',(4.8375,12.1,30.5135090637988));
#113573=CARTESIAN_POINT('',(4.5864359353945,12.1,30.6283647796503));
#113574=CARTESIAN_POINT('Origin',(4.5864359353945,14.,30.6283647796503));
#113575=CARTESIAN_POINT('Ctrl Pts',(4.82931847453212,13.7,30.4214590201012));
#113576=CARTESIAN_POINT('Ctrl Pts',(4.89173995322246,13.7778888548065,30.3682836724353));
#113577=CARTESIAN_POINT('Ctrl Pts',(4.95,13.85,30.3186533479473));
#113578=CARTESIAN_POINT('Origin',(5.2817576990161,14.,30.4733545036504));
#113579=CARTESIAN_POINT('',(5.2817576990161,13.85,30.4733545036504));
#113580=CARTESIAN_POINT('Ctrl Pts',(5.2817576990161,13.85,30.4733545036504));
#113581=CARTESIAN_POINT('Ctrl Pts',(5.28118750094022,13.7778888548068,30.5498860463855));
#113582=CARTESIAN_POINT('Ctrl Pts',(5.28057657443035,13.7,30.6318841278882));
#113583=CARTESIAN_POINT('',(5.2817576990161,12.1,30.4733545036504));
#113584=CARTESIAN_POINT('',(5.2817576990161,14.,30.4733545036504));
#113585=CARTESIAN_POINT('',(5.2817576990161,12.1,30.4733545036504));
#113586=CARTESIAN_POINT('Origin',(5.20480316676782,12.1,30.6847853433272));
#113587=CARTESIAN_POINT('',(4.97749781519381,12.1,30.841492960072));
#113588=CARTESIAN_POINT('Origin',(4.97749781519381,14.,30.841492960072));
#113589=CARTESIAN_POINT('Ctrl Pts',(5.18076161471333,13.7,30.5955544536167));
#113590=CARTESIAN_POINT('Ctrl Pts',(5.23300096866312,13.7778888548066,30.5323475829444));
#113591=CARTESIAN_POINT('Ctrl Pts',(5.2817576990161,13.85,30.4733545036504));
#113592=CARTESIAN_POINT('Origin',(5.63533882689945,14.,30.5680962813256));
#113593=CARTESIAN_POINT('',(5.63533882689945,13.85,30.5680962813256));
#113594=CARTESIAN_POINT('Ctrl Pts',(5.63533882689945,13.85,30.5680962813256));
#113595=CARTESIAN_POINT('Ctrl Pts',(5.64806685434359,13.7778888548066,30.6435641518181));
#113596=CARTESIAN_POINT('Ctrl Pts',(5.66170402660524,13.7,30.724422584489));
#113597=CARTESIAN_POINT('',(5.63533882689945,12.1,30.5680962813256));
#113598=CARTESIAN_POINT('',(5.63533882689945,14.,30.5680962813256));
#113599=CARTESIAN_POINT('',(5.63533882689945,12.1,30.5680962813256));
#113600=CARTESIAN_POINT('Origin',(5.59626798692439,12.1,30.7896780257534));
#113601=CARTESIAN_POINT('',(5.39962790646737,12.1,30.9834760617544));
#113602=CARTESIAN_POINT('Origin',(5.39962790646737,14.,30.9834760617544));
#113603=CARTESIAN_POINT('Ctrl Pts',(5.55709689867685,13.7,30.7059775254608));
#113604=CARTESIAN_POINT('Ctrl Pts',(5.59756686155053,13.7778888548063,30.6346596405635));
#113605=CARTESIAN_POINT('Ctrl Pts',(5.63533882689945,13.85,30.5680962813256));
#113606=CARTESIAN_POINT('Origin',(6.,14.,30.6));
#113607=CARTESIAN_POINT('',(6.,13.85,30.6));
#113608=CARTESIAN_POINT('Ctrl Pts',(6.,13.85,30.6));
#113609=CARTESIAN_POINT('Ctrl Pts',(6.02563951829106,13.7778888548064,30.6721111451936));
#113610=CARTESIAN_POINT('Ctrl Pts',(6.05311043074571,13.7,30.7493730864723));
#113611=CARTESIAN_POINT('',(6.,12.1,30.6));
#113612=CARTESIAN_POINT('',(6.,14.,30.6));
#113613=CARTESIAN_POINT('',(6.,12.1,30.6));
#113614=CARTESIAN_POINT('Origin',(6.,12.1,30.825));
#113615=CARTESIAN_POINT('',(5.84,12.1,31.05));
#113616=CARTESIAN_POINT('Origin',(5.84,14.,31.05));
#113617=CARTESIAN_POINT('Ctrl Pts',(5.94688956925429,13.7,30.7493730864723));
#113618=CARTESIAN_POINT('Ctrl Pts',(5.97436048170889,13.7778888548063,30.6721111451937));
#113619=CARTESIAN_POINT('Ctrl Pts',(6.,13.85,30.6));
#113620=CARTESIAN_POINT('Origin',(6.36466117310055,14.,30.5680962813256));
#113621=CARTESIAN_POINT('',(6.36466117310056,13.85,30.5680962813256));
#113622=CARTESIAN_POINT('Ctrl Pts',(6.36466117310056,13.85,30.5680962813256));
#113623=CARTESIAN_POINT('Ctrl Pts',(6.40243313844958,13.7778888548061,30.6346596405636));
#113624=CARTESIAN_POINT('Ctrl Pts',(6.44290310132316,13.7,30.7059775254608));
#113625=CARTESIAN_POINT('',(6.36466117310055,12.1,30.5680962813256));
#113626=CARTESIAN_POINT('',(6.36466117310055,14.,30.5680962813256));
#113627=CARTESIAN_POINT('',(6.36466117310055,12.1,30.5680962813256));
#113628=CARTESIAN_POINT('Origin',(6.40373201307562,12.1,30.7896780257534));
#113629=CARTESIAN_POINT('',(6.28523361256872,12.1,31.0390434786078));
#113630=CARTESIAN_POINT('Origin',(6.28523361256872,14.,31.0390434786078));
#113631=CARTESIAN_POINT('Ctrl Pts',(6.33829597339476,13.7,30.724422584489));
#113632=CARTESIAN_POINT('Ctrl Pts',(6.35193314565637,13.7778888548064,30.6435641518184));
#113633=CARTESIAN_POINT('Ctrl Pts',(6.36466117310056,13.85,30.5680962813256));
#113634=CARTESIAN_POINT('Origin',(6.71824230098391,14.,30.4733545036504));
#113635=CARTESIAN_POINT('',(6.71824230098391,13.85,30.4733545036504));
#113636=CARTESIAN_POINT('Ctrl Pts',(6.71824230098391,13.85,30.4733545036504));
#113637=CARTESIAN_POINT('Ctrl Pts',(6.76699903133736,13.7778888548059,30.532347582945));
#113638=CARTESIAN_POINT('Ctrl Pts',(6.81923838528667,13.7,30.5955544536167));
#113639=CARTESIAN_POINT('',(6.71824230098391,12.1,30.4733545036504));
#113640=CARTESIAN_POINT('',(6.71824230098391,14.,30.4733545036504));
#113641=CARTESIAN_POINT('',(6.71824230098391,12.1,30.4733545036504));
#113642=CARTESIAN_POINT('Origin',(6.79519683323218,12.1,30.6847853433272));
#113643=CARTESIAN_POINT('',(6.72180054615471,12.1,30.9509394059362));
#113644=CARTESIAN_POINT('Origin',(6.72180054615471,14.,30.9509394059362));
#113645=CARTESIAN_POINT('Ctrl Pts',(6.71942342556966,13.7,30.6318841278882));
#113646=CARTESIAN_POINT('Ctrl Pts',(6.71881249905979,13.7778888548063,30.5498860463861));
#113647=CARTESIAN_POINT('Ctrl Pts',(6.71824230098391,13.85,30.4733545036504));
#113648=CARTESIAN_POINT('Origin',(7.05000000000001,14.,30.3186533479473));
#113649=CARTESIAN_POINT('',(7.05000000000001,13.85,30.3186533479473));
#113650=CARTESIAN_POINT('Ctrl Pts',(7.05000000000001,13.85,30.3186533479473));
#113651=CARTESIAN_POINT('Ctrl Pts',(7.10826004677755,13.7778888548065,30.3682836724353));
#113652=CARTESIAN_POINT('Ctrl Pts',(7.17068152546789,13.7,30.4214590201012));
#113653=CARTESIAN_POINT('',(7.05000000000001,12.1,30.3186533479473));
#113654=CARTESIAN_POINT('',(7.05000000000001,14.,30.3186533479473));
#113655=CARTESIAN_POINT('',(7.05000000000001,12.1,30.3186533479473));
#113656=CARTESIAN_POINT('Origin',(7.1625,12.1,30.5135090637988));
#113657=CARTESIAN_POINT('',(7.13643593539449,12.1,30.7883647796503));
#113658=CARTESIAN_POINT('Origin',(7.13643593539449,14.,30.7883647796503));
#113659=CARTESIAN_POINT('Ctrl Pts',(7.07869156100444,13.7,30.4745694508469));
#113660=CARTESIAN_POINT('Ctrl Pts',(7.06385109841591,13.7778888548066,30.3939231907262));
#113661=CARTESIAN_POINT('Ctrl Pts',(7.05000000000001,13.85,30.3186533479473));
#113662=CARTESIAN_POINT('Origin',(7.34985398034173,14.,30.1086933305499));
#113663=CARTESIAN_POINT('',(7.34985398034173,13.85,30.1086933305499));
#113664=CARTESIAN_POINT('Ctrl Pts',(7.34985398034173,13.85,30.1086933305499));
#113665=CARTESIAN_POINT('Ctrl Pts',(7.41584714150318,13.7778888548069,30.1474529079363));
#113666=CARTESIAN_POINT('Ctrl Pts',(7.48655409989118,13.7,30.188981026565));
#113667=CARTESIAN_POINT('',(7.34985398034173,12.1,30.1086933305499));
#113668=CARTESIAN_POINT('',(7.34985398034173,14.,30.1086933305499));
#113669=CARTESIAN_POINT('',(7.34985398034173,12.1,30.1086933305499));
#113670=CARTESIAN_POINT('Origin',(7.4944811925212,12.1,30.2810533302516));
#113671=CARTESIAN_POINT('',(7.51654129380164,12.1,30.5562593475032));
#113672=CARTESIAN_POINT('Origin',(7.51654129380164,14.,30.5562593475032));
#113673=CARTESIAN_POINT('Ctrl Pts',(7.40518419920237,13.7,30.257258480222));
#113674=CARTESIAN_POINT('Ctrl Pts',(7.3765651204814,13.7778888548063,30.1804144372883));
#113675=CARTESIAN_POINT('Ctrl Pts',(7.34985398034173,13.85,30.1086933305499));
#113676=CARTESIAN_POINT('Origin',(7.60869333054985,14.,29.8498539803417));
#113677=CARTESIAN_POINT('',(7.60869333054985,13.85,29.8498539803417));
#113678=CARTESIAN_POINT('Ctrl Pts',(7.60869333054985,13.85,29.8498539803417));
#113679=CARTESIAN_POINT('Ctrl Pts',(7.6804144372882,13.7778888548064,29.8765651204814));
#113680=CARTESIAN_POINT('Ctrl Pts',(7.75725848022197,13.7,29.9051841992024));
#113681=CARTESIAN_POINT('',(7.60869333054985,12.1,29.8498539803417));
#113682=CARTESIAN_POINT('',(7.60869333054985,14.,29.8498539803417));
#113683=CARTESIAN_POINT('',(7.60869333054985,12.1,29.8498539803417));
#113684=CARTESIAN_POINT('Origin',(7.78105333025163,12.1,29.9944811925212));
#113685=CARTESIAN_POINT('',(7.85056731240355,12.1,30.2616755155997));
#113686=CARTESIAN_POINT('Origin',(7.85056731240355,14.,30.2616755155997));
#113687=CARTESIAN_POINT('Ctrl Pts',(7.68898102656505,13.7,29.9865540998912));
#113688=CARTESIAN_POINT('Ctrl Pts',(7.64745290793635,13.7778888548067,29.9158471415033));
#113689=CARTESIAN_POINT('Ctrl Pts',(7.60869333054985,13.85,29.8498539803417));
#113690=CARTESIAN_POINT('Origin',(7.81865334794732,14.,29.55));
#113691=CARTESIAN_POINT('',(7.81865334794732,13.85,29.55));
#113692=CARTESIAN_POINT('Ctrl Pts',(7.81865334794732,13.85,29.55));
#113693=CARTESIAN_POINT('Ctrl Pts',(7.89392319072661,13.7778888548063,29.563851098416));
#113694=CARTESIAN_POINT('Ctrl Pts',(7.9745694508469,13.7,29.5786915610044));
#113695=CARTESIAN_POINT('',(7.81865334794732,12.1,29.55));
#113696=CARTESIAN_POINT('',(7.81865334794732,14.,29.55));
#113697=CARTESIAN_POINT('',(7.81865334794732,12.1,29.55));
#113698=CARTESIAN_POINT('Origin',(8.01350906379882,12.1,29.6625));
#113699=CARTESIAN_POINT('',(8.12836477965032,12.1,29.9135640646055));
#113700=CARTESIAN_POINT('Origin',(8.12836477965032,14.,29.9135640646055));
#113701=CARTESIAN_POINT('Ctrl Pts',(7.92145902010118,13.7,29.6706815254679));
#113702=CARTESIAN_POINT('Ctrl Pts',(7.86828367243554,13.7778888548062,29.6082600467778));
#113703=CARTESIAN_POINT('Ctrl Pts',(7.81865334794732,13.85,29.55));
#113704=CARTESIAN_POINT('Origin',(7.97335450365041,14.,29.2182423009839));
#113705=CARTESIAN_POINT('',(7.97335450365041,13.85,29.2182423009839));
#113706=CARTESIAN_POINT('Ctrl Pts',(7.97335450365041,13.85,29.2182423009839));
#113707=CARTESIAN_POINT('Ctrl Pts',(8.04988604638594,13.7778888548064,29.2188124990598));
#113708=CARTESIAN_POINT('Ctrl Pts',(8.1318841278882,13.7,29.2194234255697));
#113709=CARTESIAN_POINT('',(7.97335450365041,12.1,29.2182423009839));
#113710=CARTESIAN_POINT('',(7.97335450365041,14.,29.2182423009839));
#113711=CARTESIAN_POINT('',(7.97335450365041,12.1,29.2182423009839));
#113712=CARTESIAN_POINT('Origin',(8.18478534332724,12.1,29.2951968332322));
#113713=CARTESIAN_POINT('',(8.34149296007196,12.1,29.5225021848062));
#113714=CARTESIAN_POINT('Origin',(8.34149296007196,14.,29.5225021848062));
#113715=CARTESIAN_POINT('Ctrl Pts',(8.09555445361673,13.7,29.3192383852867));
#113716=CARTESIAN_POINT('Ctrl Pts',(8.03234758294446,13.7778888548065,29.2669990313369));
#113717=CARTESIAN_POINT('Ctrl Pts',(7.97335450365041,13.85,29.2182423009839));
#113718=CARTESIAN_POINT('Origin',(8.06809628132564,14.,28.8646611731006));
#113719=CARTESIAN_POINT('',(8.06809628132564,13.85,28.8646611731006));
#113720=CARTESIAN_POINT('Ctrl Pts',(8.06809628132564,13.85,28.8646611731006));
#113721=CARTESIAN_POINT('Ctrl Pts',(8.1435641518183,13.7778888548065,28.8519331456564));
#113722=CARTESIAN_POINT('Ctrl Pts',(8.22442258448904,13.7,28.8382959733948));
#113723=CARTESIAN_POINT('',(8.06809628132564,12.1,28.8646611731006));
#113724=CARTESIAN_POINT('',(8.06809628132564,14.,28.8646611731006));
#113725=CARTESIAN_POINT('',(8.06809628132564,12.1,28.8646611731006));
#113726=CARTESIAN_POINT('Origin',(8.28967802575338,12.1,28.9037320130756));
#113727=CARTESIAN_POINT('',(8.48347606175442,12.1,29.1003720935326));
#113728=CARTESIAN_POINT('Origin',(8.48347606175442,14.,29.1003720935326));
#113729=CARTESIAN_POINT('Ctrl Pts',(8.20597752546084,13.7,28.9429031013232));
#113730=CARTESIAN_POINT('Ctrl Pts',(8.13465964056348,13.7778888548063,28.9024331384495));
#113731=CARTESIAN_POINT('Ctrl Pts',(8.06809628132564,13.85,28.8646611731006));
#113732=CARTESIAN_POINT('Origin',(8.1,14.,28.5));
#113733=CARTESIAN_POINT('',(8.1,13.85,28.5));
#113734=CARTESIAN_POINT('Ctrl Pts',(8.1,13.85,28.5));
#113735=CARTESIAN_POINT('Ctrl Pts',(8.17211114519331,13.7778888548067,28.474360481709));
#113736=CARTESIAN_POINT('Ctrl Pts',(8.24937308647232,13.7,28.4468895692543));
#113737=CARTESIAN_POINT('',(8.1,12.1,28.5));
#113738=CARTESIAN_POINT('',(8.1,14.,28.5));
#113739=CARTESIAN_POINT('',(8.1,12.1,28.5));
#113740=CARTESIAN_POINT('Origin',(8.325,12.1,28.5));
#113741=CARTESIAN_POINT('',(8.55,12.1,28.66));
#113742=CARTESIAN_POINT('Origin',(8.55,14.,28.66));
#113743=CARTESIAN_POINT('Ctrl Pts',(8.24937308647232,13.7,28.5531104307457));
#113744=CARTESIAN_POINT('Ctrl Pts',(8.17211114519331,13.7778888548067,28.525639518291));
#113745=CARTESIAN_POINT('Ctrl Pts',(8.1,13.85,28.5));
#113746=CARTESIAN_POINT('Origin',(6.,11.7,28.5));
#113747=CARTESIAN_POINT('Origin',(6.,11.7,26.45));
#113748=CARTESIAN_POINT('Origin',(6.,13.85,28.5));
#113749=CARTESIAN_POINT('',(4.05,14.,28.5));
#113750=CARTESIAN_POINT('Origin',(6.,14.,28.5));
#113751=CARTESIAN_POINT('',(3.9,13.85,28.5));
#113752=CARTESIAN_POINT('Origin',(6.,14.,28.5));
#113753=CARTESIAN_POINT('',(4.69529946162075,14.,28.5));
#113754=CARTESIAN_POINT('Origin',(6.,14.,28.5));
#113755=CARTESIAN_POINT('Origin',(6.,13.9,28.5));
#113756=CARTESIAN_POINT('',(4.84529946162075,13.85,28.5));
#113757=CARTESIAN_POINT('',(4.79529946162075,13.9,28.5));
#113758=CARTESIAN_POINT('',(4.89926025947012,13.8,28.4065371565079));
#113759=CARTESIAN_POINT('Ctrl Pts',(4.89926025947012,13.8,28.4065371565079));
#113760=CARTESIAN_POINT('Ctrl Pts',(4.87287693025568,13.8224225313651,28.4522344231802));
#113761=CARTESIAN_POINT('Ctrl Pts',(4.84529946162075,13.85,28.5));
#113762=CARTESIAN_POINT('',(5.368688932961,13.8,27.5934628434921));
#113763=CARTESIAN_POINT('Origin',(6.,13.8,28.5));
#113764=CARTESIAN_POINT('',(5.42264973081037,13.85,27.5));
#113765=CARTESIAN_POINT('Ctrl Pts',(5.42264973081037,13.85,27.5));
#113766=CARTESIAN_POINT('Ctrl Pts',(5.39507226217544,13.8224225313651,27.5477655768198));
#113767=CARTESIAN_POINT('Ctrl Pts',(5.368688932961,13.8,27.5934628434921));
#113768=CARTESIAN_POINT('',(5.53057132650912,13.8,27.5));
#113769=CARTESIAN_POINT('Ctrl Pts',(5.53057132650913,13.8,27.5));
#113770=CARTESIAN_POINT('Ctrl Pts',(5.47780466808023,13.8224225313651,27.5));
#113771=CARTESIAN_POINT('Ctrl Pts',(5.42264973081037,13.85,27.5));
#113772=CARTESIAN_POINT('',(6.46942867349088,13.8,27.5));
#113773=CARTESIAN_POINT('Origin',(6.,13.8,28.5));
#113774=CARTESIAN_POINT('',(6.57735026918963,13.85,27.5));
#113775=CARTESIAN_POINT('Ctrl Pts',(6.57735026918963,13.85,27.5));
#113776=CARTESIAN_POINT('Ctrl Pts',(6.52219533191977,13.8224225313651,27.5));
#113777=CARTESIAN_POINT('Ctrl Pts',(6.46942867349087,13.8,27.5));
#113778=CARTESIAN_POINT('',(6.631311067039,13.8,27.5934628434921));
#113779=CARTESIAN_POINT('Ctrl Pts',(6.631311067039,13.8,27.5934628434921));
#113780=CARTESIAN_POINT('Ctrl Pts',(6.60492773782455,13.8224225313651,27.5477655768198));
#113781=CARTESIAN_POINT('Ctrl Pts',(6.57735026918963,13.85,27.5));
#113782=CARTESIAN_POINT('',(7.10073974052988,13.8,28.4065371565079));
#113783=CARTESIAN_POINT('Origin',(6.,13.8,28.5));
#113784=CARTESIAN_POINT('',(7.15470053837925,13.85,28.5));
#113785=CARTESIAN_POINT('Ctrl Pts',(7.15470053837925,13.85,28.5));
#113786=CARTESIAN_POINT('Ctrl Pts',(7.12712306974432,13.8224225313651,28.4522344231802));
#113787=CARTESIAN_POINT('Ctrl Pts',(7.10073974052988,13.8,28.4065371565079));
#113788=CARTESIAN_POINT('',(7.10073974052988,13.8,28.5934628434921));
#113789=CARTESIAN_POINT('Ctrl Pts',(7.10073974052988,13.8,28.5934628434921));
#113790=CARTESIAN_POINT('Ctrl Pts',(7.12712306974432,13.8224225313651,28.5477655768198));
#113791=CARTESIAN_POINT('Ctrl Pts',(7.15470053837925,13.85,28.5));
#113792=CARTESIAN_POINT('',(6.631311067039,13.8,29.4065371565079));
#113793=CARTESIAN_POINT('Origin',(6.,13.8,28.5));
#113794=CARTESIAN_POINT('',(6.57735026918963,13.85,29.5));
#113795=CARTESIAN_POINT('Ctrl Pts',(6.57735026918963,13.85,29.5));
#113796=CARTESIAN_POINT('Ctrl Pts',(6.60492773782455,13.8224225313651,29.4522344231802));
#113797=CARTESIAN_POINT('Ctrl Pts',(6.631311067039,13.8,29.4065371565079));
#113798=CARTESIAN_POINT('',(6.46942867349088,13.8,29.5));
#113799=CARTESIAN_POINT('Ctrl Pts',(6.46942867349087,13.8,29.5));
#113800=CARTESIAN_POINT('Ctrl Pts',(6.52219533191977,13.8224225313651,29.5));
#113801=CARTESIAN_POINT('Ctrl Pts',(6.57735026918963,13.85,29.5));
#113802=CARTESIAN_POINT('',(5.53057132650912,13.8,29.5));
#113803=CARTESIAN_POINT('Origin',(6.,13.8,28.5));
#113804=CARTESIAN_POINT('',(5.42264973081037,13.85,29.5));
#113805=CARTESIAN_POINT('Ctrl Pts',(5.42264973081037,13.85,29.5));
#113806=CARTESIAN_POINT('Ctrl Pts',(5.47780466808023,13.8224225313651,29.5));
#113807=CARTESIAN_POINT('Ctrl Pts',(5.53057132650913,13.8,29.5));
#113808=CARTESIAN_POINT('',(5.368688932961,13.8,29.4065371565079));
#113809=CARTESIAN_POINT('Ctrl Pts',(5.368688932961,13.8,29.4065371565079));
#113810=CARTESIAN_POINT('Ctrl Pts',(5.39507226217544,13.8224225313651,29.4522344231802));
#113811=CARTESIAN_POINT('Ctrl Pts',(5.42264973081037,13.85,29.5));
#113812=CARTESIAN_POINT('',(4.89926025947012,13.8,28.5934628434921));
#113813=CARTESIAN_POINT('Origin',(6.,13.8,28.5));
#113814=CARTESIAN_POINT('Ctrl Pts',(4.84529946162075,13.85,28.5));
#113815=CARTESIAN_POINT('Ctrl Pts',(4.87287693025568,13.8224225313651,28.5477655768198));
#113816=CARTESIAN_POINT('Ctrl Pts',(4.89926025947012,13.8,28.5934628434921));
#113817=CARTESIAN_POINT('Origin',(6.,13.9,28.5));
#113818=CARTESIAN_POINT('',(6.46942867349088,14.,27.5));
#113819=CARTESIAN_POINT('',(6.46942867349088,13.9,27.5));
#113820=CARTESIAN_POINT('',(5.53057132650912,14.,27.5));
#113821=CARTESIAN_POINT('',(5.53057132650912,13.9,27.5));
#113822=CARTESIAN_POINT('Origin',(6.,14.,28.5));
#113823=CARTESIAN_POINT('Origin',(6.,13.9,28.5));
#113824=CARTESIAN_POINT('',(7.10073974052988,14.,28.4065371565079));
#113825=CARTESIAN_POINT('',(7.10073974052988,13.9,28.4065371565079));
#113826=CARTESIAN_POINT('',(6.631311067039,14.,27.5934628434921));
#113827=CARTESIAN_POINT('',(6.631311067039,13.9,27.5934628434921));
#113828=CARTESIAN_POINT('Origin',(6.,14.,28.5));
#113829=CARTESIAN_POINT('Origin',(6.,13.9,28.5));
#113830=CARTESIAN_POINT('',(4.89926025947012,14.,28.4065371565079));
#113831=CARTESIAN_POINT('',(4.89926025947012,13.9,28.4065371565079));
#113832=CARTESIAN_POINT('',(5.368688932961,14.,27.5934628434921));
#113833=CARTESIAN_POINT('Origin',(6.,14.,28.5));
#113834=CARTESIAN_POINT('',(5.368688932961,13.9,27.5934628434921));
#113835=CARTESIAN_POINT('Origin',(6.,13.9,28.5));
#113836=CARTESIAN_POINT('',(6.631311067039,14.,29.4065371565079));
#113837=CARTESIAN_POINT('',(6.631311067039,13.9,29.4065371565079));
#113838=CARTESIAN_POINT('',(7.10073974052988,14.,28.5934628434921));
#113839=CARTESIAN_POINT('',(7.10073974052988,13.9,28.5934628434921));
#113840=CARTESIAN_POINT('Origin',(6.,14.,28.5));
#113841=CARTESIAN_POINT('Origin',(6.,13.9,28.5));
#113842=CARTESIAN_POINT('',(5.368688932961,14.,29.4065371565079));
#113843=CARTESIAN_POINT('',(5.368688932961,13.9,29.4065371565079));
#113844=CARTESIAN_POINT('',(4.89926025947012,14.,28.5934628434921));
#113845=CARTESIAN_POINT('Origin',(6.,14.,28.5));
#113846=CARTESIAN_POINT('',(4.89926025947012,13.9,28.5934628434921));
#113847=CARTESIAN_POINT('Origin',(6.,13.9,28.5));
#113848=CARTESIAN_POINT('',(6.46942867349088,14.,29.5));
#113849=CARTESIAN_POINT('',(6.46942867349088,13.9,29.5));
#113850=CARTESIAN_POINT('',(5.53057132650912,14.,29.5));
#113851=CARTESIAN_POINT('Origin',(6.,14.,28.5));
#113852=CARTESIAN_POINT('',(5.53057132650912,13.9,29.5));
#113853=CARTESIAN_POINT('Origin',(7.15470053837925,14.,28.5));
#113854=CARTESIAN_POINT('',(7.01036297108184,14.,28.75));
#113855=CARTESIAN_POINT('',(7.15470053837925,12.9,28.5));
#113856=CARTESIAN_POINT('',(7.15470053837925,14.,28.5));
#113857=CARTESIAN_POINT('',(6.57735026918963,12.9,29.5));
#113858=CARTESIAN_POINT('',(7.15470053837925,12.9,28.5));
#113859=CARTESIAN_POINT('',(6.57735026918963,14.,29.5));
#113860=CARTESIAN_POINT('Origin',(6.57735026918963,14.,27.5));
#113861=CARTESIAN_POINT('',(6.72168783648703,14.,27.75));
#113862=CARTESIAN_POINT('',(6.57735026918963,12.9,27.5));
#113863=CARTESIAN_POINT('',(6.57735026918963,14.,27.5));
#113864=CARTESIAN_POINT('',(6.57735026918963,12.9,27.5));
#113865=CARTESIAN_POINT('Origin',(5.42264973081037,14.,27.5));
#113866=CARTESIAN_POINT('',(5.71132486540519,14.,27.5));
#113867=CARTESIAN_POINT('',(5.42264973081037,12.9,27.5));
#113868=CARTESIAN_POINT('',(5.42264973081037,14.,27.5));
#113869=CARTESIAN_POINT('',(5.42264973081037,12.9,27.5));
#113870=CARTESIAN_POINT('Origin',(6.,14.,28.5));
#113871=CARTESIAN_POINT('Origin',(6.,14.,28.5));
#113872=CARTESIAN_POINT('Origin',(6.,14.,28.5));
#113873=CARTESIAN_POINT('',(4.98963702891815,14.,28.25));
#113874=CARTESIAN_POINT('Origin',(6.,14.,28.5));
#113875=CARTESIAN_POINT('Origin',(6.,14.,28.5));
#113876=CARTESIAN_POINT('',(5.27831216351297,14.,29.25));
#113877=CARTESIAN_POINT('Origin',(6.,14.,28.5));
#113878=CARTESIAN_POINT('',(6.28867513459481,14.,29.5));
#113879=CARTESIAN_POINT('Origin',(7.15470053837925,12.9,28.5));
#113880=CARTESIAN_POINT('',(4.84529946162075,12.9,28.5));
#113881=CARTESIAN_POINT('',(4.84529946162075,12.9,28.5));
#113882=CARTESIAN_POINT('Origin',(6.,12.9,28.5));
#113883=CARTESIAN_POINT('Origin',(7.15470053837925,12.9,28.5));
#113884=CARTESIAN_POINT('Origin',(6.,12.9,28.5));
#113885=CARTESIAN_POINT('Origin',(7.15470053837925,12.9,28.5));
#113886=CARTESIAN_POINT('Origin',(6.,12.9,28.5));
#113887=CARTESIAN_POINT('Origin',(7.15470053837925,12.9,28.5));
#113888=CARTESIAN_POINT('Origin',(6.,12.9,28.5));
#113889=CARTESIAN_POINT('Origin',(7.15470053837925,12.9,28.5));
#113890=CARTESIAN_POINT('',(5.42264973081037,12.9,29.5));
#113891=CARTESIAN_POINT('',(6.57735026918963,12.9,29.5));
#113892=CARTESIAN_POINT('Origin',(6.,12.9,28.5));
#113893=CARTESIAN_POINT('Origin',(7.15470053837925,12.9,28.5));
#113894=CARTESIAN_POINT('',(5.42264973081037,12.9,29.5));
#113895=CARTESIAN_POINT('Origin',(6.,12.9,28.5));
#113896=CARTESIAN_POINT('Origin',(6.,12.9,28.5));
#113897=CARTESIAN_POINT('',(6.,12.206185919718,28.5));
#113898=CARTESIAN_POINT('',(4.84529946162075,12.9,28.5));
#113899=CARTESIAN_POINT('Origin',(4.84529946162075,14.,28.5));
#113900=CARTESIAN_POINT('',(4.84529946162075,14.,28.5));
#113901=CARTESIAN_POINT('Origin',(5.42264973081037,14.,29.5));
#113902=CARTESIAN_POINT('',(5.42264973081037,14.,29.5));
#113903=CARTESIAN_POINT('Origin',(6.57735026918963,14.,29.5));
#113962=UNCERTAINTY_MEASURE_WITH_UNIT(LENGTH_MEASURE(0.01),#113985,
'DISTANCE_ACCURACY_VALUE',
'Maximum model space distance between geometric entities at asserted c
onnectivities');
#113964=UNCERTAINTY_MEASURE_WITH_UNIT(LENGTH_MEASURE(0.01),#113985,
'DISTANCE_ACCURACY_VALUE',
'Maximum model space distance between geometric entities at asserted c
onnectivities');
#113982=(
GEOMETRIC_REPRESENTATION_CONTEXT(3)
GLOBAL_UNCERTAINTY_ASSIGNED_CONTEXT((#113962))
GLOBAL_UNIT_ASSIGNED_CONTEXT((#113985,#113987,#113988))
REPRESENTATION_CONTEXT('','3D')
);
#113984=(
GEOMETRIC_REPRESENTATION_CONTEXT(3)
GLOBAL_UNCERTAINTY_ASSIGNED_CONTEXT((#113964))
GLOBAL_UNIT_ASSIGNED_CONTEXT((#113985,#113987,#113988))
REPRESENTATION_CONTEXT('','3D')
);
#113985=(
LENGTH_UNIT()
NAMED_UNIT(*)
SI_UNIT(.MILLI.,.METRE.)
);
#113987=(
NAMED_UNIT(*)
PLANE_ANGLE_UNIT()
SI_UNIT($,.RADIAN.)
);
#113988=(
NAMED_UNIT(*)
SI_UNIT($,.STERADIAN.)
SOLID_ANGLE_UNIT()
);
#114006=SHAPE_DEFINITION_REPRESENTATION(#114025,#114068);
#114025=PRODUCT_DEFINITION_SHAPE('',$,#114088);
#114068=SHAPE_REPRESENTATION('',(#63462),#113982);
#114070=PRODUCT_DEFINITION_CONTEXT('part definition',#114129,'design');
#114088=PRODUCT_DEFINITION('2026-10-05-09-52-12-383',
'ISO 4762 - M2.5 x 6 - 12.9 (Rack Screw)',#114107,#114070);
#114107=PRODUCT_DEFINITION_FORMATION('',$,#114148);
#114129=APPLICATION_CONTEXT(
'Core Data for Automotive Mechanical Design Process');
#114130=PRODUCT_CONTEXT('part definition',#114129,'mechanical');
#114148=PRODUCT('2026-10-05-09-52-12-383',
'ISO 4762 - M2.5 x 6 - 12.9 (Rack Screw)',$,(#114130));
#114311=COLOUR_RGB('Black',0.12,0.14,0.17);
#114312=FILL_AREA_STYLE_COLOUR('',#114311);
#114313=FILL_AREA_STYLE('',(#114312));
#114314=SURFACE_STYLE_FILL_AREA(#114313);
#114315=SURFACE_SIDE_STYLE('',(#114314));
#114316=SURFACE_STYLE_USAGE(.BOTH.,#114315);
#114317=PRESENTATION_STYLE_ASSIGNMENT((#114316));
ENDSEC;
END-ISO-10303-21;
